ISO-10303-21;
HEADER;
/* Generated by software containing ST-Developer
 * from STEP Tools, Inc. (www.steptools.com) 
 */

FILE_DESCRIPTION(
/* description */ (''),
/* implementation_level */ '2;1');

FILE_NAME(
/* name */ 'Socket head cap screw M3x16.step',
/* time_stamp */ '2026-11-10T09:05:57-08:00',
/* author */ (''),
/* organization */ (''),
/* preprocessor_version */ 'ST-DEVELOPER v20.2',
/* originating_system */ 'Autodesk Translation Framework v15.17.0.0',
/* authorisation */ '');

FILE_SCHEMA (('AUTOMOTIVE_DESIGN { 1 0 10303 214 3 1 1 }'));
ENDSEC;

DATA;
#10=MECHANICAL_DESIGN_GEOMETRIC_PRESENTATION_REPRESENTATION('',(#572),#19618);
#167=B_SPLINE_SURFACE_WITH_KNOTS('',3,3,((#16866,#16867,#16868,#16869,#16870,
#16871,#16872,#16873,#16874,#16875,#16876,#16877,#16878,#16879,#16880,#16881,
#16882,#16883,#16884,#16885,#16886,#16887,#16888,#16889,#16890,#16891,#16892,
#16893,#16894,#16895,#16896,#16897,#16898,#16899,#16900,#16901,#16902,#16903,
#16904,#16905,#16906,#16907,#16908,#16909,#16910,#16911,#16912,#16913,#16914,
#16915,#16916,#16917,#16918,#16919,#16920,#16921,#16922,#16923,#16924,#16925,
#16926,#16927,#16928,#16929,#16930,#16931,#16932,#16933,#16934,#16935,#16936,
#16937,#16938,#16939,#16940,#16941,#16942,#16943,#16944,#16945,#16946,#16947,
#16948,#16949,#16950,#16951,#16952,#16953,#16954,#16955,#16956,#16957,#16958,
#16959,#16960,#16961,#16962,#16963,#16964,#16965,#16966,#16967,#16968,#16969,
#16970,#16971,#16972,#16973,#16974,#16975,#16976,#16977,#16978,#16979,#16980,
#16981,#16982,#16983,#16984,#16985,#16986,#16987,#16988,#16989,#16990,#16991,
#16992,#16993,#16994,#16995,#16996,#16997,#16998,#16999,#17000,#17001,#17002,
#17003,#17004,#17005,#17006,#17007,#17008,#17009,#17010,#17011,#17012,#17013,
#17014,#17015,#17016,#17017,#17018,#17019,#17020,#17021,#17022,#17023,#17024,
#17025,#17026,#17027,#17028,#17029,#17030,#17031,#17032,#17033,#17034,#17035,
#17036,#17037,#17038,#17039,#17040,#17041,#17042,#17043,#17044,#17045,#17046,
#17047,#17048,#17049,#17050,#17051,#17052,#17053,#17054,#17055,#17056,#17057,
#17058,#17059,#17060,#17061),(#17062,#17063,#17064,#17065,#17066,#17067,
#17068,#17069,#17070,#17071,#17072,#17073,#17074,#17075,#17076,#17077,#17078,
#17079,#17080,#17081,#17082,#17083,#17084,#17085,#17086,#17087,#17088,#17089,
#17090,#17091,#17092,#17093,#17094,#17095,#17096,#17097,#17098,#17099,#17100,
#17101,#17102,#17103,#17104,#17105,#17106,#17107,#17108,#17109,#17110,#17111,
#17112,#17113,#17114,#17115,#17116,#17117,#17118,#17119,#17120,#17121,#17122,
#17123,#17124,#17125,#17126,#17127,#17128,#17129,#17130,#17131,#17132,#17133,
#17134,#17135,#17136,#17137,#17138,#17139,#17140,#17141,#17142,#17143,#17144,
#17145,#17146,#17147,#17148,#17149,#17150,#17151,#17152,#17153,#17154,#17155,
#17156,#17157,#17158,#17159,#17160,#17161,#17162,#17163,#17164,#17165,#17166,
#17167,#17168,#17169,#17170,#17171,#17172,#17173,#17174,#17175,#17176,#17177,
#17178,#17179,#17180,#17181,#17182,#17183,#17184,#17185,#17186,#17187,#17188,
#17189,#17190,#17191,#17192,#17193,#17194,#17195,#17196,#17197,#17198,#17199,
#17200,#17201,#17202,#17203,#17204,#17205,#17206,#17207,#17208,#17209,#17210,
#17211,#17212,#17213,#17214,#17215,#17216,#17217,#17218,#17219,#17220,#17221,
#17222,#17223,#17224,#17225,#17226,#17227,#17228,#17229,#17230,#17231,#17232,
#17233,#17234,#17235,#17236,#17237,#17238,#17239,#17240,#17241,#17242,#17243,
#17244,#17245,#17246,#17247,#17248,#17249,#17250,#17251,#17252,#17253,#17254,
#17255,#17256,#17257),(#17258,#17259,#17260,#17261,#17262,#17263,#17264,
#17265,#17266,#17267,#17268,#17269,#17270,#17271,#17272,#17273,#17274,#17275,
#17276,#17277,#17278,#17279,#17280,#17281,#17282,#17283,#17284,#17285,#17286,
#17287,#17288,#17289,#17290,#17291,#17292,#17293,#17294,#17295,#17296,#17297,
#17298,#17299,#17300,#17301,#17302,#17303,#17304,#17305,#17306,#17307,#17308,
#17309,#17310,#17311,#17312,#17313,#17314,#17315,#17316,#17317,#17318,#17319,
#17320,#17321,#17322,#17323,#17324,#17325,#17326,#17327,#17328,#17329,#17330,
#17331,#17332,#17333,#17334,#17335,#17336,#17337,#17338,#17339,#17340,#17341,
#17342,#17343,#17344,#17345,#17346,#17347,#17348,#17349,#17350,#17351,#17352,
#17353,#17354,#17355,#17356,#17357,#17358,#17359,#17360,#17361,#17362,#17363,
#17364,#17365,#17366,#17367,#17368,#17369,#17370,#17371,#17372,#17373,#17374,
#17375,#17376,#17377,#17378,#17379,#17380,#17381,#17382,#17383,#17384,#17385,
#17386,#17387,#17388,#17389,#17390,#17391,#17392,#17393,#17394,#17395,#17396,
#17397,#17398,#17399,#17400,#17401,#17402,#17403,#17404,#17405,#17406,#17407,
#17408,#17409,#17410,#17411,#17412,#17413,#17414,#17415,#17416,#17417,#17418,
#17419,#17420,#17421,#17422,#17423,#17424,#17425,#17426,#17427,#17428,#17429,
#17430,#17431,#17432,#17433,#17434,#17435,#17436,#17437,#17438,#17439,#17440,
#17441,#17442,#17443,#17444,#17445,#17446,#17447,#17448,#17449,#17450,#17451,
#17452,#17453),(#17454,#17455,#17456,#17457,#17458,#17459,#17460,#17461,
#17462,#17463,#17464,#17465,#17466,#17467,#17468,#17469,#17470,#17471,#17472,
#17473,#17474,#17475,#17476,#17477,#17478,#17479,#17480,#17481,#17482,#17483,
#17484,#17485,#17486,#17487,#17488,#17489,#17490,#17491,#17492,#17493,#17494,
#17495,#17496,#17497,#17498,#17499,#17500,#17501,#17502,#17503,#17504,#17505,
#17506,#17507,#17508,#17509,#17510,#17511,#17512,#17513,#17514,#17515,#17516,
#17517,#17518,#17519,#17520,#17521,#17522,#17523,#17524,#17525,#17526,#17527,
#17528,#17529,#17530,#17531,#17532,#17533,#17534,#17535,#17536,#17537,#17538,
#17539,#17540,#17541,#17542,#17543,#17544,#17545,#17546,#17547,#17548,#17549,
#17550,#17551,#17552,#17553,#17554,#17555,#17556,#17557,#17558,#17559,#17560,
#17561,#17562,#17563,#17564,#17565,#17566,#17567,#17568,#17569,#17570,#17571,
#17572,#17573,#17574,#17575,#17576,#17577,#17578,#17579,#17580,#17581,#17582,
#17583,#17584,#17585,#17586,#17587,#17588,#17589,#17590,#17591,#17592,#17593,
#17594,#17595,#17596,#17597,#17598,#17599,#17600,#17601,#17602,#17603,#17604,
#17605,#17606,#17607,#17608,#17609,#17610,#17611,#17612,#17613,#17614,#17615,
#17616,#17617,#17618,#17619,#17620,#17621,#17622,#17623,#17624,#17625,#17626,
#17627,#17628,#17629,#17630,#17631,#17632,#17633,#17634,#17635,#17636,#17637,
#17638,#17639,#17640,#17641,#17642,#17643,#17644,#17645,#17646,#17647,#17648,
#17649)),.UNSPECIFIED.,.F.,.F.,.F.,(4,4),(4,1,1,1,1,1,1,1,1,1,1,1,1,1,1,
1,1,1,1,1,1,1,1,1,1,1,1,1,1,1,1,1,1,1,1,1,1,1,1,1,1,1,1,1,1,1,1,1,1,1,1,
1,1,1,1,1,1,1,1,1,1,1,1,1,1,1,1,1,1,1,1,1,1,1,1,1,1,1,1,1,1,1,1,1,1,1,1,
1,1,1,1,1,1,1,1,1,1,1,1,1,1,1,1,1,1,1,1,1,1,1,1,1,1,1,1,1,1,1,1,1,1,1,1,
1,1,1,1,1,1,1,1,1,1,1,1,1,1,1,1,1,1,1,1,1,1,1,1,1,1,1,1,1,1,1,1,1,1,1,1,
1,1,1,1,1,1,1,1,1,1,1,1,1,1,1,1,1,1,1,1,1,1,1,1,1,1,1,1,1,1,1,1,1,1,4),
(0.,0.0329955678841871),(11.6159397475006,12.61358260836,13.6112254692194,
14.6088683300789,15.6065111909383,16.6041540517977,17.6017969126571,18.5994397735165,
19.5970826343759,20.5947254952353,21.5923683560947,22.5900112169541,23.5876540778135,
24.5852969386729,25.5829397995323,26.5805826603917,27.5782255212511,28.5758683821105,
29.5735112429699,30.5711541038294,31.5687969646888,32.5664398255482,33.5640826864076,
34.561725547267,35.5593684081264,36.5570112689858,37.5546541298452,38.5522969907046,
39.549939851564,40.5475827124234,41.5452255732828,42.5428684341422,43.5405112950016,
44.538154155861,45.5357970167204,46.5334398775799,47.5310827384393,48.5287255992987,
49.5263684601581,50.5240113210175,51.5216541818769,52.5192970427363,53.5169399035957,
54.5145827644551,55.5122256253145,56.5098684861739,57.5075113470333,58.5051542078927,
59.5027970687521,60.5004399296115,61.4980827904709,62.4957256513303,63.4933685121897,
64.4910113730492,65.4886542339086,66.486297094768,67.4839399556274,68.4815828164868,
69.4792256773462,70.4768685382056,71.474511399065,72.4721542599244,73.4697971207838,
74.4674399816432,75.4650828425026,76.462725703362,77.4603685642214,78.4580114250808,
79.4556542859402,80.4532971467996,81.4509400076591,82.4485828685185,83.4462257293779,
84.4438685902373,85.4415114510967,86.4391543119561,87.4367971728155,88.4344400336749,
89.4320828945343,90.4297257553937,91.4273686162531,92.4250114771125,93.4226543379719,
94.4202971988313,95.4179400596907,96.4155829205502,97.4132257814096,98.410868642269,
99.4085115031284,100.406154363988,101.403797224847,102.401440085707,103.399082946566,
104.396725807425,105.394368668285,106.392011529144,107.389654390004,108.387297250863,
109.384940111722,110.382582972582,111.380225833441,112.377868694301,113.37551155516,
114.373154416019,115.370797276879,116.368440137738,117.366082998598,118.363725859457,
119.361368720316,120.359011581176,121.356654442035,122.354297302895,123.351940163754,
124.349583024614,125.347225885473,126.344868746332,127.342511607192,128.340154468051,
129.337797328911,130.33544018977,131.333083050629,132.330725911489,133.328368772348,
134.326011633208,135.323654494067,136.321297354926,137.318940215786,138.316583076645,
139.314225937505,140.311868798364,141.309511659223,142.307154520083,143.304797380942,
144.302440241802,145.300083102661,146.29772596352,147.29536882438,148.293011685239,
149.290654546099,150.288297406958,151.285940267817,152.283583128677,153.281225989536,
154.278868850396,155.276511711255,156.274154572115,157.271797432974,158.269440293833,
159.267083154693,160.264726015552,161.262368876412,162.260011737271,163.25765459813,
164.25529745899,165.252940319849,166.250583180709,167.248226041568,168.245868902427,
169.243511763287,170.241154624146,171.238797485006,172.236440345865,173.234083206724,
174.231726067584,175.229368928443,176.227011789303,177.224654650162,178.222297511021,
179.219940371881,180.21758323274,181.2152260936,182.212868954459,183.210511815318,
184.208154676178,185.205797537037,186.203440397897,187.201083258756,188.198726119616,
189.196368980475,190.194011841334,191.191654702194,192.189297563053,193.186940423913,
194.184583284772,195.182226145631,196.179869006491,197.17751186735,198.17515472821,
199.172797589069,200.170440449928,201.168083310788,202.165726171647,203.163369032507,
204.161011893366),.UNSPECIFIED.);
#168=B_SPLINE_SURFACE_WITH_KNOTS('',3,3,((#17739,#17740,#17741,#17742,#17743,
#17744,#17745,#17746,#17747,#17748,#17749,#17750,#17751,#17752,#17753,#17754,
#17755,#17756,#17757,#17758,#17759,#17760,#17761,#17762,#17763,#17764,#17765,
#17766,#17767,#17768,#17769,#17770,#17771,#17772,#17773,#17774,#17775,#17776,
#17777,#17778,#17779,#17780,#17781,#17782,#17783,#17784,#17785,#17786,#17787,
#17788,#17789,#17790,#17791,#17792,#17793,#17794,#17795,#17796,#17797,#17798,
#17799,#17800,#17801,#17802,#17803,#17804,#17805,#17806,#17807,#17808,#17809,
#17810,#17811,#17812,#17813,#17814,#17815,#17816,#17817,#17818,#17819,#17820,
#17821,#17822,#17823,#17824,#17825,#17826,#17827,#17828,#17829,#17830,#17831,
#17832,#17833,#17834,#17835,#17836,#17837,#17838,#17839,#17840,#17841,#17842,
#17843,#17844,#17845,#17846,#17847,#17848,#17849,#17850,#17851,#17852,#17853,
#17854,#17855,#17856,#17857,#17858,#17859,#17860,#17861,#17862,#17863,#17864,
#17865,#17866,#17867,#17868,#17869,#17870,#17871,#17872,#17873,#17874,#17875,
#17876,#17877,#17878,#17879,#17880,#17881,#17882,#17883,#17884,#17885,#17886,
#17887,#17888,#17889,#17890,#17891,#17892,#17893,#17894,#17895,#17896,#17897,
#17898,#17899,#17900,#17901,#17902,#17903,#17904,#17905,#17906,#17907,#17908,
#17909,#17910,#17911,#17912,#17913,#17914,#17915,#17916,#17917,#17918,#17919,
#17920,#17921,#17922,#17923,#17924,#17925,#17926,#17927,#17928,#17929,#17930,
#17931,#17932,#17933,#17934,#17935,#17936),(#17937,#17938,#17939,#17940,
#17941,#17942,#17943,#17944,#17945,#17946,#17947,#17948,#17949,#17950,#17951,
#17952,#17953,#17954,#17955,#17956,#17957,#17958,#17959,#17960,#17961,#17962,
#17963,#17964,#17965,#17966,#17967,#17968,#17969,#17970,#17971,#17972,#17973,
#17974,#17975,#17976,#17977,#17978,#17979,#17980,#17981,#17982,#17983,#17984,
#17985,#17986,#17987,#17988,#17989,#17990,#17991,#17992,#17993,#17994,#17995,
#17996,#17997,#17998,#17999,#18000,#18001,#18002,#18003,#18004,#18005,#18006,
#18007,#18008,#18009,#18010,#18011,#18012,#18013,#18014,#18015,#18016,#18017,
#18018,#18019,#18020,#18021,#18022,#18023,#18024,#18025,#18026,#18027,#18028,
#18029,#18030,#18031,#18032,#18033,#18034,#18035,#18036,#18037,#18038,#18039,
#18040,#18041,#18042,#18043,#18044,#18045,#18046,#18047,#18048,#18049,#18050,
#18051,#18052,#18053,#18054,#18055,#18056,#18057,#18058,#18059,#18060,#18061,
#18062,#18063,#18064,#18065,#18066,#18067,#18068,#18069,#18070,#18071,#18072,
#18073,#18074,#18075,#18076,#18077,#18078,#18079,#18080,#18081,#18082,#18083,
#18084,#18085,#18086,#18087,#18088,#18089,#18090,#18091,#18092,#18093,#18094,
#18095,#18096,#18097,#18098,#18099,#18100,#18101,#18102,#18103,#18104,#18105,
#18106,#18107,#18108,#18109,#18110,#18111,#18112,#18113,#18114,#18115,#18116,
#18117,#18118,#18119,#18120,#18121,#18122,#18123,#18124,#18125,#18126,#18127,
#18128,#18129,#18130,#18131,#18132,#18133,#18134),(#18135,#18136,#18137,
#18138,#18139,#18140,#18141,#18142,#18143,#18144,#18145,#18146,#18147,#18148,
#18149,#18150,#18151,#18152,#18153,#18154,#18155,#18156,#18157,#18158,#18159,
#18160,#18161,#18162,#18163,#18164,#18165,#18166,#18167,#18168,#18169,#18170,
#18171,#18172,#18173,#18174,#18175,#18176,#18177,#18178,#18179,#18180,#18181,
#18182,#18183,#18184,#18185,#18186,#18187,#18188,#18189,#18190,#18191,#18192,
#18193,#18194,#18195,#18196,#18197,#18198,#18199,#18200,#18201,#18202,#18203,
#18204,#18205,#18206,#18207,#18208,#18209,#18210,#18211,#18212,#18213,#18214,
#18215,#18216,#18217,#18218,#18219,#18220,#18221,#18222,#18223,#18224,#18225,
#18226,#18227,#18228,#18229,#18230,#18231,#18232,#18233,#18234,#18235,#18236,
#18237,#18238,#18239,#18240,#18241,#18242,#18243,#18244,#18245,#18246,#18247,
#18248,#18249,#18250,#18251,#18252,#18253,#18254,#18255,#18256,#18257,#18258,
#18259,#18260,#18261,#18262,#18263,#18264,#18265,#18266,#18267,#18268,#18269,
#18270,#18271,#18272,#18273,#18274,#18275,#18276,#18277,#18278,#18279,#18280,
#18281,#18282,#18283,#18284,#18285,#18286,#18287,#18288,#18289,#18290,#18291,
#18292,#18293,#18294,#18295,#18296,#18297,#18298,#18299,#18300,#18301,#18302,
#18303,#18304,#18305,#18306,#18307,#18308,#18309,#18310,#18311,#18312,#18313,
#18314,#18315,#18316,#18317,#18318,#18319,#18320,#18321,#18322,#18323,#18324,
#18325,#18326,#18327,#18328,#18329,#18330,#18331,#18332),(#18333,#18334,
#18335,#18336,#18337,#18338,#18339,#18340,#18341,#18342,#18343,#18344,#18345,
#18346,#18347,#18348,#18349,#18350,#18351,#18352,#18353,#18354,#18355,#18356,
#18357,#18358,#18359,#18360,#18361,#18362,#18363,#18364,#18365,#18366,#18367,
#18368,#18369,#18370,#18371,#18372,#18373,#18374,#18375,#18376,#18377,#18378,
#18379,#18380,#18381,#18382,#18383,#18384,#18385,#18386,#18387,#18388,#18389,
#18390,#18391,#18392,#18393,#18394,#18395,#18396,#18397,#18398,#18399,#18400,
#18401,#18402,#18403,#18404,#18405,#18406,#18407,#18408,#18409,#18410,#18411,
#18412,#18413,#18414,#18415,#18416,#18417,#18418,#18419,#18420,#18421,#18422,
#18423,#18424,#18425,#18426,#18427,#18428,#18429,#18430,#18431,#18432,#18433,
#18434,#18435,#18436,#18437,#18438,#18439,#18440,#18441,#18442,#18443,#18444,
#18445,#18446,#18447,#18448,#18449,#18450,#18451,#18452,#18453,#18454,#18455,
#18456,#18457,#18458,#18459,#18460,#18461,#18462,#18463,#18464,#18465,#18466,
#18467,#18468,#18469,#18470,#18471,#18472,#18473,#18474,#18475,#18476,#18477,
#18478,#18479,#18480,#18481,#18482,#18483,#18484,#18485,#18486,#18487,#18488,
#18489,#18490,#18491,#18492,#18493,#18494,#18495,#18496,#18497,#18498,#18499,
#18500,#18501,#18502,#18503,#18504,#18505,#18506,#18507,#18508,#18509,#18510,
#18511,#18512,#18513,#18514,#18515,#18516,#18517,#18518,#18519,#18520,#18521,
#18522,#18523,#18524,#18525,#18526,#18527,#18528,#18529,#18530)),
 .UNSPECIFIED.,.F.,.F.,.F.,(4,4),(4,1,1,1,1,1,1,1,1,1,1,1,1,1,1,1,1,1,1,
1,1,1,1,1,1,1,1,1,1,1,1,1,1,1,1,1,1,1,1,1,1,1,1,1,1,1,1,1,1,1,1,1,1,1,1,
1,1,1,1,1,1,1,1,1,1,1,1,1,1,1,1,1,1,1,1,1,1,1,1,1,1,1,1,1,1,1,1,1,1,1,1,
1,1,1,1,1,1,1,1,1,1,1,1,1,1,1,1,1,1,1,1,1,1,1,1,1,1,1,1,1,1,1,1,1,1,1,1,
1,1,1,1,1,1,1,1,1,1,1,1,1,1,1,1,1,1,1,1,1,1,1,1,1,1,1,1,1,1,1,1,1,1,1,1,
1,1,1,1,1,1,1,1,1,1,1,1,1,1,1,1,1,1,1,1,1,1,1,1,1,1,1,1,1,1,1,1,4),(0.,
0.0329955678841871),(8.30203615430855,9.30007843543257,10.2981207165566,
11.2961629976806,12.2942052788047,13.2922475599287,14.2902898410527,15.2883321221767,
16.2863744033008,17.2844166844248,18.2824589655488,19.2805012466728,20.2785435277969,
21.2765858089209,22.2746280900449,23.272670371169,24.270712652293,25.268754933417,
26.266797214541,27.2648394956651,28.2628817767891,29.2609240579131,30.2589663390371,
31.2570086201612,32.2550509012852,33.2530931824092,34.2511354635333,35.2491777446573,
36.2472200257813,37.2452623069053,38.2433045880294,39.2413468691534,40.2393891502774,
41.2374314314014,42.2354737125255,43.2335159936495,44.2315582747735,45.2296005558975,
46.2276428370216,47.2256851181456,48.2237273992696,49.2217696803937,50.2198119615177,
51.2178542426417,52.2158965237657,53.2139388048898,54.2119810860138,55.2100233671378,
56.2080656482619,57.2061079293859,58.2041502105099,59.2021924916339,60.200234772758,
61.198277053882,62.196319335006,63.19436161613,64.1924038972541,65.1904461783781,
66.1884884595021,67.1865307406262,68.1845730217502,69.1826153028742,70.1806575839982,
71.1786998651223,72.1767421462463,73.1747844273703,74.1728267084943,75.1708689896184,
76.1689112707424,77.1669535518664,78.1649958329905,79.1630381141145,80.1610803952385,
81.1591226763625,82.1571649574865,83.1552072386106,84.1532495197346,85.1512918008586,
86.1493340819827,87.1473763631067,88.1454186442307,89.1434609253548,90.1415032064788,
91.1395454876028,92.1375877687268,93.1356300498508,94.1336723309749,95.1317146120989,
96.1297568932229,97.127799174347,98.125841455471,99.123883736595,100.121926017719,
101.119968298843,102.118010579967,103.116052861091,104.114095142215,105.112137423339,
106.110179704463,107.108221985587,108.106264266711,109.104306547835,110.102348828959,
111.100391110083,112.098433391207,113.096475672331,114.094517953455,115.092560234579,
116.090602515703,117.088644796828,118.086687077952,119.084729359076,120.0827716402,
121.080813921324,122.078856202448,123.076898483572,124.074940764696,125.07298304582,
126.071025326944,127.069067608068,128.067109889192,129.065152170316,130.06319445144,
131.061236732564,132.059279013688,133.057321294812,134.055363575936,135.05340585706,
136.051448138184,137.049490419308,138.047532700432,139.045574981556,140.04361726268,
141.041659543804,142.039701824928,143.037744106052,144.035786387176,145.0338286683,
146.031870949424,147.029913230548,148.027955511672,149.025997792796,150.02404007392,
151.022082355044,152.020124636168,153.018166917292,154.016209198417,155.014251479541,
156.012293760665,157.010336041789,158.008378322913,159.006420604037,160.004462885161,
161.002505166285,162.000547447409,162.998589728533,163.996632009657,164.994674290781,
165.992716571905,166.990758853029,167.988801134153,168.986843415277,169.984885696401,
170.982927977525,171.980970258649,172.979012539773,173.977054820897,174.975097102021,
175.973139383145,176.971181664269,177.969223945393,178.967266226517,179.965308507641,
180.963350788765,181.961393069889,182.959435351013,183.957477632137,184.955519913261,
185.953562194385,186.951604475509,187.949646756633,188.947689037757,189.945731318881,
190.943773600006,191.94181588113,192.939858162254,193.937900443378,194.935942724502,
195.933985005626,196.93202728675,197.930069567874,198.928111848998,199.926154130122,
200.924196411246,201.92223869237,202.920280973494),.UNSPECIFIED.);
#389=B_SPLINE_CURVE_WITH_KNOTS('',3,(#14490,#14491,#14492,#14493,#14494,
#14495,#14496,#14497,#14498,#14499),.UNSPECIFIED.,.F.,.F.,(4,3,3,4),(-4.09202352044852,
-3.99057144343763,-2.99292858257822,-2.07317267331971),.UNSPECIFIED.);
#390=B_SPLINE_CURVE_WITH_KNOTS('',3,(#14502,#14503,#14504,#14505,#14506,
#14507,#14508),.UNSPECIFIED.,.F.,.F.,(4,3,4),(0.,0.998042281124014,1.12274180646116),
 .UNSPECIFIED.);
#391=B_SPLINE_CURVE_WITH_KNOTS('',3,(#14513,#14514,#14515,#14516,#14517,
#14518,#14519,#14520,#14521,#14522,#14523,#14524,#14525,#14526,#14527,#14528,
#14529,#14530,#14531,#14532,#14533,#14534),.UNSPECIFIED.,.F.,.F.,(4,3,3,
3,3,3,3,4),(-10.3752088276281,-9.97642860859406,-8.97878574773466,-7.98114288687525,
-6.98350002601584,-5.98585716515644,-4.98821430429703,-4.09202352044852),
 .UNSPECIFIED.);
#392=B_SPLINE_CURVE_WITH_KNOTS('',3,(#14535,#14536,#14537,#14538,#14539,
#14540,#14541,#14542,#14543,#14544,#14545,#14546,#14547,#14548,#14549,#14550,
#14551,#14552,#14553,#14554,#14555,#14556),.UNSPECIFIED.,.F.,.F.,(4,3,3,
3,3,3,3,4),(1.12274180646116,1.99608456224804,2.99412684337208,3.99216912449611,
4.99021140562014,5.98825368674417,6.98629596786821,7.40592711364074),
 .UNSPECIFIED.);
#393=B_SPLINE_CURVE_WITH_KNOTS('',3,(#14561,#14562,#14563,#14564,#14565,
#14566,#14567,#14568,#14569,#14570,#14571,#14572,#14573,#14574,#14575,#14576,
#14577,#14578,#14579,#14580,#14581,#14582),.UNSPECIFIED.,.F.,.F.,(4,3,3,
3,3,3,3,4),(-16.6583941348077,-15.9622857737505,-14.9646429128911,-13.9670000520317,
-12.9693571911723,-11.9717143303129,-10.9740714694535,-10.3752088276281),
 .UNSPECIFIED.);
#394=B_SPLINE_CURVE_WITH_KNOTS('',3,(#14583,#14584,#14585,#14586,#14587,
#14588,#14589,#14590,#14591,#14592,#14593,#14594,#14595,#14596,#14597,#14598,
#14599,#14600,#14601,#14602,#14603,#14604),.UNSPECIFIED.,.F.,.F.,(4,3,3,
3,3,3,3,4),(7.40592711364074,7.98433824899223,8.98238053011626,9.98042281124028,
10.9784650923643,11.9765073734883,12.9745496546124,13.6891124208203),
 .UNSPECIFIED.);
#395=B_SPLINE_CURVE_WITH_KNOTS('',3,(#14609,#14610,#14611,#14612,#14613,
#14614,#14615,#14616,#14617,#14618,#14619,#14620,#14621,#14622,#14623,#14624,
#14625,#14626,#14627,#14628,#14629,#14630),.UNSPECIFIED.,.F.,.F.,(4,3,3,
3,3,3,3,4),(-22.9415794419873,-21.9481429389069,-20.9505000780475,-19.9528572171881,
-18.9552143563287,-17.9575714954693,-16.9599286346099,-16.6583941348077),
 .UNSPECIFIED.);
#396=B_SPLINE_CURVE_WITH_KNOTS('',3,(#14631,#14632,#14633,#14634,#14635,
#14636,#14637,#14638,#14639,#14640,#14641,#14642,#14643,#14644,#14645,#14646,
#14647,#14648,#14649,#14650,#14651,#14652,#14653,#14654,#14655),
 .UNSPECIFIED.,.F.,.F.,(4,3,3,3,3,3,3,3,4),(13.6891124208203,13.9725919357364,
14.9706342168604,15.9686764979844,16.9667187791085,17.9647610602325,18.9628033413565,
19.9608456224805,19.9722977279999),.UNSPECIFIED.);
#397=B_SPLINE_CURVE_WITH_KNOTS('',3,(#14660,#14661,#14662,#14663,#14664,
#14665,#14666,#14667,#14668,#14669,#14670,#14671,#14672,#14673,#14674,#14675,
#14676,#14677,#14678,#14679,#14680,#14681),.UNSPECIFIED.,.F.,.F.,(4,3,3,
3,3,3,3,4),(-29.2247647491669,-28.9316429649228,-27.9340001040634,-26.936357243204,
-25.9387143823446,-24.9410715214852,-23.9434286606257,-22.9415794419873),
 .UNSPECIFIED.);
#398=B_SPLINE_CURVE_WITH_KNOTS('',3,(#14682,#14683,#14684,#14685,#14686,
#14687,#14688,#14689,#14690,#14691,#14692,#14693,#14694,#14695,#14696,#14697,
#14698,#14699,#14700,#14701,#14702,#14703),.UNSPECIFIED.,.F.,.F.,(4,3,3,
3,3,3,3,4),(19.9722977279999,20.9588879036046,21.9569301847286,22.9549724658526,
23.9530147469767,24.9510570281007,25.9490993092247,26.2554830351795),
 .UNSPECIFIED.);
#399=B_SPLINE_CURVE_WITH_KNOTS('',3,(#14708,#14709,#14710,#14711,#14712,
#14713,#14714,#14715,#14716,#14717,#14718,#14719,#14720,#14721,#14722,#14723,
#14724,#14725,#14726,#14727,#14728,#14729),.UNSPECIFIED.,.F.,.F.,(4,3,3,
3,3,3,3,4),(-35.5079500563465,-34.9175001300792,-33.9198572692198,-32.9222144083604,
-31.924571547501,-30.9269286866416,-29.9292858257822,-29.2247647491669),
 .UNSPECIFIED.);
#400=B_SPLINE_CURVE_WITH_KNOTS('',3,(#14730,#14731,#14732,#14733,#14734,
#14735,#14736,#14737,#14738,#14739,#14740,#14741,#14742,#14743,#14744,#14745,
#14746,#14747,#14748,#14749,#14750,#14751),.UNSPECIFIED.,.F.,.F.,(4,3,3,
3,3,3,3,4),(26.2554830351795,26.9471415903487,27.9451838714728,28.9432261525968,
29.9412684337208,30.9393107148448,31.9373529959689,32.5386683423591),
 .UNSPECIFIED.);
#401=B_SPLINE_CURVE_WITH_KNOTS('',3,(#14756,#14757,#14758,#14759,#14760,
#14761,#14762,#14763,#14764,#14765,#14766,#14767,#14768,#14769,#14770,#14771,
#14772,#14773,#14774,#14775,#14776,#14777),.UNSPECIFIED.,.F.,.F.,(4,3,3,
3,3,3,3,4),(-41.791135363526,-40.9033572952357,-39.9057144343762,-38.9080715735168,
-37.9104287126574,-36.912785851798,-35.9151429909386,-35.5079500563465),
 .UNSPECIFIED.);
#402=B_SPLINE_CURVE_WITH_KNOTS('',3,(#14778,#14779,#14780,#14781,#14782,
#14783,#14784,#14785,#14786,#14787,#14788,#14789,#14790,#14791,#14792,#14793,
#14794,#14795,#14796,#14797,#14798,#14799),.UNSPECIFIED.,.F.,.F.,(4,3,3,
3,3,3,3,4),(32.5386683423591,32.9353952770929,33.9334375582169,34.931479839341,
35.929522120465,36.927564401589,37.9256066827131,38.8218536495387),
 .UNSPECIFIED.);
#403=B_SPLINE_CURVE_WITH_KNOTS('',3,(#14804,#14805,#14806,#14807,#14808,
#14809,#14810,#14811,#14812,#14813,#14814,#14815,#14816,#14817,#14818,#14819,
#14820,#14821,#14822,#14823,#14824,#14825,#14826,#14827,#14828),
 .UNSPECIFIED.,.F.,.F.,(4,3,3,3,3,3,3,3,4),(-48.0743206707056,-47.8868573212515,
-46.8892144603921,-45.8915715995327,-44.8939287386733,-43.8962858778139,
-42.8986430169545,-41.9010001560951,-41.791135363526),.UNSPECIFIED.);
#404=B_SPLINE_CURVE_WITH_KNOTS('',3,(#14829,#14830,#14831,#14832,#14833,
#14834,#14835,#14836,#14837,#14838,#14839,#14840,#14841,#14842,#14843,#14844,
#14845,#14846,#14847,#14848,#14849,#14850,#14851,#14852,#14853),
 .UNSPECIFIED.,.F.,.F.,(4,3,3,3,3,3,3,3,4),(38.8218536495387,38.9236489638371,
39.9216912449611,40.9197335260851,41.9177758072091,42.9158180883332,43.9138603694572,
44.9119026505812,45.1050389567183),.UNSPECIFIED.);
#405=B_SPLINE_CURVE_WITH_KNOTS('',3,(#14858,#14859,#14860,#14861,#14862,
#14863,#14864,#14865,#14866,#14867,#14868,#14869,#14870,#14871,#14872,#14873,
#14874,#14875,#14876,#14877,#14878,#14879),.UNSPECIFIED.,.F.,.F.,(4,3,3,
3,3,3,3,4),(-54.3575059778852,-53.8727144864079,-52.8750716255485,-51.8774287646891,
-50.8797859038297,-49.8821430429703,-48.8845001821109,-48.0743206707056),
 .UNSPECIFIED.);
#406=B_SPLINE_CURVE_WITH_KNOTS('',3,(#14880,#14881,#14882,#14883,#14884,
#14885,#14886,#14887,#14888,#14889,#14890,#14891,#14892,#14893,#14894,#14895,
#14896,#14897,#14898,#14899,#14900,#14901),.UNSPECIFIED.,.F.,.F.,(4,3,3,
3,3,3,3,4),(45.1050389567183,45.9099449317052,46.9079872128293,47.9060294939533,
48.9040717750773,49.9021140562014,50.9001563373254,51.3882242638979),
 .UNSPECIFIED.);
#407=B_SPLINE_CURVE_WITH_KNOTS('',3,(#14906,#14907,#14908,#14909,#14910,
#14911,#14912,#14913,#14914,#14915,#14916,#14917,#14918,#14919,#14920,#14921,
#14922,#14923,#14924,#14925,#14926,#14927),.UNSPECIFIED.,.F.,.F.,(4,3,3,
3,3,3,3,4),(-60.6406912850648,-59.8585716515644,-58.860928790705,-57.8632859298455,
-56.8656430689861,-55.8680002081267,-54.8703573472673,-54.3575059778852),
 .UNSPECIFIED.);
#408=B_SPLINE_CURVE_WITH_KNOTS('',3,(#14928,#14929,#14930,#14931,#14932,
#14933,#14934,#14935,#14936,#14937,#14938,#14939,#14940,#14941,#14942,#14943,
#14944,#14945,#14946,#14947,#14948,#14949),.UNSPECIFIED.,.F.,.F.,(4,3,3,
3,3,3,3,4),(51.3882242638979,51.8981986184494,52.8962408995734,53.8942831806975,
54.8923254618215,55.8903677429455,56.8884100240695,57.6714095710775),
 .UNSPECIFIED.);
#409=B_SPLINE_CURVE_WITH_KNOTS('',3,(#14954,#14955,#14956,#14957,#14958,
#14959,#14960,#14961,#14962,#14963,#14964,#14965,#14966,#14967,#14968,#14969,
#14970,#14971,#14972,#14973,#14974,#14975,#14976,#14977,#14978),
 .UNSPECIFIED.,.F.,.F.,(4,3,3,3,3,3,3,3,4),(-66.9238765922444,-66.8420716775802,
-65.8444288167208,-64.8467859558614,-63.849143095002,-62.8515002341426,
-61.8538573732832,-60.8562145124238,-60.6406912850648),.UNSPECIFIED.);
#410=B_SPLINE_CURVE_WITH_KNOTS('',3,(#14979,#14980,#14981,#14982,#14983,
#14984,#14985,#14986,#14987,#14988,#14989,#14990,#14991,#14992,#14993,#14994,
#14995,#14996,#14997,#14998,#14999,#15000,#15001,#15002,#15003),
 .UNSPECIFIED.,.F.,.F.,(4,3,3,3,3,3,3,3,4),(57.6714095710775,57.8864523051936,
58.8844945863176,59.8825368674416,60.8805791485657,61.8786214296897,62.8766637108137,
63.8747059919378,63.9545948782571),.UNSPECIFIED.);
#411=B_SPLINE_CURVE_WITH_KNOTS('',3,(#15008,#15009,#15010,#15011,#15012,
#15013,#15014,#15015,#15016,#15017,#15018,#15019,#15020,#15021,#15022,#15023,
#15024,#15025,#15026,#15027,#15028,#15029),.UNSPECIFIED.,.F.,.F.,(4,3,3,
3,3,3,3,4),(-73.207061899424,-72.8279288427366,-71.8302859818773,-70.8326431210178,
-69.8350002601584,-68.837357399299,-67.8397145384396,-66.9238765922444),
 .UNSPECIFIED.);
#412=B_SPLINE_CURVE_WITH_KNOTS('',3,(#15030,#15031,#15032,#15033,#15034,
#15035,#15036,#15037,#15038,#15039,#15040,#15041,#15042,#15043,#15044,#15045,
#15046,#15047,#15048,#15049,#15050,#15051),.UNSPECIFIED.,.F.,.F.,(4,3,3,
3,3,3,3,4),(63.9545948782571,64.8727482730618,65.8707905541858,66.8688328353098,
67.8668751164338,68.8649173975579,69.8629596786819,70.2377801854366),
 .UNSPECIFIED.);
#413=B_SPLINE_CURVE_WITH_KNOTS('',3,(#15056,#15057,#15058,#15059,#15060,
#15061,#15062,#15063,#15064,#15065,#15066,#15067,#15068,#15069,#15070,#15071,
#15072,#15073,#15074,#15075,#15076,#15077),.UNSPECIFIED.,.F.,.F.,(4,3,3,
3,3,3,3,4),(-79.4902472066036,-78.8137860078931,-77.8161431470337,-76.8185002861743,
-75.8208574253149,-74.8232145644555,-73.825571703596,-73.207061899424),
 .UNSPECIFIED.);
#414=B_SPLINE_CURVE_WITH_KNOTS('',3,(#15078,#15079,#15080,#15081,#15082,
#15083,#15084,#15085,#15086,#15087,#15088,#15089,#15090,#15091,#15092,#15093,
#15094,#15095,#15096,#15097,#15098,#15099),.UNSPECIFIED.,.F.,.F.,(4,3,3,
3,3,3,3,4),(70.2377801854366,70.8610019598059,71.85904424093,72.857086522054,
73.855128803178,74.853171084302,75.8512133654261,76.5209654926162),
 .UNSPECIFIED.);
#415=B_SPLINE_CURVE_WITH_KNOTS('',3,(#15104,#15105,#15106,#15107,#15108,
#15109,#15110,#15111,#15112,#15113,#15114,#15115,#15116,#15117,#15118,#15119,
#15120,#15121,#15122,#15123,#15124,#15125),.UNSPECIFIED.,.F.,.F.,(4,3,3,
3,3,3,3,4),(-85.7734325137832,-84.7996431730495,-83.8020003121901,-82.8043574513307,
-81.8067145904713,-80.8090717296119,-79.8114288687525,-79.4902472066036),
 .UNSPECIFIED.);
#416=B_SPLINE_CURVE_WITH_KNOTS('',3,(#15126,#15127,#15128,#15129,#15130,
#15131,#15132,#15133,#15134,#15135,#15136,#15137,#15138,#15139,#15140,#15141,
#15142,#15143,#15144,#15145,#15146,#15147),.UNSPECIFIED.,.F.,.F.,(4,3,3,
3,3,3,3,4),(76.5209654926162,76.8492556465501,77.8472979276741,78.8453402087982,
79.8433824899222,80.8414247710462,81.8394670521702,82.8041507997958),
 .UNSPECIFIED.);
#417=B_SPLINE_CURVE_WITH_KNOTS('',3,(#15152,#15153,#15154,#15155,#15156,
#15157,#15158,#15159,#15160,#15161,#15162,#15163,#15164,#15165,#15166,#15167,
#15168,#15169,#15170,#15171,#15172,#15173,#15174,#15175,#15176),
 .UNSPECIFIED.,.F.,.F.,(4,3,3,3,3,3,3,3,4),(-92.0566178209628,-91.7831431990654,
-90.7855003382059,-89.7878574773465,-88.7902146164871,-87.7925717556277,
-86.7949288947683,-85.7972860339089,-85.7734325137832),.UNSPECIFIED.);
#418=B_SPLINE_CURVE_WITH_KNOTS('',3,(#15177,#15178,#15179,#15180,#15181,
#15182,#15183,#15184,#15185,#15186,#15187,#15188,#15189,#15190,#15191,#15192,
#15193,#15194,#15195,#15196,#15197,#15198,#15199,#15200,#15201),
 .UNSPECIFIED.,.F.,.F.,(4,3,3,3,3,3,3,3,4),(82.8041507997958,82.8375093332942,
83.8355516144183,84.8335938955423,85.8316361766664,86.8296784577904,87.8277207389144,
88.8257630200384,89.0873361069754),.UNSPECIFIED.);
#419=B_SPLINE_CURVE_WITH_KNOTS('',3,(#15206,#15207,#15208,#15209,#15210,
#15211,#15212,#15213,#15214,#15215,#15216,#15217,#15218,#15219,#15220,#15221,
#15222,#15223,#15224,#15225,#15226,#15227),.UNSPECIFIED.,.F.,.F.,(4,3,3,
3,3,3,3,4),(-98.3398031281424,-97.7690003642218,-96.7713575033624,-95.773714642503,
-94.7760717816436,-93.7784289207842,-92.7807860599248,-92.0566178209628),
 .UNSPECIFIED.);
#420=B_SPLINE_CURVE_WITH_KNOTS('',3,(#15228,#15229,#15230,#15231,#15232,
#15233,#15234,#15235,#15236,#15237,#15238,#15239,#15240,#15241,#15242,#15243,
#15244,#15245,#15246,#15247,#15248,#15249),.UNSPECIFIED.,.F.,.F.,(4,3,3,
3,3,3,3,4),(89.0873361069754,89.8238053011624,90.8218475822865,91.8198898634105,
92.8179321445345,93.8159744256585,94.8140167067826,95.370521414155),
 .UNSPECIFIED.);
#421=B_SPLINE_CURVE_WITH_KNOTS('',3,(#15254,#15255,#15256,#15257,#15258,
#15259,#15260,#15261,#15262,#15263,#15264,#15265,#15266,#15267,#15268,#15269,
#15270,#15271,#15272,#15273,#15274,#15275),.UNSPECIFIED.,.F.,.F.,(4,3,3,
3,3,3,3,4),(-104.622988435322,-103.754857529378,-102.757214668519,-101.759571807659,
-100.7619289468,-99.7642860859406,-98.7666432250812,-98.3398031281424),
 .UNSPECIFIED.);
#422=B_SPLINE_CURVE_WITH_KNOTS('',3,(#15276,#15277,#15278,#15279,#15280,
#15281,#15282,#15283,#15284,#15285,#15286,#15287,#15288,#15289,#15290,#15291,
#15292,#15293,#15294,#15295,#15296,#15297),.UNSPECIFIED.,.F.,.F.,(4,3,3,
3,3,3,3,4),(95.370521414155,95.8120589879066,96.8101012690306,97.8081435501546,
98.8061858312787,99.8042281124027,100.802270393527,101.653706721335),
 .UNSPECIFIED.);
#423=B_SPLINE_CURVE_WITH_KNOTS('',3,(#15302,#15303,#15304,#15305,#15306,
#15307,#15308,#15309,#15310,#15311,#15312,#15313,#15314,#15315,#15316,#15317,
#15318,#15319,#15320,#15321,#15322,#15323,#15324,#15325,#15326),
 .UNSPECIFIED.,.F.,.F.,(4,3,3,3,3,3,3,3,4),(-110.906173742502,-110.738357555394,
-109.740714694535,-108.743071833675,-107.745428972816,-106.747786111956,
-105.750143251097,-104.752500390238,-104.622988435322),.UNSPECIFIED.);
#424=B_SPLINE_CURVE_WITH_KNOTS('',3,(#15327,#15328,#15329,#15330,#15331,
#15332,#15333,#15334,#15335,#15336,#15337,#15338,#15339,#15340,#15341,#15342,
#15343,#15344,#15345,#15346,#15347,#15348,#15349,#15350,#15351),
 .UNSPECIFIED.,.F.,.F.,(4,3,3,3,3,3,3,3,4),(101.653706721335,101.800312674651,
102.798354955775,103.796397236899,104.794439518023,105.792481799147,106.790524080271,
107.788566361395,107.936892028514),.UNSPECIFIED.);
#425=B_SPLINE_CURVE_WITH_KNOTS('',3,(#15356,#15357,#15358,#15359,#15360,
#15361,#15362,#15363,#15364,#15365,#15366,#15367,#15368,#15369,#15370,#15371,
#15372,#15373,#15374,#15375,#15376,#15377),.UNSPECIFIED.,.F.,.F.,(4,3,3,
3,3,3,3,4),(-117.189359049681,-116.724214720551,-115.726571859691,-114.728928998832,
-113.731286137972,-112.733643277113,-111.736000416253,-110.906173742502),
 .UNSPECIFIED.);
#426=B_SPLINE_CURVE_WITH_KNOTS('',3,(#15378,#15379,#15380,#15381,#15382,
#15383,#15384,#15385,#15386,#15387,#15388,#15389,#15390,#15391,#15392,#15393,
#15394,#15395,#15396,#15397,#15398,#15399),.UNSPECIFIED.,.F.,.F.,(4,3,3,
3,3,3,3,4),(107.936892028514,108.786608642519,109.784650923643,110.782693204767,
111.780735485891,112.778777767015,113.776820048139,114.220077335694),
 .UNSPECIFIED.);
#427=B_SPLINE_CURVE_WITH_KNOTS('',3,(#15404,#15405,#15406,#15407,#15408,
#15409,#15410,#15411,#15412,#15413,#15414,#15415,#15416,#15417,#15418,#15419,
#15420,#15421,#15422,#15423,#15424,#15425),.UNSPECIFIED.,.F.,.F.,(4,3,3,
3,3,3,3,4),(-123.472544356861,-122.710071885707,-121.712429024848,-120.714786163988,
-119.717143303129,-118.719500442269,-117.72185758141,-117.189359049681),
 .UNSPECIFIED.);
#428=B_SPLINE_CURVE_WITH_KNOTS('',3,(#15426,#15427,#15428,#15429,#15430,
#15431,#15432,#15433,#15434,#15435,#15436,#15437,#15438,#15439,#15440,#15441,
#15442,#15443,#15444,#15445,#15446,#15447),.UNSPECIFIED.,.F.,.F.,(4,3,3,
3,3,3,3,4),(114.220077335694,114.774862329263,115.772904610387,116.770946891511,
117.768989172635,118.767031453759,119.765073734883,120.503262642873),
 .UNSPECIFIED.);
#429=B_SPLINE_CURVE_WITH_KNOTS('',3,(#15452,#15453,#15454,#15455,#15456,
#15457,#15458,#15459,#15460,#15461,#15462,#15463,#15464,#15465,#15466,#15467,
#15468,#15469,#15470,#15471,#15472,#15473,#15474,#15475,#15476),
 .UNSPECIFIED.,.F.,.F.,(4,3,3,3,3,3,3,3,4),(-129.75572966404,-129.693571911723,
-128.695929050863,-127.698286190004,-126.700643329145,-125.703000468285,
-124.705357607426,-123.707714746566,-123.472544356861),.UNSPECIFIED.);
#430=B_SPLINE_CURVE_WITH_KNOTS('',3,(#15477,#15478,#15479,#15480,#15481,
#15482,#15483,#15484,#15485,#15486,#15487,#15488,#15489,#15490,#15491,#15492,
#15493,#15494,#15495,#15496,#15497,#15498,#15499,#15500,#15501),
 .UNSPECIFIED.,.F.,.F.,(4,3,3,3,3,3,3,3,4),(120.503262642873,120.763116016007,
121.761158297131,122.759200578255,123.757242859379,124.755285140503,125.753327421627,
126.751369702751,126.786447950053),.UNSPECIFIED.);
#431=B_SPLINE_CURVE_WITH_KNOTS('',3,(#15506,#15507,#15508,#15509,#15510,
#15511,#15512,#15513,#15514,#15515,#15516,#15517,#15518,#15519,#15520,#15521,
#15522,#15523,#15524,#15525,#15526,#15527),.UNSPECIFIED.,.F.,.F.,(4,3,3,
3,3,3,3,4),(-136.03891497122,-135.679429076879,-134.68178621602,-133.68414335516,
-132.686500494301,-131.688857633442,-130.691214772582,-129.75572966404),
 .UNSPECIFIED.);
#432=B_SPLINE_CURVE_WITH_KNOTS('',3,(#15528,#15529,#15530,#15531,#15532,
#15533,#15534,#15535,#15536,#15537,#15538,#15539,#15540,#15541,#15542,#15543,
#15544,#15545,#15546,#15547,#15548,#15549),.UNSPECIFIED.,.F.,.F.,(4,3,3,
3,3,3,3,4),(126.786447950053,127.749411983875,128.747454265,129.745496546124,
130.743538827248,131.741581108372,132.739623389496,133.069633257233),
 .UNSPECIFIED.);
#433=B_SPLINE_CURVE_WITH_KNOTS('',3,(#15554,#15555,#15556,#15557,#15558,
#15559,#15560,#15561,#15562,#15563,#15564,#15565,#15566,#15567,#15568,#15569,
#15570,#15571,#15572,#15573,#15574,#15575),.UNSPECIFIED.,.F.,.F.,(4,3,3,
3,3,3,3,4),(-142.322100278399,-141.665286242036,-140.667643381176,-139.670000520317,
-138.672357659457,-137.674714798598,-136.677071937739,-136.03891497122),
 .UNSPECIFIED.);
#434=B_SPLINE_CURVE_WITH_KNOTS('',3,(#15576,#15577,#15578,#15579,#15580,
#15581,#15582,#15583,#15584,#15585,#15586,#15587,#15588,#15589,#15590,#15591,
#15592,#15593,#15594,#15595,#15596,#15597),.UNSPECIFIED.,.F.,.F.,(4,3,3,
3,3,3,3,4),(133.069633257233,133.73766567062,134.735707951744,135.733750232868,
136.731792513992,137.729834795116,138.72787707624,139.352818564412),
 .UNSPECIFIED.);
#435=B_SPLINE_CURVE_WITH_KNOTS('',3,(#15602,#15603,#15604,#15605,#15606,
#15607,#15608,#15609,#15610,#15611,#15612,#15613,#15614,#15615,#15616,#15617,
#15618,#15619,#15620,#15621,#15622,#15623),.UNSPECIFIED.,.F.,.F.,(4,3,3,
3,3,3,3,4),(-148.605285585579,-147.651143407192,-146.653500546333,-145.655857685473,
-144.658214824614,-143.660571963754,-142.662929102895,-142.322100278399),
 .UNSPECIFIED.);
#436=B_SPLINE_CURVE_WITH_KNOTS('',3,(#15624,#15625,#15626,#15627,#15628,
#15629,#15630,#15631,#15632,#15633,#15634,#15635,#15636,#15637,#15638,#15639,
#15640,#15641,#15642,#15643,#15644,#15645),.UNSPECIFIED.,.F.,.F.,(4,3,3,
3,3,3,3,4),(139.352818564412,139.725919357364,140.723961638488,141.722003919612,
142.720046200736,143.71808848186,144.716130762984,145.636003871592),
 .UNSPECIFIED.);
#437=B_SPLINE_CURVE_WITH_KNOTS('',3,(#15650,#15651,#15652,#15653,#15654,
#15655,#15656,#15657,#15658,#15659,#15660,#15661,#15662,#15663,#15664,#15665,
#15666,#15667,#15668,#15669,#15670,#15671,#15672,#15673,#15674),
 .UNSPECIFIED.,.F.,.F.,(4,3,3,3,3,3,3,3,4),(-154.888470892759,-154.634643433208,
-153.637000572349,-152.639357711489,-151.64171485063,-150.64407198977,-149.646429128911,
-148.648786268052,-148.605285585579),.UNSPECIFIED.);
#438=B_SPLINE_CURVE_WITH_KNOTS('',3,(#15675,#15676,#15677,#15678,#15679,
#15680,#15681,#15682,#15683,#15684,#15685,#15686,#15687,#15688,#15689,#15690,
#15691,#15692,#15693,#15694,#15695,#15696,#15697,#15698,#15699),
 .UNSPECIFIED.,.F.,.F.,(4,3,3,3,3,3,3,3,4),(145.636003871592,145.714173044108,
146.712215325232,147.710257606356,148.70829988748,149.706342168604,150.704384449728,
151.702426730852,151.919189178771),.UNSPECIFIED.);
#439=B_SPLINE_CURVE_WITH_KNOTS('',3,(#15704,#15705,#15706,#15707,#15708,
#15709,#15710,#15711,#15712,#15713,#15714,#15715,#15716,#15717,#15718,#15719,
#15720,#15721,#15722,#15723,#15724,#15725),.UNSPECIFIED.,.F.,.F.,(4,3,3,
3,3,3,3,4),(-161.171656199938,-160.620500598364,-159.622857737505,-158.625214876646,
-157.627572015786,-156.629929154927,-155.632286294067,-154.888470892759),
 .UNSPECIFIED.);
#440=B_SPLINE_CURVE_WITH_KNOTS('',3,(#15726,#15727,#15728,#15729,#15730,
#15731,#15732,#15733,#15734,#15735,#15736,#15737,#15738,#15739,#15740,#15741,
#15742,#15743,#15744,#15745,#15746,#15747),.UNSPECIFIED.,.F.,.F.,(4,3,3,
3,3,3,3,4),(151.919189178771,152.700469011976,153.6985112931,154.696553574224,
155.694595855348,156.692638136472,157.690680417596,158.202374485951),
 .UNSPECIFIED.);
#441=B_SPLINE_CURVE_WITH_KNOTS('',3,(#15752,#15753,#15754,#15755,#15756,
#15757,#15758,#15759,#15760,#15761,#15762,#15763,#15764,#15765,#15766,#15767,
#15768,#15769,#15770,#15771,#15772,#15773),.UNSPECIFIED.,.F.,.F.,(4,3,3,
3,3,3,3,4),(-167.454841507118,-166.606357763521,-165.608714902661,-164.611072041802,
-163.613429180943,-162.615786320083,-161.618143459224,-161.171656199938),
 .UNSPECIFIED.);
#442=B_SPLINE_CURVE_WITH_KNOTS('',3,(#15774,#15775,#15776,#15777,#15778,
#15779,#15780,#15781,#15782,#15783,#15784,#15785,#15786,#15787,#15788,#15789,
#15790,#15791,#15792,#15793,#15794,#15795),.UNSPECIFIED.,.F.,.F.,(4,3,3,
3,3,3,3,4),(158.202374485951,158.68872269872,159.686764979844,160.684807260968,
161.682849542092,162.680891823216,163.67893410434,164.48555979313),
 .UNSPECIFIED.);
#443=B_SPLINE_CURVE_WITH_KNOTS('',3,(#15800,#15801,#15802,#15803,#15804,
#15805,#15806,#15807,#15808,#15809,#15810,#15811,#15812,#15813,#15814,#15815,
#15816,#15817,#15818,#15819,#15820,#15821,#15822,#15823,#15824),
 .UNSPECIFIED.,.F.,.F.,(4,3,3,3,3,3,3,3,4),(-173.738026814297,-173.589857789537,
-172.592214928677,-171.594572067818,-170.596929206958,-169.599286346099,
-168.60164348524,-167.60400062438,-167.454841507118),.UNSPECIFIED.);
#444=B_SPLINE_CURVE_WITH_KNOTS('',3,(#15825,#15826,#15827,#15828,#15829,
#15830,#15831,#15832,#15833,#15834,#15835,#15836,#15837,#15838,#15839,#15840,
#15841,#15842,#15843,#15844,#15845,#15846,#15847,#15848,#15849),
 .UNSPECIFIED.,.F.,.F.,(4,3,3,3,3,3,3,3,4),(164.48555979313,164.676976385465,
165.675018666588,166.673060947713,167.671103228837,168.669145509961,169.667187791085,
170.665230072209,170.76874510031),.UNSPECIFIED.);
#445=B_SPLINE_CURVE_WITH_KNOTS('',3,(#15854,#15855,#15856,#15857,#15858,
#15859,#15860,#15861,#15862,#15863,#15864,#15865,#15866,#15867,#15868,#15869,
#15870,#15871,#15872,#15873,#15874,#15875),.UNSPECIFIED.,.F.,.F.,(4,3,3,
3,3,3,3,4),(-180.021212121477,-179.575714954693,-178.578072093834,-177.580429232974,
-176.582786372115,-175.585143511255,-174.587500650396,-173.738026814297),
 .UNSPECIFIED.);
#446=B_SPLINE_CURVE_WITH_KNOTS('',3,(#15876,#15877,#15878,#15879,#15880,
#15881,#15882,#15883,#15884,#15885,#15886,#15887,#15888,#15889,#15890,#15891,
#15892,#15893,#15894,#15895,#15896,#15897),.UNSPECIFIED.,.F.,.F.,(4,3,3,
3,3,3,3,4),(170.76874510031,171.663272353333,172.661314634457,173.659356915581,
174.657399196705,175.655441477829,176.653483758953,177.051930407489),
 .UNSPECIFIED.);
#447=B_SPLINE_CURVE_WITH_KNOTS('',3,(#15902,#15903,#15904,#15905,#15906,
#15907,#15908,#15909,#15910,#15911,#15912,#15913,#15914,#15915,#15916,#15917,
#15918,#15919,#15920,#15921,#15922,#15923),.UNSPECIFIED.,.F.,.F.,(4,3,3,
3,3,3,3,4),(-186.304397428656,-185.56157211985,-184.56392925899,-183.566286398131,
-182.568643537271,-181.571000676412,-180.573357815553,-180.021212121477),
 .UNSPECIFIED.);
#448=B_SPLINE_CURVE_WITH_KNOTS('',3,(#15924,#15925,#15926,#15927,#15928,
#15929,#15930,#15931,#15932,#15933,#15934,#15935,#15936,#15937,#15938,#15939,
#15940,#15941,#15942,#15943,#15944,#15945),.UNSPECIFIED.,.F.,.F.,(4,3,3,
3,3,3,3,4),(177.051930407489,177.651526040077,178.649568321201,179.647610602325,
180.645652883449,181.643695164573,182.641737445697,183.335115714669),
 .UNSPECIFIED.);
#449=B_SPLINE_CURVE_WITH_KNOTS('',3,(#15951,#15952,#15953,#15954,#15955,
#15956,#15957,#15958,#15959,#15960),.UNSPECIFIED.,.F.,.F.,(4,1,1,1,1,1,
1,4),(197.920337176157,198.17515472821,199.172797589069,200.170440449928,
201.168083310788,202.165726171647,203.163369032507,204.161011893366),
 .UNSPECIFIED.);
#450=B_SPLINE_CURVE_WITH_KNOTS('',3,(#15963,#15964,#15965,#15966,#15967,
#15968,#15969,#15970,#15971),.UNSPECIFIED.,.F.,.F.,(4,1,1,1,1,1,4),(197.920337176157,
197.930069567874,198.928111848998,199.926154130122,200.924196411246,201.92223869237,
202.920280973494),.UNSPECIFIED.);
#451=B_SPLINE_CURVE_WITH_KNOTS('',3,(#15976,#15977,#15978,#15979,#15980,
#15981,#15982,#15983,#15984,#15985),.UNSPECIFIED.,.F.,.F.,(4,1,1,1,1,1,
1,4),(191.637151868977,192.189297563053,193.186940423913,194.184583284772,
195.182226145631,196.179869006491,197.17751186735,197.920337176157),
 .UNSPECIFIED.);
#452=B_SPLINE_CURVE_WITH_KNOTS('',3,(#15986,#15987,#15988,#15989,#15990,
#15991,#15992,#15993,#15994,#15995),.UNSPECIFIED.,.F.,.F.,(4,1,1,1,1,1,
1,4),(191.637151868977,191.94181588113,192.939858162254,193.937900443378,
194.935942724502,195.933985005626,196.93202728675,197.920337176157),
 .UNSPECIFIED.);
#453=B_SPLINE_CURVE_WITH_KNOTS('',3,(#16000,#16001,#16002,#16003,#16004,
#16005,#16006,#16007,#16008,#16009),.UNSPECIFIED.,.F.,.F.,(4,1,1,1,1,1,
1,4),(185.353966561798,186.203440397897,187.201083258756,188.198726119616,
189.196368980475,190.194011841334,191.191654702194,191.637151868977),
 .UNSPECIFIED.);
#454=B_SPLINE_CURVE_WITH_KNOTS('',3,(#16010,#16011,#16012,#16013,#16014,
#16015,#16016,#16017,#16018,#16019),.UNSPECIFIED.,.F.,.F.,(4,1,1,1,1,1,
1,4),(185.353966561798,185.953562194385,186.951604475509,187.949646756633,
188.947689037757,189.945731318881,190.943773600006,191.637151868977),
 .UNSPECIFIED.);
#455=B_SPLINE_CURVE_WITH_KNOTS('',3,(#16024,#16025,#16026,#16027,#16028,
#16029,#16030,#16031,#16032,#16033,#16034),.UNSPECIFIED.,.F.,.F.,(4,1,1,
1,1,1,1,1,4),(179.070781254618,179.219940371881,180.21758323274,181.2152260936,
182.212868954459,183.210511815318,184.208154676178,185.205797537037,185.353966561798),
 .UNSPECIFIED.);
#456=B_SPLINE_CURVE_WITH_KNOTS('',3,(#16035,#16036,#16037,#16038,#16039,
#16040,#16041,#16042,#16043,#16044),.UNSPECIFIED.,.F.,.F.,(4,1,1,1,1,1,
1,4),(179.070781254618,179.965308507641,180.963350788765,181.961393069889,
182.959435351013,183.957477632137,184.955519913261,185.353966561798),
 .UNSPECIFIED.);
#457=B_SPLINE_CURVE_WITH_KNOTS('',3,(#16049,#16050,#16051,#16052,#16053,
#16054,#16055,#16056,#16057,#16058),.UNSPECIFIED.,.F.,.F.,(4,1,1,1,1,1,
1,4),(172.787595947439,173.234083206724,174.231726067584,175.229368928443,
176.227011789303,177.224654650162,178.222297511021,179.070781254618),
 .UNSPECIFIED.);
#458=B_SPLINE_CURVE_WITH_KNOTS('',3,(#16059,#16060,#16061,#16062,#16063,
#16064,#16065,#16066,#16067,#16068,#16069),.UNSPECIFIED.,.F.,.F.,(4,1,1,
1,1,1,1,1,4),(172.787595947439,172.979012539773,173.977054820897,174.975097102021,
175.973139383145,176.971181664269,177.969223945393,178.967266226517,179.070781254618),
 .UNSPECIFIED.);
#459=B_SPLINE_CURVE_WITH_KNOTS('',3,(#16074,#16075,#16076,#16077,#16078,
#16079,#16080,#16081,#16082,#16083),.UNSPECIFIED.,.F.,.F.,(4,1,1,1,1,1,
1,4),(166.504410640259,167.248226041568,168.245868902427,169.243511763287,
170.241154624146,171.238797485006,172.236440345865,172.787595947439),
 .UNSPECIFIED.);
#460=B_SPLINE_CURVE_WITH_KNOTS('',3,(#16084,#16085,#16086,#16087,#16088,
#16089,#16090,#16091,#16092,#16093),.UNSPECIFIED.,.F.,.F.,(4,1,1,1,1,1,
1,4),(166.504410640259,166.990758853029,167.988801134153,168.986843415277,
169.984885696401,170.982927977525,171.980970258649,172.787595947439),
 .UNSPECIFIED.);
#461=B_SPLINE_CURVE_WITH_KNOTS('',3,(#16098,#16099,#16100,#16101,#16102,
#16103,#16104,#16105,#16106,#16107,#16108),.UNSPECIFIED.,.F.,.F.,(4,1,1,
1,1,1,1,1,4),(160.22122533308,160.264726015552,161.262368876412,162.260011737271,
163.25765459813,164.25529745899,165.252940319849,166.250583180709,166.504410640259),
 .UNSPECIFIED.);
#462=B_SPLINE_CURVE_WITH_KNOTS('',3,(#16109,#16110,#16111,#16112,#16113,
#16114,#16115,#16116,#16117,#16118),.UNSPECIFIED.,.F.,.F.,(4,1,1,1,1,1,
1,4),(160.22122533308,161.002505166285,162.000547447409,162.998589728533,
163.996632009657,164.994674290781,165.992716571905,166.504410640259),
 .UNSPECIFIED.);
#463=B_SPLINE_CURVE_WITH_KNOTS('',3,(#16123,#16124,#16125,#16126,#16127,
#16128,#16129,#16130,#16131,#16132),.UNSPECIFIED.,.F.,.F.,(4,1,1,1,1,1,
1,4),(153.9380400259,154.278868850396,155.276511711255,156.274154572115,
157.271797432974,158.269440293833,159.267083154693,160.22122533308),
 .UNSPECIFIED.);
#464=B_SPLINE_CURVE_WITH_KNOTS('',3,(#16133,#16134,#16135,#16136,#16137,
#16138,#16139,#16140,#16141,#16142,#16143),.UNSPECIFIED.,.F.,.F.,(4,1,1,
1,1,1,1,1,4),(153.9380400259,154.016209198417,155.014251479541,156.012293760665,
157.010336041789,158.008378322913,159.006420604037,160.004462885161,160.22122533308),
 .UNSPECIFIED.);
#465=B_SPLINE_CURVE_WITH_KNOTS('',3,(#16148,#16149,#16150,#16151,#16152,
#16153,#16154,#16155,#16156,#16157),.UNSPECIFIED.,.F.,.F.,(4,1,1,1,1,1,
1,4),(147.65485471872,148.293011685239,149.290654546099,150.288297406958,
151.285940267817,152.283583128677,153.281225989536,153.9380400259),
 .UNSPECIFIED.);
#466=B_SPLINE_CURVE_WITH_KNOTS('',3,(#16158,#16159,#16160,#16161,#16162,
#16163,#16164,#16165,#16166,#16167),.UNSPECIFIED.,.F.,.F.,(4,1,1,1,1,1,
1,4),(147.65485471872,148.027955511672,149.025997792796,150.02404007392,
151.022082355044,152.020124636168,153.018166917292,153.9380400259),
 .UNSPECIFIED.);
#467=B_SPLINE_CURVE_WITH_KNOTS('',3,(#16172,#16173,#16174,#16175,#16176,
#16177,#16178,#16179,#16180,#16181),.UNSPECIFIED.,.F.,.F.,(4,1,1,1,1,1,
1,4),(141.371669411541,142.307154520083,143.304797380942,144.302440241802,
145.300083102661,146.29772596352,147.29536882438,147.65485471872),
 .UNSPECIFIED.);
#468=B_SPLINE_CURVE_WITH_KNOTS('',3,(#16182,#16183,#16184,#16185,#16186,
#16187,#16188,#16189,#16190,#16191),.UNSPECIFIED.,.F.,.F.,(4,1,1,1,1,1,
1,4),(141.371669411541,142.039701824928,143.037744106052,144.035786387176,
145.0338286683,146.031870949424,147.029913230548,147.65485471872),
 .UNSPECIFIED.);
#469=B_SPLINE_CURVE_WITH_KNOTS('',3,(#16196,#16197,#16198,#16199,#16200,
#16201,#16202,#16203,#16204,#16205,#16206),.UNSPECIFIED.,.F.,.F.,(4,1,1,
1,1,1,1,1,4),(135.088484104361,135.323654494067,136.321297354926,137.318940215786,
138.316583076645,139.314225937505,140.311868798364,141.309511659223,141.371669411541),
 .UNSPECIFIED.);
#470=B_SPLINE_CURVE_WITH_KNOTS('',3,(#16207,#16208,#16209,#16210,#16211,
#16212,#16213,#16214,#16215,#16216),.UNSPECIFIED.,.F.,.F.,(4,1,1,1,1,1,
1,4),(135.088484104361,136.051448138184,137.049490419308,138.047532700432,
139.045574981556,140.04361726268,141.041659543804,141.371669411541),
 .UNSPECIFIED.);
#471=B_SPLINE_CURVE_WITH_KNOTS('',3,(#16221,#16222,#16223,#16224,#16225,
#16226,#16227,#16228,#16229,#16230),.UNSPECIFIED.,.F.,.F.,(4,1,1,1,1,1,
1,4),(128.805298797182,129.337797328911,130.33544018977,131.333083050629,
132.330725911489,133.328368772348,134.326011633208,135.088484104361),
 .UNSPECIFIED.);
#472=B_SPLINE_CURVE_WITH_KNOTS('',3,(#16231,#16232,#16233,#16234,#16235,
#16236,#16237,#16238,#16239,#16240,#16241),.UNSPECIFIED.,.F.,.F.,(4,1,1,
1,1,1,1,1,4),(128.805298797182,129.065152170316,130.06319445144,131.061236732564,
132.059279013688,133.057321294812,134.055363575936,135.05340585706,135.088484104361),
 .UNSPECIFIED.);
#473=B_SPLINE_CURVE_WITH_KNOTS('',3,(#16246,#16247,#16248,#16249,#16250,
#16251,#16252,#16253,#16254,#16255),.UNSPECIFIED.,.F.,.F.,(4,1,1,1,1,1,
1,4),(122.522113490002,123.351940163754,124.349583024614,125.347225885473,
126.344868746332,127.342511607192,128.340154468051,128.805298797182),
 .UNSPECIFIED.);
#474=B_SPLINE_CURVE_WITH_KNOTS('',3,(#16256,#16257,#16258,#16259,#16260,
#16261,#16262,#16263,#16264,#16265),.UNSPECIFIED.,.F.,.F.,(4,1,1,1,1,1,
1,4),(122.522113490002,123.076898483572,124.074940764696,125.07298304582,
126.071025326944,127.069067608068,128.067109889192,128.805298797182),
 .UNSPECIFIED.);
#475=B_SPLINE_CURVE_WITH_KNOTS('',3,(#16270,#16271,#16272,#16273,#16274,
#16275,#16276,#16277,#16278,#16279,#16280),.UNSPECIFIED.,.F.,.F.,(4,1,1,
1,1,1,1,1,4),(116.238928182823,116.368440137738,117.366082998598,118.363725859457,
119.361368720316,120.359011581176,121.356654442035,122.354297302895,122.522113490002),
 .UNSPECIFIED.);
#476=B_SPLINE_CURVE_WITH_KNOTS('',3,(#16281,#16282,#16283,#16284,#16285,
#16286,#16287,#16288,#16289,#16290),.UNSPECIFIED.,.F.,.F.,(4,1,1,1,1,1,
1,4),(116.238928182823,117.088644796828,118.086687077952,119.084729359076,
120.0827716402,121.080813921324,122.078856202448,122.522113490002),
 .UNSPECIFIED.);
#477=B_SPLINE_CURVE_WITH_KNOTS('',3,(#16295,#16296,#16297,#16298,#16299,
#16300,#16301,#16302,#16303,#16304),.UNSPECIFIED.,.F.,.F.,(4,1,1,1,1,1,
1,4),(109.955742875643,110.382582972582,111.380225833441,112.377868694301,
113.37551155516,114.373154416019,115.370797276879,116.238928182823),
 .UNSPECIFIED.);
#478=B_SPLINE_CURVE_WITH_KNOTS('',3,(#16305,#16306,#16307,#16308,#16309,
#16310,#16311,#16312,#16313,#16314,#16315),.UNSPECIFIED.,.F.,.F.,(4,1,1,
1,1,1,1,1,4),(109.955742875643,110.102348828959,111.100391110083,112.098433391207,
113.096475672331,114.094517953455,115.092560234579,116.090602515703,116.238928182823),
 .UNSPECIFIED.);
#479=B_SPLINE_CURVE_WITH_KNOTS('',3,(#16320,#16321,#16322,#16323,#16324,
#16325,#16326,#16327,#16328,#16329),.UNSPECIFIED.,.F.,.F.,(4,1,1,1,1,1,
1,4),(103.672557568463,104.396725807425,105.394368668285,106.392011529144,
107.389654390004,108.387297250863,109.384940111722,109.955742875643),
 .UNSPECIFIED.);
#480=B_SPLINE_CURVE_WITH_KNOTS('',3,(#16330,#16331,#16332,#16333,#16334,
#16335,#16336,#16337,#16338,#16339),.UNSPECIFIED.,.F.,.F.,(4,1,1,1,1,1,
1,4),(103.672557568463,104.114095142215,105.112137423339,106.110179704463,
107.108221985587,108.106264266711,109.104306547835,109.955742875643),
 .UNSPECIFIED.);
#481=B_SPLINE_CURVE_WITH_KNOTS('',3,(#16344,#16345,#16346,#16347,#16348,
#16349,#16350,#16351,#16352,#16353,#16354),.UNSPECIFIED.,.F.,.F.,(4,1,1,
1,1,1,1,1,4),(97.3893722612837,97.4132257814096,98.410868642269,99.4085115031284,
100.406154363988,101.403797224847,102.401440085707,103.399082946566,103.672557568463),
 .UNSPECIFIED.);
#482=B_SPLINE_CURVE_WITH_KNOTS('',3,(#16355,#16356,#16357,#16358,#16359,
#16360,#16361,#16362,#16363,#16364),.UNSPECIFIED.,.F.,.F.,(4,1,1,1,1,1,
1,4),(97.3893722612838,98.125841455471,99.123883736595,100.121926017719,
101.119968298843,102.118010579967,103.116052861091,103.672557568463),
 .UNSPECIFIED.);
#483=B_SPLINE_CURVE_WITH_KNOTS('',3,(#16369,#16370,#16371,#16372,#16373,
#16374,#16375,#16376,#16377,#16378),.UNSPECIFIED.,.F.,.F.,(4,1,1,1,1,1,
1,4),(91.1061869541041,91.4273686162531,92.4250114771125,93.4226543379719,
94.4202971988313,95.4179400596907,96.4155829205502,97.3893722612837),
 .UNSPECIFIED.);
#484=B_SPLINE_CURVE_WITH_KNOTS('',3,(#16379,#16380,#16381,#16382,#16383,
#16384,#16385,#16386,#16387,#16388,#16389),.UNSPECIFIED.,.F.,.F.,(4,1,1,
1,1,1,1,1,4),(91.1061869541042,91.1395454876028,92.1375877687268,93.1356300498508,
94.1336723309749,95.1317146120989,96.1297568932229,97.127799174347,97.3893722612838),
 .UNSPECIFIED.);
#485=B_SPLINE_CURVE_WITH_KNOTS('',3,(#16394,#16395,#16396,#16397,#16398,
#16399,#16400,#16401,#16402,#16403),.UNSPECIFIED.,.F.,.F.,(4,1,1,1,1,1,
1,4),(84.8230016469245,85.4415114510967,86.4391543119561,87.4367971728155,
88.4344400336749,89.4320828945343,90.4297257553937,91.1061869541041),
 .UNSPECIFIED.);
#486=B_SPLINE_CURVE_WITH_KNOTS('',3,(#16404,#16405,#16406,#16407,#16408,
#16409,#16410,#16411,#16412,#16413),.UNSPECIFIED.,.F.,.F.,(4,1,1,1,1,1,
1,4),(84.8230016469246,85.1512918008586,86.1493340819827,87.1473763631067,
88.1454186442307,89.1434609253548,90.1415032064788,91.1061869541042),
 .UNSPECIFIED.);
#487=B_SPLINE_CURVE_WITH_KNOTS('',3,(#16418,#16419,#16420,#16421,#16422,
#16423,#16424,#16425,#16426,#16427),.UNSPECIFIED.,.F.,.F.,(4,1,1,1,1,1,
1,4),(78.539816339745,79.4556542859402,80.4532971467996,81.4509400076591,
82.4485828685185,83.4462257293779,84.4438685902373,84.8230016469245),
 .UNSPECIFIED.);
#488=B_SPLINE_CURVE_WITH_KNOTS('',3,(#16428,#16429,#16430,#16431,#16432,
#16433,#16434,#16435,#16436,#16437),.UNSPECIFIED.,.F.,.F.,(4,1,1,1,1,1,
1,4),(78.539816339745,79.1630381141145,80.1610803952385,81.1591226763625,
82.1571649574865,83.1552072386106,84.1532495197346,84.8230016469246),
 .UNSPECIFIED.);
#489=B_SPLINE_CURVE_WITH_KNOTS('',3,(#16442,#16443,#16444,#16445,#16446,
#16447,#16448,#16449,#16450,#16451,#16452),.UNSPECIFIED.,.F.,.F.,(4,1,1,
1,1,1,1,1,4),(72.2566310325654,72.4721542599244,73.4697971207838,74.4674399816432,
75.4650828425026,76.462725703362,77.4603685642214,78.4580114250808,78.539816339745),
 .UNSPECIFIED.);
#490=B_SPLINE_CURVE_WITH_KNOTS('',3,(#16453,#16454,#16455,#16456,#16457,
#16458,#16459,#16460,#16461,#16462),.UNSPECIFIED.,.F.,.F.,(4,1,1,1,1,1,
1,4),(72.2566310325654,73.1747844273703,74.1728267084943,75.1708689896184,
76.1689112707424,77.1669535518664,78.1649958329905,78.539816339745),
 .UNSPECIFIED.);
#491=B_SPLINE_CURVE_WITH_KNOTS('',3,(#16467,#16468,#16469,#16470,#16471,
#16472,#16473,#16474,#16475,#16476),.UNSPECIFIED.,.F.,.F.,(4,1,1,1,1,1,
1,4),(65.9734457253858,66.486297094768,67.4839399556274,68.4815828164868,
69.4792256773462,70.4768685382056,71.474511399065,72.2566310325654),
 .UNSPECIFIED.);
#492=B_SPLINE_CURVE_WITH_KNOTS('',3,(#16477,#16478,#16479,#16480,#16481,
#16482,#16483,#16484,#16485,#16486,#16487),.UNSPECIFIED.,.F.,.F.,(4,1,1,
1,1,1,1,1,4),(65.9734457253858,66.1884884595021,67.1865307406262,68.1845730217502,
69.1826153028742,70.1806575839982,71.1786998651223,72.1767421462463,72.2566310325654),
 .UNSPECIFIED.);
#493=B_SPLINE_CURVE_WITH_KNOTS('',3,(#16492,#16493,#16494,#16495,#16496,
#16497,#16498,#16499,#16500,#16501),.UNSPECIFIED.,.F.,.F.,(4,1,1,1,1,1,
1,4),(59.6902604182062,60.5004399296115,61.4980827904709,62.4957256513303,
63.4933685121897,64.4910113730492,65.4886542339086,65.9734457253858),
 .UNSPECIFIED.);
#494=B_SPLINE_CURVE_WITH_KNOTS('',3,(#16502,#16503,#16504,#16505,#16506,
#16507,#16508,#16509,#16510,#16511),.UNSPECIFIED.,.F.,.F.,(4,1,1,1,1,1,
1,4),(59.6902604182062,60.200234772758,61.198277053882,62.196319335006,
63.19436161613,64.1924038972541,65.1904461783781,65.9734457253858),
 .UNSPECIFIED.);
#495=B_SPLINE_CURVE_WITH_KNOTS('',3,(#16516,#16517,#16518,#16519,#16520,
#16521,#16522,#16523,#16524,#16525,#16526),.UNSPECIFIED.,.F.,.F.,(4,1,1,
1,1,1,1,1,4),(53.4070751110266,53.5169399035957,54.5145827644551,55.5122256253145,
56.5098684861739,57.5075113470333,58.5051542078927,59.5027970687521,59.6902604182062),
 .UNSPECIFIED.);
#496=B_SPLINE_CURVE_WITH_KNOTS('',3,(#16527,#16528,#16529,#16530,#16531,
#16532,#16533,#16534,#16535,#16536),.UNSPECIFIED.,.F.,.F.,(4,1,1,1,1,1,
1,4),(53.4070751110266,54.2119810860138,55.2100233671378,56.2080656482619,
57.2061079293859,58.2041502105099,59.2021924916339,59.6902604182062),
 .UNSPECIFIED.);
#497=B_SPLINE_CURVE_WITH_KNOTS('',3,(#16541,#16542,#16543,#16544,#16545,
#16546,#16547,#16548,#16549,#16550),.UNSPECIFIED.,.F.,.F.,(4,1,1,1,1,1,
1,4),(47.123889803847,47.5310827384393,48.5287255992987,49.5263684601581,
50.5240113210175,51.5216541818769,52.5192970427363,53.4070751110266),
 .UNSPECIFIED.);
#498=B_SPLINE_CURVE_WITH_KNOTS('',3,(#16551,#16552,#16553,#16554,#16555,
#16556,#16557,#16558,#16559,#16560,#16561),.UNSPECIFIED.,.F.,.F.,(4,1,1,
1,1,1,1,1,4),(47.123889803847,47.2256851181456,48.2237273992696,49.2217696803937,
50.2198119615177,51.2178542426417,52.2158965237657,53.2139388048898,53.4070751110266),
 .UNSPECIFIED.);
#499=B_SPLINE_CURVE_WITH_KNOTS('',3,(#16566,#16567,#16568,#16569,#16570,
#16571,#16572,#16573,#16574,#16575),.UNSPECIFIED.,.F.,.F.,(4,1,1,1,1,1,
1,4),(40.8407044966674,41.5452255732828,42.5428684341422,43.5405112950016,
44.538154155861,45.5357970167204,46.5334398775799,47.123889803847),
 .UNSPECIFIED.);
#500=B_SPLINE_CURVE_WITH_KNOTS('',3,(#16576,#16577,#16578,#16579,#16580,
#16581,#16582,#16583,#16584,#16585),.UNSPECIFIED.,.F.,.F.,(4,1,1,1,1,1,
1,4),(40.8407044966675,41.2374314314014,42.2354737125255,43.2335159936495,
44.2315582747735,45.2296005558975,46.2276428370216,47.123889803847),
 .UNSPECIFIED.);
#501=B_SPLINE_CURVE_WITH_KNOTS('',3,(#16590,#16591,#16592,#16593,#16594,
#16595,#16596,#16597,#16598,#16599,#16600),.UNSPECIFIED.,.F.,.F.,(4,1,1,
1,1,1,1,1,4),(34.5575191894878,34.561725547267,35.5593684081264,36.5570112689858,
37.5546541298452,38.5522969907046,39.549939851564,40.5475827124234,40.8407044966674),
 .UNSPECIFIED.);
#502=B_SPLINE_CURVE_WITH_KNOTS('',3,(#16601,#16602,#16603,#16604,#16605,
#16606,#16607,#16608,#16609,#16610),.UNSPECIFIED.,.F.,.F.,(4,1,1,1,1,1,
1,4),(34.5575191894879,35.2491777446573,36.2472200257813,37.2452623069053,
38.2433045880294,39.2413468691534,40.2393891502774,40.8407044966675),
 .UNSPECIFIED.);
#503=B_SPLINE_CURVE_WITH_KNOTS('',3,(#16615,#16616,#16617,#16618,#16619,
#16620,#16621,#16622,#16623,#16624),.UNSPECIFIED.,.F.,.F.,(4,1,1,1,1,1,
1,4),(28.2743338823082,28.5758683821105,29.5735112429699,30.5711541038294,
31.5687969646888,32.5664398255482,33.5640826864076,34.5575191894878),
 .UNSPECIFIED.);
#504=B_SPLINE_CURVE_WITH_KNOTS('',3,(#16625,#16626,#16627,#16628,#16629,
#16630,#16631,#16632,#16633,#16634),.UNSPECIFIED.,.F.,.F.,(4,1,1,1,1,1,
1,4),(28.2743338823083,29.2609240579131,30.2589663390371,31.2570086201612,
32.2550509012852,33.2530931824092,34.2511354635333,34.5575191894879),
 .UNSPECIFIED.);
#505=B_SPLINE_CURVE_WITH_KNOTS('',3,(#16639,#16640,#16641,#16642,#16643,
#16644,#16645,#16646,#16647,#16648),.UNSPECIFIED.,.F.,.F.,(4,1,1,1,1,1,
1,4),(21.9911485751286,22.5900112169541,23.5876540778135,24.5852969386729,
25.5829397995323,26.5805826603917,27.5782255212511,28.2743338823082),
 .UNSPECIFIED.);
#506=B_SPLINE_CURVE_WITH_KNOTS('',3,(#16649,#16650,#16651,#16652,#16653,
#16654,#16655,#16656,#16657,#16658,#16659),.UNSPECIFIED.,.F.,.F.,(4,1,1,
1,1,1,1,1,4),(21.9911485751287,22.2746280900449,23.272670371169,24.270712652293,
25.268754933417,26.266797214541,27.2648394956651,28.2628817767891,28.2743338823083),
 .UNSPECIFIED.);
#507=B_SPLINE_CURVE_WITH_KNOTS('',3,(#16664,#16665,#16666,#16667,#16668,
#16669,#16670,#16671,#16672,#16673),.UNSPECIFIED.,.F.,.F.,(4,1,1,1,1,1,
1,4),(15.707963267949,16.6041540517977,17.6017969126571,18.5994397735165,
19.5970826343759,20.5947254952353,21.5923683560947,21.9911485751286),
 .UNSPECIFIED.);
#508=B_SPLINE_CURVE_WITH_KNOTS('',3,(#16674,#16675,#16676,#16677,#16678,
#16679,#16680,#16681,#16682,#16683),.UNSPECIFIED.,.F.,.F.,(4,1,1,1,1,1,
1,4),(15.7079632679491,16.2863744033008,17.2844166844248,18.2824589655488,
19.2805012466728,20.2785435277969,21.2765858089209,21.9911485751287),
 .UNSPECIFIED.);
#509=B_SPLINE_CURVE_WITH_KNOTS('',3,(#16686,#16687,#16688,#16689,#16690,
#16691,#16692,#16693,#16694,#16695,#16696,#16697,#16698,#16699,#16700,#16701,
#16702,#16703,#16704,#16705,#16706,#16707,#16708,#16709,#16710,#16711,#16712,
#16713,#16714,#16715,#16716,#16717,#16718,#16719,#16720,#16721,#16722,#16723,
#16724,#16725,#16726,#16727,#16728,#16729,#16730,#16731,#16732,#16733,#16734,
#16735,#16736,#16737,#16738,#16739,#16740,#16741,#16742,#16743,#16744,#16745,
#16746,#16747,#16748,#16749,#16750,#16751,#16752,#16753,#16754,#16755,#16756,
#16757,#16758,#16759,#16760,#16761,#16762,#16763,#16764,#16765,#16766,#16767,
#16768,#16769,#16770,#16771,#16772,#16773,#16774,#16775,#16776,#16777,#16778,
#16779,#16780,#16781,#16782,#16783,#16784,#16785,#16786,#16787,#16788,#16789,
#16790,#16791,#16792,#16793,#16794,#16795,#16796,#16797,#16798,#16799,#16800,
#16801,#16802,#16803,#16804,#16805,#16806),.UNSPECIFIED.,.F.,.F.,(4,3,3,
3,3,3,3,3,3,3,3,3,3,3,3,3,3,3,3,3,3,3,3,3,3,3,3,3,3,3,3,3,3,3,3,3,3,3,3,
3,4),(-0.753008129282056,-0.726412283548368,-0.715911613874471,-0.694893371653716,
-0.683361029549332,-0.673826434412814,-0.652889016486892,-0.639679181765185,
-0.63195159856097,-0.60480408471638,-0.59150990338668,-0.582561183693184,
-0.554067746128576,-0.540494882749548,-0.528208608719221,-0.505843484121927,
-0.4921308028701,-0.483102814228457,-0.456032674248847,-0.436199115577779,
-0.427073928162626,-0.400948091236321,-0.382860905241332,-0.374822254310016,
-0.34584221065474,-0.333939649620793,-0.324058619604945,-0.29393738163796,
-0.278576588250954,-0.269234263278142,-0.238815915606663,-0.225742435796944,
-0.216239773488962,-0.18666367230127,-0.170750005528772,-0.161294486761502,
-0.129614927749849,-0.114924930935507,-0.106250072717365,-0.0979353687381955,
-0.0965360155478562),.UNSPECIFIED.);
#510=B_SPLINE_CURVE_WITH_KNOTS('',3,(#16808,#16809,#16810,#16811,#16812,
#16813,#16814,#16815,#16816,#16817,#16818,#16819,#16820,#16821,#16822,#16823,
#16824,#16825,#16826,#16827,#16828,#16829,#16830,#16831,#16832,#16833,#16834,
#16835,#16836,#16837,#16838,#16839,#16840,#16841,#16842,#16843,#16844),
 .UNSPECIFIED.,.F.,.F.,(4,3,3,3,3,3,3,3,3,3,3,3,4),(-0.204609524178132,
-0.173922074105667,-0.152149392827302,-0.142793959810126,-0.12983323009626,
-0.11308637627832,-0.0998536142809363,-0.090547498816978,-0.0679106241127335,
-0.0514558350659385,-0.042025593252969,-0.0155529233063705,0.),
 .UNSPECIFIED.);
#511=B_SPLINE_CURVE_WITH_KNOTS('',3,(#16847,#16848,#16849,#16850,#16851,
#16852,#16853,#16854,#16855,#16856,#16857,#16858,#16859,#16860,#16861,#16862),
 .UNSPECIFIED.,.F.,.F.,(4,3,3,3,3,4),(-0.0965360155478562,-0.0724020116608921,
-0.0590232605257019,-0.050388474335024,-0.0186937936910934,0.),
 .UNSPECIFIED.);
#512=B_SPLINE_CURVE_WITH_KNOTS('',3,(#17651,#17652,#17653,#17654,#17655,
#17656,#17657,#17658),.UNSPECIFIED.,.F.,.F.,(4,1,1,1,1,4),(11.6159397475006,
12.61358260836,13.6112254692194,14.6088683300789,15.6065111909383,15.707963267949),
 .UNSPECIFIED.);
#513=B_SPLINE_CURVE_WITH_KNOTS('',3,(#17659,#17660,#17661,#17662,#17663,
#17664,#17665,#17666,#17667,#17668,#17669,#17670,#17671,#17672,#17673,#17674,
#17675,#17676,#17677,#17678,#17679,#17680,#17681,#17682,#17683,#17684,#17685,
#17686,#17687,#17688,#17689,#17690,#17691,#17692,#17693,#17694,#17695,#17696,
#17697,#17698,#17699,#17700,#17701,#17702,#17703,#17704,#17705,#17706,#17707),
 .UNSPECIFIED.,.F.,.F.,(4,3,3,3,3,3,3,3,3,3,3,3,3,3,3,3,4),(-0.275362278356892,
-0.263988733943187,-0.242277787653762,-0.228409792083558,-0.208856161945484,
-0.197709057767663,-0.168075464588018,-0.150222803571495,-0.140083955862437,
-0.125365894046572,-0.0997819296507484,-0.0889593225835958,-0.0667194919376969,
-0.0511923416312717,-0.0404361839568205,-0.0141940669149386,0.),
 .UNSPECIFIED.);
#514=B_SPLINE_CURVE_WITH_KNOTS('',3,(#17708,#17709,#17710,#17711,#17712,
#17713,#17714,#17715,#17716,#17717,#17718,#17719,#17720,#17721,#17722,#17723,
#17724,#17725,#17726),.UNSPECIFIED.,.F.,.F.,(4,3,3,3,3,3,4),(-191.027404416132,
-190.549786424147,-189.552143563287,-188.554500702428,-187.556857841568,
-186.559214980709,-186.304397428656),.UNSPECIFIED.);
#515=B_SPLINE_CURVE_WITH_KNOTS('',3,(#17729,#17730,#17731,#17732,#17733,
#17734,#17735,#17736,#17737),.UNSPECIFIED.,.F.,.F.,(4,1,1,1,1,1,4),(10.3752088276283,
11.2961629976806,12.2942052788047,13.2922475599287,14.2902898410527,15.2883321221767,
15.7079632679491),.UNSPECIFIED.);
#516=B_SPLINE_CURVE_WITH_KNOTS('',3,(#18531,#18532,#18533,#18534,#18535,
#18536,#18537,#18538,#18539,#18540,#18541,#18542,#18543,#18544,#18545,#18546,
#18547,#18548,#18549,#18550,#18551,#18552),.UNSPECIFIED.,.F.,.F.,(4,3,3,
3,3,3,3,4),(183.335115714669,183.639779726821,184.637822007945,185.635864289069,
186.633906570193,187.631948851317,188.629991132441,188.954231742812),
 .UNSPECIFIED.);
#517=B_SPLINE_CURVE_WITH_KNOTS('',3,(#18553,#18554,#18555,#18556,#18557,
#18558,#18559,#18560,#18561,#18562,#18563,#18564,#18565,#18566,#18567,#18568,
#18569,#18570,#18571,#18572,#18573,#18574,#18575,#18576,#18577,#18578,#18579,
#18580,#18581,#18582,#18583,#18584,#18585,#18586,#18587,#18588,#18589,#18590,
#18591,#18592,#18593,#18594,#18595,#18596,#18597,#18598,#18599,#18600,#18601,
#18602,#18603,#18604),.UNSPECIFIED.,.F.,.F.,(4,3,3,3,3,3,3,3,3,3,3,3,3,
3,3,3,3,4),(-0.276631791712714,-0.267404104599176,-0.245529112929484,-0.233826742508505,
-0.212230201958684,-0.201819484750363,-0.173281546649687,-0.162756755581661,
-0.152537502224722,-0.140478169692516,-0.120739781640826,-0.110641775261762,
-0.100726383882944,-0.0755447879122082,-0.0587891884452614,-0.0493012364577666,
-0.0182848522583483,0.),.UNSPECIFIED.);
#552=SHAPE_REPRESENTATION_RELATIONSHIP('SRR','None',#19672,#562);
#562=ADVANCED_BREP_SHAPE_REPRESENTATION('',(#582),#19615);
#572=STYLED_ITEM('',(#19730),#582);
#582=MANIFOLD_SOLID_BREP('Body1',#7110);
#654=FACE_BOUND('',#1663,.T.);
#655=FACE_BOUND('',#1666,.T.);
#661=CONICAL_SURFACE('',#7699,0.1,0.785398163397448);
#801=PLANE('',#7705);
#802=PLANE('',#7706);
#803=PLANE('',#7707);
#804=PLANE('',#7708);
#805=PLANE('',#7709);
#806=PLANE('',#7710);
#807=PLANE('',#7711);
#808=PLANE('',#7712);
#809=PLANE('',#7716);
#810=PLANE('',#7717);
#1122=FACE_OUTER_BOUND('',#1590,.T.);
#1123=FACE_OUTER_BOUND('',#1591,.T.);
#1124=FACE_OUTER_BOUND('',#1592,.T.);
#1125=FACE_OUTER_BOUND('',#1593,.T.);
#1126=FACE_OUTER_BOUND('',#1594,.T.);
#1127=FACE_OUTER_BOUND('',#1595,.T.);
#1128=FACE_OUTER_BOUND('',#1596,.T.);
#1129=FACE_OUTER_BOUND('',#1597,.T.);
#1130=FACE_OUTER_BOUND('',#1598,.T.);
#1131=FACE_OUTER_BOUND('',#1599,.T.);
#1132=FACE_OUTER_BOUND('',#1600,.T.);
#1133=FACE_OUTER_BOUND('',#1601,.T.);
#1134=FACE_OUTER_BOUND('',#1602,.T.);
#1135=FACE_OUTER_BOUND('',#1603,.T.);
#1136=FACE_OUTER_BOUND('',#1604,.T.);
#1137=FACE_OUTER_BOUND('',#1605,.T.);
#1138=FACE_OUTER_BOUND('',#1606,.T.);
#1139=FACE_OUTER_BOUND('',#1607,.T.);
#1140=FACE_OUTER_BOUND('',#1608,.T.);
#1141=FACE_OUTER_BOUND('',#1609,.T.);
#1142=FACE_OUTER_BOUND('',#1610,.T.);
#1143=FACE_OUTER_BOUND('',#1611,.T.);
#1144=FACE_OUTER_BOUND('',#1612,.T.);
#1145=FACE_OUTER_BOUND('',#1613,.T.);
#1146=FACE_OUTER_BOUND('',#1614,.T.);
#1147=FACE_OUTER_BOUND('',#1615,.T.);
#1148=FACE_OUTER_BOUND('',#1616,.T.);
#1149=FACE_OUTER_BOUND('',#1617,.T.);
#1150=FACE_OUTER_BOUND('',#1618,.T.);
#1151=FACE_OUTER_BOUND('',#1619,.T.);
#1152=FACE_OUTER_BOUND('',#1620,.T.);
#1153=FACE_OUTER_BOUND('',#1621,.T.);
#1154=FACE_OUTER_BOUND('',#1622,.T.);
#1155=FACE_OUTER_BOUND('',#1623,.T.);
#1156=FACE_OUTER_BOUND('',#1624,.T.);
#1157=FACE_OUTER_BOUND('',#1625,.T.);
#1158=FACE_OUTER_BOUND('',#1626,.T.);
#1159=FACE_OUTER_BOUND('',#1627,.T.);
#1160=FACE_OUTER_BOUND('',#1628,.T.);
#1161=FACE_OUTER_BOUND('',#1629,.T.);
#1162=FACE_OUTER_BOUND('',#1630,.T.);
#1163=FACE_OUTER_BOUND('',#1631,.T.);
#1164=FACE_OUTER_BOUND('',#1632,.T.);
#1165=FACE_OUTER_BOUND('',#1633,.T.);
#1166=FACE_OUTER_BOUND('',#1634,.T.);
#1167=FACE_OUTER_BOUND('',#1635,.T.);
#1168=FACE_OUTER_BOUND('',#1636,.T.);
#1169=FACE_OUTER_BOUND('',#1637,.T.);
#1170=FACE_OUTER_BOUND('',#1638,.T.);
#1171=FACE_OUTER_BOUND('',#1639,.T.);
#1172=FACE_OUTER_BOUND('',#1640,.T.);
#1173=FACE_OUTER_BOUND('',#1641,.T.);
#1174=FACE_OUTER_BOUND('',#1642,.T.);
#1175=FACE_OUTER_BOUND('',#1643,.T.);
#1176=FACE_OUTER_BOUND('',#1644,.T.);
#1177=FACE_OUTER_BOUND('',#1645,.T.);
#1178=FACE_OUTER_BOUND('',#1646,.T.);
#1179=FACE_OUTER_BOUND('',#1647,.T.);
#1180=FACE_OUTER_BOUND('',#1648,.T.);
#1181=FACE_OUTER_BOUND('',#1649,.T.);
#1182=FACE_OUTER_BOUND('',#1650,.T.);
#1183=FACE_OUTER_BOUND('',#1651,.T.);
#1184=FACE_OUTER_BOUND('',#1652,.T.);
#1185=FACE_OUTER_BOUND('',#1653,.T.);
#1186=FACE_OUTER_BOUND('',#1654,.T.);
#1187=FACE_OUTER_BOUND('',#1655,.T.);
#1188=FACE_OUTER_BOUND('',#1656,.T.);
#1189=FACE_OUTER_BOUND('',#1657,.T.);
#1190=FACE_OUTER_BOUND('',#1658,.T.);
#1191=FACE_OUTER_BOUND('',#1659,.T.);
#1192=FACE_OUTER_BOUND('',#1660,.T.);
#1193=FACE_OUTER_BOUND('',#1661,.T.);
#1194=FACE_OUTER_BOUND('',#1662,.T.);
#1195=FACE_OUTER_BOUND('',#1664,.T.);
#1196=FACE_OUTER_BOUND('',#1665,.T.);
#1197=FACE_OUTER_BOUND('',#1667,.T.);
#1590=EDGE_LOOP('',(#5994,#5995,#5996,#5997));
#1591=EDGE_LOOP('',(#5998,#5999,#6000,#6001));
#1592=EDGE_LOOP('',(#6002,#6003,#6004,#6005));
#1593=EDGE_LOOP('',(#6006,#6007,#6008,#6009));
#1594=EDGE_LOOP('',(#6010,#6011,#6012,#6013));
#1595=EDGE_LOOP('',(#6014,#6015,#6016,#6017));
#1596=EDGE_LOOP('',(#6018,#6019,#6020,#6021));
#1597=EDGE_LOOP('',(#6022,#6023,#6024,#6025));
#1598=EDGE_LOOP('',(#6026,#6027,#6028,#6029));
#1599=EDGE_LOOP('',(#6030,#6031,#6032,#6033));
#1600=EDGE_LOOP('',(#6034,#6035,#6036,#6037));
#1601=EDGE_LOOP('',(#6038,#6039,#6040,#6041));
#1602=EDGE_LOOP('',(#6042,#6043,#6044,#6045));
#1603=EDGE_LOOP('',(#6046,#6047,#6048,#6049));
#1604=EDGE_LOOP('',(#6050,#6051,#6052,#6053));
#1605=EDGE_LOOP('',(#6054,#6055,#6056,#6057));
#1606=EDGE_LOOP('',(#6058,#6059,#6060,#6061));
#1607=EDGE_LOOP('',(#6062,#6063,#6064,#6065));
#1608=EDGE_LOOP('',(#6066,#6067,#6068,#6069));
#1609=EDGE_LOOP('',(#6070,#6071,#6072,#6073));
#1610=EDGE_LOOP('',(#6074,#6075,#6076,#6077));
#1611=EDGE_LOOP('',(#6078,#6079,#6080,#6081));
#1612=EDGE_LOOP('',(#6082,#6083,#6084,#6085));
#1613=EDGE_LOOP('',(#6086,#6087,#6088,#6089));
#1614=EDGE_LOOP('',(#6090,#6091,#6092,#6093));
#1615=EDGE_LOOP('',(#6094,#6095,#6096,#6097));
#1616=EDGE_LOOP('',(#6098,#6099,#6100,#6101));
#1617=EDGE_LOOP('',(#6102,#6103,#6104,#6105));
#1618=EDGE_LOOP('',(#6106,#6107,#6108,#6109));
#1619=EDGE_LOOP('',(#6110,#6111,#6112,#6113));
#1620=EDGE_LOOP('',(#6114,#6115,#6116,#6117));
#1621=EDGE_LOOP('',(#6118,#6119,#6120,#6121));
#1622=EDGE_LOOP('',(#6122,#6123,#6124,#6125));
#1623=EDGE_LOOP('',(#6126,#6127,#6128,#6129));
#1624=EDGE_LOOP('',(#6130,#6131,#6132,#6133));
#1625=EDGE_LOOP('',(#6134,#6135,#6136,#6137));
#1626=EDGE_LOOP('',(#6138,#6139,#6140,#6141));
#1627=EDGE_LOOP('',(#6142,#6143,#6144,#6145));
#1628=EDGE_LOOP('',(#6146,#6147,#6148,#6149));
#1629=EDGE_LOOP('',(#6150,#6151,#6152,#6153));
#1630=EDGE_LOOP('',(#6154,#6155,#6156,#6157));
#1631=EDGE_LOOP('',(#6158,#6159,#6160,#6161));
#1632=EDGE_LOOP('',(#6162,#6163,#6164,#6165));
#1633=EDGE_LOOP('',(#6166,#6167,#6168,#6169));
#1634=EDGE_LOOP('',(#6170,#6171,#6172,#6173));
#1635=EDGE_LOOP('',(#6174,#6175,#6176,#6177));
#1636=EDGE_LOOP('',(#6178,#6179,#6180,#6181));
#1637=EDGE_LOOP('',(#6182,#6183,#6184,#6185));
#1638=EDGE_LOOP('',(#6186,#6187,#6188,#6189));
#1639=EDGE_LOOP('',(#6190,#6191,#6192,#6193));
#1640=EDGE_LOOP('',(#6194,#6195,#6196,#6197));
#1641=EDGE_LOOP('',(#6198,#6199,#6200,#6201));
#1642=EDGE_LOOP('',(#6202,#6203,#6204,#6205));
#1643=EDGE_LOOP('',(#6206,#6207,#6208,#6209));
#1644=EDGE_LOOP('',(#6210,#6211,#6212,#6213));
#1645=EDGE_LOOP('',(#6214,#6215,#6216,#6217));
#1646=EDGE_LOOP('',(#6218,#6219,#6220,#6221));
#1647=EDGE_LOOP('',(#6222,#6223,#6224,#6225));
#1648=EDGE_LOOP('',(#6226,#6227,#6228,#6229));
#1649=EDGE_LOOP('',(#6230,#6231,#6232,#6233));
#1650=EDGE_LOOP('',(#6234,#6235,#6236,#6237,#6238,#6239,#6240,#6241));
#1651=EDGE_LOOP('',(#6242,#6243,#6244,#6245,#6246,#6247,#6248,#6249,#6250,
#6251,#6252,#6253,#6254,#6255,#6256,#6257,#6258,#6259,#6260,#6261,#6262,
#6263,#6264,#6265,#6266,#6267,#6268,#6269,#6270,#6271,#6272,#6273,#6274,
#6275,#6276,#6277,#6278,#6279,#6280,#6281,#6282,#6283,#6284,#6285,#6286,
#6287,#6288,#6289,#6290,#6291,#6292,#6293,#6294,#6295,#6296,#6297,#6298,
#6299,#6300,#6301,#6302,#6303,#6304,#6305));
#1652=EDGE_LOOP('',(#6306,#6307,#6308,#6309));
#1653=EDGE_LOOP('',(#6310,#6311,#6312,#6313,#6314,#6315,#6316,#6317,#6318,
#6319,#6320,#6321,#6322,#6323,#6324,#6325,#6326,#6327,#6328,#6329,#6330,
#6331,#6332,#6333,#6334,#6335,#6336,#6337,#6338,#6339,#6340,#6341,#6342,
#6343,#6344,#6345,#6346,#6347,#6348,#6349,#6350,#6351,#6352,#6353,#6354,
#6355,#6356,#6357,#6358,#6359,#6360,#6361,#6362,#6363,#6364,#6365,#6366,
#6367,#6368,#6369,#6370,#6371,#6372,#6373,#6374));
#1654=EDGE_LOOP('',(#6375,#6376,#6377,#6378));
#1655=EDGE_LOOP('',(#6379,#6380,#6381,#6382));
#1656=EDGE_LOOP('',(#6383,#6384,#6385,#6386));
#1657=EDGE_LOOP('',(#6387,#6388,#6389,#6390));
#1658=EDGE_LOOP('',(#6391,#6392,#6393,#6394));
#1659=EDGE_LOOP('',(#6395,#6396,#6397,#6398));
#1660=EDGE_LOOP('',(#6399,#6400,#6401,#6402));
#1661=EDGE_LOOP('',(#6403,#6404,#6405,#6406,#6407,#6408));
#1662=EDGE_LOOP('',(#6409));
#1663=EDGE_LOOP('',(#6410,#6411,#6412,#6413));
#1664=EDGE_LOOP('',(#6414,#6415,#6416,#6417));
#1665=EDGE_LOOP('',(#6418));
#1666=EDGE_LOOP('',(#6419,#6420,#6421,#6422,#6423,#6424));
#1667=EDGE_LOOP('',(#6425));
#2047=LINE('',#14488,#2506);
#2048=LINE('',#14512,#2507);
#2049=LINE('',#14560,#2508);
#2050=LINE('',#14608,#2509);
#2051=LINE('',#14659,#2510);
#2052=LINE('',#14707,#2511);
#2053=LINE('',#14755,#2512);
#2054=LINE('',#14803,#2513);
#2055=LINE('',#14857,#2514);
#2056=LINE('',#14905,#2515);
#2057=LINE('',#14953,#2516);
#2058=LINE('',#15007,#2517);
#2059=LINE('',#15055,#2518);
#2060=LINE('',#15103,#2519);
#2061=LINE('',#15151,#2520);
#2062=LINE('',#15205,#2521);
#2063=LINE('',#15253,#2522);
#2064=LINE('',#15301,#2523);
#2065=LINE('',#15355,#2524);
#2066=LINE('',#15403,#2525);
#2067=LINE('',#15451,#2526);
#2068=LINE('',#15505,#2527);
#2069=LINE('',#15553,#2528);
#2070=LINE('',#15601,#2529);
#2071=LINE('',#15649,#2530);
#2072=LINE('',#15703,#2531);
#2073=LINE('',#15751,#2532);
#2074=LINE('',#15799,#2533);
#2075=LINE('',#15853,#2534);
#2076=LINE('',#15901,#2535);
#2077=LINE('',#15949,#2536);
#2078=LINE('',#15975,#2537);
#2079=LINE('',#15999,#2538);
#2080=LINE('',#16023,#2539);
#2081=LINE('',#16048,#2540);
#2082=LINE('',#16073,#2541);
#2083=LINE('',#16097,#2542);
#2084=LINE('',#16122,#2543);
#2085=LINE('',#16147,#2544);
#2086=LINE('',#16171,#2545);
#2087=LINE('',#16195,#2546);
#2088=LINE('',#16220,#2547);
#2089=LINE('',#16245,#2548);
#2090=LINE('',#16269,#2549);
#2091=LINE('',#16294,#2550);
#2092=LINE('',#16319,#2551);
#2093=LINE('',#16343,#2552);
#2094=LINE('',#16368,#2553);
#2095=LINE('',#16393,#2554);
#2096=LINE('',#16417,#2555);
#2097=LINE('',#16441,#2556);
#2098=LINE('',#16466,#2557);
#2099=LINE('',#16491,#2558);
#2100=LINE('',#16515,#2559);
#2101=LINE('',#16540,#2560);
#2102=LINE('',#16565,#2561);
#2103=LINE('',#16589,#2562);
#2104=LINE('',#16614,#2563);
#2105=LINE('',#16638,#2564);
#2106=LINE('',#16663,#2565);
#2107=LINE('',#16864,#2566);
#2108=LINE('',#18609,#2567);
#2109=LINE('',#18611,#2568);
#2110=LINE('',#18613,#2569);
#2111=LINE('',#18614,#2570);
#2112=LINE('',#18617,#2571);
#2113=LINE('',#18619,#2572);
#2114=LINE('',#18620,#2573);
#2115=LINE('',#18623,#2574);
#2116=LINE('',#18625,#2575);
#2117=LINE('',#18626,#2576);
#2118=LINE('',#18629,#2577);
#2119=LINE('',#18631,#2578);
#2120=LINE('',#18632,#2579);
#2121=LINE('',#18635,#2580);
#2122=LINE('',#18637,#2581);
#2123=LINE('',#18638,#2582);
#2124=LINE('',#18640,#2583);
#2125=LINE('',#18641,#2584);
#2126=LINE('',#18648,#2585);
#2506=VECTOR('',#8946,0.15);
#2507=VECTOR('',#8951,0.15);
#2508=VECTOR('',#8954,0.15);
#2509=VECTOR('',#8957,0.15);
#2510=VECTOR('',#8960,0.15);
#2511=VECTOR('',#8963,0.15);
#2512=VECTOR('',#8966,0.15);
#2513=VECTOR('',#8969,0.15);
#2514=VECTOR('',#8972,0.15);
#2515=VECTOR('',#8975,0.15);
#2516=VECTOR('',#8978,0.15);
#2517=VECTOR('',#8981,0.15);
#2518=VECTOR('',#8984,0.15);
#2519=VECTOR('',#8987,0.15);
#2520=VECTOR('',#8990,0.15);
#2521=VECTOR('',#8993,0.15);
#2522=VECTOR('',#8996,0.15);
#2523=VECTOR('',#8999,0.15);
#2524=VECTOR('',#9002,0.15);
#2525=VECTOR('',#9005,0.15);
#2526=VECTOR('',#9008,0.15);
#2527=VECTOR('',#9011,0.15);
#2528=VECTOR('',#9014,0.15);
#2529=VECTOR('',#9017,0.15);
#2530=VECTOR('',#9020,0.15);
#2531=VECTOR('',#9023,0.15);
#2532=VECTOR('',#9026,0.15);
#2533=VECTOR('',#9029,0.15);
#2534=VECTOR('',#9032,0.15);
#2535=VECTOR('',#9035,0.15);
#2536=VECTOR('',#9038,0.117775);
#2537=VECTOR('',#9043,0.117775);
#2538=VECTOR('',#9046,0.117775);
#2539=VECTOR('',#9049,0.117775);
#2540=VECTOR('',#9052,0.117775);
#2541=VECTOR('',#9055,0.117775);
#2542=VECTOR('',#9058,0.117775);
#2543=VECTOR('',#9061,0.117775);
#2544=VECTOR('',#9064,0.117775);
#2545=VECTOR('',#9067,0.117775);
#2546=VECTOR('',#9070,0.117775);
#2547=VECTOR('',#9073,0.117775);
#2548=VECTOR('',#9076,0.117775);
#2549=VECTOR('',#9079,0.117775);
#2550=VECTOR('',#9082,0.117775);
#2551=VECTOR('',#9085,0.117775);
#2552=VECTOR('',#9088,0.117775);
#2553=VECTOR('',#9091,0.117775);
#2554=VECTOR('',#9094,0.117775);
#2555=VECTOR('',#9097,0.117775);
#2556=VECTOR('',#9100,0.117775);
#2557=VECTOR('',#9103,0.117775);
#2558=VECTOR('',#9106,0.117775);
#2559=VECTOR('',#9109,0.117775);
#2560=VECTOR('',#9112,0.117775);
#2561=VECTOR('',#9115,0.117775);
#2562=VECTOR('',#9118,0.117775);
#2563=VECTOR('',#9121,0.117775);
#2564=VECTOR('',#9124,0.117775);
#2565=VECTOR('',#9127,0.117775);
#2566=VECTOR('',#9132,0.1);
#2567=VECTOR('',#9143,1.);
#2568=VECTOR('',#9144,1.);
#2569=VECTOR('',#9145,1.);
#2570=VECTOR('',#9146,1.);
#2571=VECTOR('',#9149,1.);
#2572=VECTOR('',#9150,1.);
#2573=VECTOR('',#9151,1.);
#2574=VECTOR('',#9154,1.);
#2575=VECTOR('',#9155,1.);
#2576=VECTOR('',#9156,1.);
#2577=VECTOR('',#9159,1.);
#2578=VECTOR('',#9160,1.);
#2579=VECTOR('',#9161,1.);
#2580=VECTOR('',#9164,1.);
#2581=VECTOR('',#9165,1.);
#2582=VECTOR('',#9166,1.);
#2583=VECTOR('',#9169,1.);
#2584=VECTOR('',#9170,1.);
#2585=VECTOR('',#9179,0.275);
#2794=CIRCLE('',#7638,0.14635);
#2795=CIRCLE('',#7669,0.117775);
#2796=CIRCLE('',#7700,0.14635);
#2797=CIRCLE('',#7701,0.05);
#2798=CIRCLE('',#7703,0.117775);
#2799=CIRCLE('',#7713,0.275);
#2800=CIRCLE('',#7715,0.275);
#3289=VERTEX_POINT('',#14486);
#3290=VERTEX_POINT('',#14487);
#3291=VERTEX_POINT('',#14489);
#3292=VERTEX_POINT('',#14500);
#3293=VERTEX_POINT('',#14510);
#3294=VERTEX_POINT('',#14511);
#3295=VERTEX_POINT('',#14558);
#3296=VERTEX_POINT('',#14559);
#3297=VERTEX_POINT('',#14606);
#3298=VERTEX_POINT('',#14607);
#3299=VERTEX_POINT('',#14657);
#3300=VERTEX_POINT('',#14658);
#3301=VERTEX_POINT('',#14705);
#3302=VERTEX_POINT('',#14706);
#3303=VERTEX_POINT('',#14753);
#3304=VERTEX_POINT('',#14754);
#3305=VERTEX_POINT('',#14801);
#3306=VERTEX_POINT('',#14802);
#3307=VERTEX_POINT('',#14855);
#3308=VERTEX_POINT('',#14856);
#3309=VERTEX_POINT('',#14903);
#3310=VERTEX_POINT('',#14904);
#3311=VERTEX_POINT('',#14951);
#3312=VERTEX_POINT('',#14952);
#3313=VERTEX_POINT('',#15005);
#3314=VERTEX_POINT('',#15006);
#3315=VERTEX_POINT('',#15053);
#3316=VERTEX_POINT('',#15054);
#3317=VERTEX_POINT('',#15101);
#3318=VERTEX_POINT('',#15102);
#3319=VERTEX_POINT('',#15149);
#3320=VERTEX_POINT('',#15150);
#3321=VERTEX_POINT('',#15203);
#3322=VERTEX_POINT('',#15204);
#3323=VERTEX_POINT('',#15251);
#3324=VERTEX_POINT('',#15252);
#3325=VERTEX_POINT('',#15299);
#3326=VERTEX_POINT('',#15300);
#3327=VERTEX_POINT('',#15353);
#3328=VERTEX_POINT('',#15354);
#3329=VERTEX_POINT('',#15401);
#3330=VERTEX_POINT('',#15402);
#3331=VERTEX_POINT('',#15449);
#3332=VERTEX_POINT('',#15450);
#3333=VERTEX_POINT('',#15503);
#3334=VERTEX_POINT('',#15504);
#3335=VERTEX_POINT('',#15551);
#3336=VERTEX_POINT('',#15552);
#3337=VERTEX_POINT('',#15599);
#3338=VERTEX_POINT('',#15600);
#3339=VERTEX_POINT('',#15647);
#3340=VERTEX_POINT('',#15648);
#3341=VERTEX_POINT('',#15701);
#3342=VERTEX_POINT('',#15702);
#3343=VERTEX_POINT('',#15749);
#3344=VERTEX_POINT('',#15750);
#3345=VERTEX_POINT('',#15797);
#3346=VERTEX_POINT('',#15798);
#3347=VERTEX_POINT('',#15851);
#3348=VERTEX_POINT('',#15852);
#3349=VERTEX_POINT('',#15899);
#3350=VERTEX_POINT('',#15900);
#3351=VERTEX_POINT('',#15947);
#3352=VERTEX_POINT('',#15948);
#3353=VERTEX_POINT('',#15950);
#3354=VERTEX_POINT('',#15961);
#3355=VERTEX_POINT('',#15973);
#3356=VERTEX_POINT('',#15974);
#3357=VERTEX_POINT('',#15997);
#3358=VERTEX_POINT('',#15998);
#3359=VERTEX_POINT('',#16021);
#3360=VERTEX_POINT('',#16022);
#3361=VERTEX_POINT('',#16046);
#3362=VERTEX_POINT('',#16047);
#3363=VERTEX_POINT('',#16071);
#3364=VERTEX_POINT('',#16072);
#3365=VERTEX_POINT('',#16095);
#3366=VERTEX_POINT('',#16096);
#3367=VERTEX_POINT('',#16120);
#3368=VERTEX_POINT('',#16121);
#3369=VERTEX_POINT('',#16145);
#3370=VERTEX_POINT('',#16146);
#3371=VERTEX_POINT('',#16169);
#3372=VERTEX_POINT('',#16170);
#3373=VERTEX_POINT('',#16193);
#3374=VERTEX_POINT('',#16194);
#3375=VERTEX_POINT('',#16218);
#3376=VERTEX_POINT('',#16219);
#3377=VERTEX_POINT('',#16243);
#3378=VERTEX_POINT('',#16244);
#3379=VERTEX_POINT('',#16267);
#3380=VERTEX_POINT('',#16268);
#3381=VERTEX_POINT('',#16292);
#3382=VERTEX_POINT('',#16293);
#3383=VERTEX_POINT('',#16317);
#3384=VERTEX_POINT('',#16318);
#3385=VERTEX_POINT('',#16341);
#3386=VERTEX_POINT('',#16342);
#3387=VERTEX_POINT('',#16366);
#3388=VERTEX_POINT('',#16367);
#3389=VERTEX_POINT('',#16391);
#3390=VERTEX_POINT('',#16392);
#3391=VERTEX_POINT('',#16415);
#3392=VERTEX_POINT('',#16416);
#3393=VERTEX_POINT('',#16439);
#3394=VERTEX_POINT('',#16440);
#3395=VERTEX_POINT('',#16464);
#3396=VERTEX_POINT('',#16465);
#3397=VERTEX_POINT('',#16489);
#3398=VERTEX_POINT('',#16490);
#3399=VERTEX_POINT('',#16513);
#3400=VERTEX_POINT('',#16514);
#3401=VERTEX_POINT('',#16538);
#3402=VERTEX_POINT('',#16539);
#3403=VERTEX_POINT('',#16563);
#3404=VERTEX_POINT('',#16564);
#3405=VERTEX_POINT('',#16587);
#3406=VERTEX_POINT('',#16588);
#3407=VERTEX_POINT('',#16612);
#3408=VERTEX_POINT('',#16613);
#3409=VERTEX_POINT('',#16636);
#3410=VERTEX_POINT('',#16637);
#3411=VERTEX_POINT('',#16661);
#3412=VERTEX_POINT('',#16662);
#3413=VERTEX_POINT('',#16685);
#3414=VERTEX_POINT('',#16807);
#3415=VERTEX_POINT('',#16845);
#3416=VERTEX_POINT('',#16863);
#3417=VERTEX_POINT('',#17650);
#3418=VERTEX_POINT('',#17728);
#3419=VERTEX_POINT('',#18607);
#3420=VERTEX_POINT('',#18608);
#3421=VERTEX_POINT('',#18610);
#3422=VERTEX_POINT('',#18612);
#3423=VERTEX_POINT('',#18616);
#3424=VERTEX_POINT('',#18618);
#3425=VERTEX_POINT('',#18622);
#3426=VERTEX_POINT('',#18624);
#3427=VERTEX_POINT('',#18628);
#3428=VERTEX_POINT('',#18630);
#3429=VERTEX_POINT('',#18634);
#3430=VERTEX_POINT('',#18636);
#3431=VERTEX_POINT('',#18644);
#3432=VERTEX_POINT('',#18647);
#4222=EDGE_CURVE('',#3289,#3290,#2047,.T.);
#4223=EDGE_CURVE('',#3289,#3291,#389,.T.);
#4224=EDGE_CURVE('',#3291,#3292,#2794,.F.);
#4225=EDGE_CURVE('',#3292,#3290,#390,.T.);
#4226=EDGE_CURVE('',#3293,#3294,#2048,.T.);
#4227=EDGE_CURVE('',#3293,#3289,#391,.T.);
#4228=EDGE_CURVE('',#3290,#3294,#392,.T.);
#4229=EDGE_CURVE('',#3295,#3296,#2049,.T.);
#4230=EDGE_CURVE('',#3295,#3293,#393,.T.);
#4231=EDGE_CURVE('',#3294,#3296,#394,.T.);
#4232=EDGE_CURVE('',#3297,#3298,#2050,.T.);
#4233=EDGE_CURVE('',#3297,#3295,#395,.T.);
#4234=EDGE_CURVE('',#3296,#3298,#396,.T.);
#4235=EDGE_CURVE('',#3299,#3300,#2051,.T.);
#4236=EDGE_CURVE('',#3299,#3297,#397,.T.);
#4237=EDGE_CURVE('',#3298,#3300,#398,.T.);
#4238=EDGE_CURVE('',#3301,#3302,#2052,.T.);
#4239=EDGE_CURVE('',#3301,#3299,#399,.T.);
#4240=EDGE_CURVE('',#3300,#3302,#400,.T.);
#4241=EDGE_CURVE('',#3303,#3304,#2053,.T.);
#4242=EDGE_CURVE('',#3303,#3301,#401,.T.);
#4243=EDGE_CURVE('',#3302,#3304,#402,.T.);
#4244=EDGE_CURVE('',#3305,#3306,#2054,.T.);
#4245=EDGE_CURVE('',#3305,#3303,#403,.T.);
#4246=EDGE_CURVE('',#3304,#3306,#404,.T.);
#4247=EDGE_CURVE('',#3307,#3308,#2055,.T.);
#4248=EDGE_CURVE('',#3307,#3305,#405,.T.);
#4249=EDGE_CURVE('',#3306,#3308,#406,.T.);
#4250=EDGE_CURVE('',#3309,#3310,#2056,.T.);
#4251=EDGE_CURVE('',#3309,#3307,#407,.T.);
#4252=EDGE_CURVE('',#3308,#3310,#408,.T.);
#4253=EDGE_CURVE('',#3311,#3312,#2057,.T.);
#4254=EDGE_CURVE('',#3311,#3309,#409,.T.);
#4255=EDGE_CURVE('',#3310,#3312,#410,.T.);
#4256=EDGE_CURVE('',#3313,#3314,#2058,.T.);
#4257=EDGE_CURVE('',#3313,#3311,#411,.T.);
#4258=EDGE_CURVE('',#3312,#3314,#412,.T.);
#4259=EDGE_CURVE('',#3315,#3316,#2059,.T.);
#4260=EDGE_CURVE('',#3315,#3313,#413,.T.);
#4261=EDGE_CURVE('',#3314,#3316,#414,.T.);
#4262=EDGE_CURVE('',#3317,#3318,#2060,.T.);
#4263=EDGE_CURVE('',#3317,#3315,#415,.T.);
#4264=EDGE_CURVE('',#3316,#3318,#416,.T.);
#4265=EDGE_CURVE('',#3319,#3320,#2061,.T.);
#4266=EDGE_CURVE('',#3319,#3317,#417,.T.);
#4267=EDGE_CURVE('',#3318,#3320,#418,.T.);
#4268=EDGE_CURVE('',#3321,#3322,#2062,.T.);
#4269=EDGE_CURVE('',#3321,#3319,#419,.T.);
#4270=EDGE_CURVE('',#3320,#3322,#420,.T.);
#4271=EDGE_CURVE('',#3323,#3324,#2063,.T.);
#4272=EDGE_CURVE('',#3323,#3321,#421,.T.);
#4273=EDGE_CURVE('',#3322,#3324,#422,.T.);
#4274=EDGE_CURVE('',#3325,#3326,#2064,.T.);
#4275=EDGE_CURVE('',#3325,#3323,#423,.T.);
#4276=EDGE_CURVE('',#3324,#3326,#424,.T.);
#4277=EDGE_CURVE('',#3327,#3328,#2065,.T.);
#4278=EDGE_CURVE('',#3327,#3325,#425,.T.);
#4279=EDGE_CURVE('',#3326,#3328,#426,.T.);
#4280=EDGE_CURVE('',#3329,#3330,#2066,.T.);
#4281=EDGE_CURVE('',#3329,#3327,#427,.T.);
#4282=EDGE_CURVE('',#3328,#3330,#428,.T.);
#4283=EDGE_CURVE('',#3331,#3332,#2067,.T.);
#4284=EDGE_CURVE('',#3331,#3329,#429,.T.);
#4285=EDGE_CURVE('',#3330,#3332,#430,.T.);
#4286=EDGE_CURVE('',#3333,#3334,#2068,.T.);
#4287=EDGE_CURVE('',#3333,#3331,#431,.T.);
#4288=EDGE_CURVE('',#3332,#3334,#432,.T.);
#4289=EDGE_CURVE('',#3335,#3336,#2069,.T.);
#4290=EDGE_CURVE('',#3335,#3333,#433,.T.);
#4291=EDGE_CURVE('',#3334,#3336,#434,.T.);
#4292=EDGE_CURVE('',#3337,#3338,#2070,.T.);
#4293=EDGE_CURVE('',#3337,#3335,#435,.T.);
#4294=EDGE_CURVE('',#3336,#3338,#436,.T.);
#4295=EDGE_CURVE('',#3339,#3340,#2071,.T.);
#4296=EDGE_CURVE('',#3339,#3337,#437,.T.);
#4297=EDGE_CURVE('',#3338,#3340,#438,.T.);
#4298=EDGE_CURVE('',#3341,#3342,#2072,.T.);
#4299=EDGE_CURVE('',#3341,#3339,#439,.T.);
#4300=EDGE_CURVE('',#3340,#3342,#440,.T.);
#4301=EDGE_CURVE('',#3343,#3344,#2073,.T.);
#4302=EDGE_CURVE('',#3343,#3341,#441,.T.);
#4303=EDGE_CURVE('',#3342,#3344,#442,.T.);
#4304=EDGE_CURVE('',#3345,#3346,#2074,.T.);
#4305=EDGE_CURVE('',#3345,#3343,#443,.T.);
#4306=EDGE_CURVE('',#3344,#3346,#444,.T.);
#4307=EDGE_CURVE('',#3347,#3348,#2075,.T.);
#4308=EDGE_CURVE('',#3347,#3345,#445,.T.);
#4309=EDGE_CURVE('',#3346,#3348,#446,.T.);
#4310=EDGE_CURVE('',#3349,#3350,#2076,.T.);
#4311=EDGE_CURVE('',#3349,#3347,#447,.T.);
#4312=EDGE_CURVE('',#3348,#3350,#448,.T.);
#4313=EDGE_CURVE('',#3351,#3352,#2077,.T.);
#4314=EDGE_CURVE('',#3351,#3353,#449,.T.);
#4315=EDGE_CURVE('',#3353,#3354,#2795,.T.);
#4316=EDGE_CURVE('',#3352,#3354,#450,.T.);
#4317=EDGE_CURVE('',#3355,#3356,#2078,.T.);
#4318=EDGE_CURVE('',#3355,#3351,#451,.T.);
#4319=EDGE_CURVE('',#3356,#3352,#452,.T.);
#4320=EDGE_CURVE('',#3357,#3358,#2079,.T.);
#4321=EDGE_CURVE('',#3357,#3355,#453,.T.);
#4322=EDGE_CURVE('',#3358,#3356,#454,.T.);
#4323=EDGE_CURVE('',#3359,#3360,#2080,.T.);
#4324=EDGE_CURVE('',#3359,#3357,#455,.T.);
#4325=EDGE_CURVE('',#3360,#3358,#456,.T.);
#4326=EDGE_CURVE('',#3361,#3362,#2081,.T.);
#4327=EDGE_CURVE('',#3361,#3359,#457,.T.);
#4328=EDGE_CURVE('',#3362,#3360,#458,.T.);
#4329=EDGE_CURVE('',#3363,#3364,#2082,.T.);
#4330=EDGE_CURVE('',#3363,#3361,#459,.T.);
#4331=EDGE_CURVE('',#3364,#3362,#460,.T.);
#4332=EDGE_CURVE('',#3365,#3366,#2083,.T.);
#4333=EDGE_CURVE('',#3365,#3363,#461,.T.);
#4334=EDGE_CURVE('',#3366,#3364,#462,.T.);
#4335=EDGE_CURVE('',#3367,#3368,#2084,.T.);
#4336=EDGE_CURVE('',#3367,#3365,#463,.T.);
#4337=EDGE_CURVE('',#3368,#3366,#464,.T.);
#4338=EDGE_CURVE('',#3369,#3370,#2085,.T.);
#4339=EDGE_CURVE('',#3369,#3367,#465,.T.);
#4340=EDGE_CURVE('',#3370,#3368,#466,.T.);
#4341=EDGE_CURVE('',#3371,#3372,#2086,.T.);
#4342=EDGE_CURVE('',#3371,#3369,#467,.T.);
#4343=EDGE_CURVE('',#3372,#3370,#468,.T.);
#4344=EDGE_CURVE('',#3373,#3374,#2087,.T.);
#4345=EDGE_CURVE('',#3373,#3371,#469,.T.);
#4346=EDGE_CURVE('',#3374,#3372,#470,.T.);
#4347=EDGE_CURVE('',#3375,#3376,#2088,.T.);
#4348=EDGE_CURVE('',#3375,#3373,#471,.T.);
#4349=EDGE_CURVE('',#3376,#3374,#472,.T.);
#4350=EDGE_CURVE('',#3377,#3378,#2089,.T.);
#4351=EDGE_CURVE('',#3377,#3375,#473,.T.);
#4352=EDGE_CURVE('',#3378,#3376,#474,.T.);
#4353=EDGE_CURVE('',#3379,#3380,#2090,.T.);
#4354=EDGE_CURVE('',#3379,#3377,#475,.T.);
#4355=EDGE_CURVE('',#3380,#3378,#476,.T.);
#4356=EDGE_CURVE('',#3381,#3382,#2091,.T.);
#4357=EDGE_CURVE('',#3381,#3379,#477,.T.);
#4358=EDGE_CURVE('',#3382,#3380,#478,.T.);
#4359=EDGE_CURVE('',#3383,#3384,#2092,.T.);
#4360=EDGE_CURVE('',#3383,#3381,#479,.T.);
#4361=EDGE_CURVE('',#3384,#3382,#480,.T.);
#4362=EDGE_CURVE('',#3385,#3386,#2093,.T.);
#4363=EDGE_CURVE('',#3385,#3383,#481,.T.);
#4364=EDGE_CURVE('',#3386,#3384,#482,.T.);
#4365=EDGE_CURVE('',#3387,#3388,#2094,.T.);
#4366=EDGE_CURVE('',#3387,#3385,#483,.T.);
#4367=EDGE_CURVE('',#3388,#3386,#484,.T.);
#4368=EDGE_CURVE('',#3389,#3390,#2095,.T.);
#4369=EDGE_CURVE('',#3389,#3387,#485,.T.);
#4370=EDGE_CURVE('',#3390,#3388,#486,.T.);
#4371=EDGE_CURVE('',#3391,#3392,#2096,.T.);
#4372=EDGE_CURVE('',#3391,#3389,#487,.T.);
#4373=EDGE_CURVE('',#3392,#3390,#488,.T.);
#4374=EDGE_CURVE('',#3393,#3394,#2097,.T.);
#4375=EDGE_CURVE('',#3393,#3391,#489,.T.);
#4376=EDGE_CURVE('',#3394,#3392,#490,.T.);
#4377=EDGE_CURVE('',#3395,#3396,#2098,.T.);
#4378=EDGE_CURVE('',#3395,#3393,#491,.T.);
#4379=EDGE_CURVE('',#3396,#3394,#492,.T.);
#4380=EDGE_CURVE('',#3397,#3398,#2099,.T.);
#4381=EDGE_CURVE('',#3397,#3395,#493,.T.);
#4382=EDGE_CURVE('',#3398,#3396,#494,.T.);
#4383=EDGE_CURVE('',#3399,#3400,#2100,.T.);
#4384=EDGE_CURVE('',#3399,#3397,#495,.T.);
#4385=EDGE_CURVE('',#3400,#3398,#496,.T.);
#4386=EDGE_CURVE('',#3401,#3402,#2101,.T.);
#4387=EDGE_CURVE('',#3401,#3399,#497,.T.);
#4388=EDGE_CURVE('',#3402,#3400,#498,.T.);
#4389=EDGE_CURVE('',#3403,#3404,#2102,.T.);
#4390=EDGE_CURVE('',#3403,#3401,#499,.T.);
#4391=EDGE_CURVE('',#3404,#3402,#500,.T.);
#4392=EDGE_CURVE('',#3405,#3406,#2103,.T.);
#4393=EDGE_CURVE('',#3405,#3403,#501,.T.);
#4394=EDGE_CURVE('',#3406,#3404,#502,.T.);
#4395=EDGE_CURVE('',#3407,#3408,#2104,.T.);
#4396=EDGE_CURVE('',#3407,#3405,#503,.T.);
#4397=EDGE_CURVE('',#3408,#3406,#504,.T.);
#4398=EDGE_CURVE('',#3409,#3410,#2105,.T.);
#4399=EDGE_CURVE('',#3409,#3407,#505,.T.);
#4400=EDGE_CURVE('',#3410,#3408,#506,.T.);
#4401=EDGE_CURVE('',#3411,#3412,#2106,.T.);
#4402=EDGE_CURVE('',#3411,#3409,#507,.T.);
#4403=EDGE_CURVE('',#3412,#3410,#508,.T.);
#4404=EDGE_CURVE('',#3354,#3413,#509,.T.);
#4405=EDGE_CURVE('',#3414,#3353,#510,.T.);
#4406=EDGE_CURVE('',#3415,#3414,#2796,.T.);
#4407=EDGE_CURVE('',#3413,#3415,#511,.T.);
#4408=EDGE_CURVE('',#3413,#3416,#2107,.T.);
#4409=EDGE_CURVE('',#3416,#3416,#2797,.T.);
#4410=EDGE_CURVE('',#3417,#3411,#512,.T.);
#4411=EDGE_CURVE('',#3291,#3417,#513,.T.);
#4412=EDGE_CURVE('',#3414,#3349,#514,.T.);
#4413=EDGE_CURVE('',#3418,#3412,#515,.T.);
#4414=EDGE_CURVE('',#3417,#3418,#2798,.T.);
#4415=EDGE_CURVE('',#3350,#3415,#516,.T.);
#4416=EDGE_CURVE('',#3418,#3292,#517,.T.);
#4417=EDGE_CURVE('',#3419,#3420,#2108,.T.);
#4418=EDGE_CURVE('',#3419,#3421,#2109,.T.);
#4419=EDGE_CURVE('',#3421,#3422,#2110,.T.);
#4420=EDGE_CURVE('',#3420,#3422,#2111,.T.);
#4421=EDGE_CURVE('',#3423,#3419,#2112,.T.);
#4422=EDGE_CURVE('',#3423,#3424,#2113,.T.);
#4423=EDGE_CURVE('',#3424,#3421,#2114,.T.);
#4424=EDGE_CURVE('',#3425,#3423,#2115,.T.);
#4425=EDGE_CURVE('',#3425,#3426,#2116,.T.);
#4426=EDGE_CURVE('',#3426,#3424,#2117,.T.);
#4427=EDGE_CURVE('',#3427,#3425,#2118,.T.);
#4428=EDGE_CURVE('',#3427,#3428,#2119,.T.);
#4429=EDGE_CURVE('',#3428,#3426,#2120,.T.);
#4430=EDGE_CURVE('',#3429,#3427,#2121,.T.);
#4431=EDGE_CURVE('',#3429,#3430,#2122,.T.);
#4432=EDGE_CURVE('',#3430,#3428,#2123,.T.);
#4433=EDGE_CURVE('',#3420,#3429,#2124,.T.);
#4434=EDGE_CURVE('',#3422,#3430,#2125,.T.);
#4435=EDGE_CURVE('',#3431,#3431,#2799,.T.);
#4436=EDGE_CURVE('',#3431,#3432,#2126,.T.);
#4437=EDGE_CURVE('',#3432,#3432,#2800,.T.);
#5994=ORIENTED_EDGE('',*,*,#4222,.F.);
#5995=ORIENTED_EDGE('',*,*,#4223,.T.);
#5996=ORIENTED_EDGE('',*,*,#4224,.T.);
#5997=ORIENTED_EDGE('',*,*,#4225,.T.);
#5998=ORIENTED_EDGE('',*,*,#4226,.F.);
#5999=ORIENTED_EDGE('',*,*,#4227,.T.);
#6000=ORIENTED_EDGE('',*,*,#4222,.T.);
#6001=ORIENTED_EDGE('',*,*,#4228,.T.);
#6002=ORIENTED_EDGE('',*,*,#4229,.F.);
#6003=ORIENTED_EDGE('',*,*,#4230,.T.);
#6004=ORIENTED_EDGE('',*,*,#4226,.T.);
#6005=ORIENTED_EDGE('',*,*,#4231,.T.);
#6006=ORIENTED_EDGE('',*,*,#4232,.F.);
#6007=ORIENTED_EDGE('',*,*,#4233,.T.);
#6008=ORIENTED_EDGE('',*,*,#4229,.T.);
#6009=ORIENTED_EDGE('',*,*,#4234,.T.);
#6010=ORIENTED_EDGE('',*,*,#4235,.F.);
#6011=ORIENTED_EDGE('',*,*,#4236,.T.);
#6012=ORIENTED_EDGE('',*,*,#4232,.T.);
#6013=ORIENTED_EDGE('',*,*,#4237,.T.);
#6014=ORIENTED_EDGE('',*,*,#4238,.F.);
#6015=ORIENTED_EDGE('',*,*,#4239,.T.);
#6016=ORIENTED_EDGE('',*,*,#4235,.T.);
#6017=ORIENTED_EDGE('',*,*,#4240,.T.);
#6018=ORIENTED_EDGE('',*,*,#4241,.F.);
#6019=ORIENTED_EDGE('',*,*,#4242,.T.);
#6020=ORIENTED_EDGE('',*,*,#4238,.T.);
#6021=ORIENTED_EDGE('',*,*,#4243,.T.);
#6022=ORIENTED_EDGE('',*,*,#4244,.F.);
#6023=ORIENTED_EDGE('',*,*,#4245,.T.);
#6024=ORIENTED_EDGE('',*,*,#4241,.T.);
#6025=ORIENTED_EDGE('',*,*,#4246,.T.);
#6026=ORIENTED_EDGE('',*,*,#4247,.F.);
#6027=ORIENTED_EDGE('',*,*,#4248,.T.);
#6028=ORIENTED_EDGE('',*,*,#4244,.T.);
#6029=ORIENTED_EDGE('',*,*,#4249,.T.);
#6030=ORIENTED_EDGE('',*,*,#4250,.F.);
#6031=ORIENTED_EDGE('',*,*,#4251,.T.);
#6032=ORIENTED_EDGE('',*,*,#4247,.T.);
#6033=ORIENTED_EDGE('',*,*,#4252,.T.);
#6034=ORIENTED_EDGE('',*,*,#4253,.F.);
#6035=ORIENTED_EDGE('',*,*,#4254,.T.);
#6036=ORIENTED_EDGE('',*,*,#4250,.T.);
#6037=ORIENTED_EDGE('',*,*,#4255,.T.);
#6038=ORIENTED_EDGE('',*,*,#4256,.F.);
#6039=ORIENTED_EDGE('',*,*,#4257,.T.);
#6040=ORIENTED_EDGE('',*,*,#4253,.T.);
#6041=ORIENTED_EDGE('',*,*,#4258,.T.);
#6042=ORIENTED_EDGE('',*,*,#4259,.F.);
#6043=ORIENTED_EDGE('',*,*,#4260,.T.);
#6044=ORIENTED_EDGE('',*,*,#4256,.T.);
#6045=ORIENTED_EDGE('',*,*,#4261,.T.);
#6046=ORIENTED_EDGE('',*,*,#4262,.F.);
#6047=ORIENTED_EDGE('',*,*,#4263,.T.);
#6048=ORIENTED_EDGE('',*,*,#4259,.T.);
#6049=ORIENTED_EDGE('',*,*,#4264,.T.);
#6050=ORIENTED_EDGE('',*,*,#4265,.F.);
#6051=ORIENTED_EDGE('',*,*,#4266,.T.);
#6052=ORIENTED_EDGE('',*,*,#4262,.T.);
#6053=ORIENTED_EDGE('',*,*,#4267,.T.);
#6054=ORIENTED_EDGE('',*,*,#4268,.F.);
#6055=ORIENTED_EDGE('',*,*,#4269,.T.);
#6056=ORIENTED_EDGE('',*,*,#4265,.T.);
#6057=ORIENTED_EDGE('',*,*,#4270,.T.);
#6058=ORIENTED_EDGE('',*,*,#4271,.F.);
#6059=ORIENTED_EDGE('',*,*,#4272,.T.);
#6060=ORIENTED_EDGE('',*,*,#4268,.T.);
#6061=ORIENTED_EDGE('',*,*,#4273,.T.);
#6062=ORIENTED_EDGE('',*,*,#4274,.F.);
#6063=ORIENTED_EDGE('',*,*,#4275,.T.);
#6064=ORIENTED_EDGE('',*,*,#4271,.T.);
#6065=ORIENTED_EDGE('',*,*,#4276,.T.);
#6066=ORIENTED_EDGE('',*,*,#4277,.F.);
#6067=ORIENTED_EDGE('',*,*,#4278,.T.);
#6068=ORIENTED_EDGE('',*,*,#4274,.T.);
#6069=ORIENTED_EDGE('',*,*,#4279,.T.);
#6070=ORIENTED_EDGE('',*,*,#4280,.F.);
#6071=ORIENTED_EDGE('',*,*,#4281,.T.);
#6072=ORIENTED_EDGE('',*,*,#4277,.T.);
#6073=ORIENTED_EDGE('',*,*,#4282,.T.);
#6074=ORIENTED_EDGE('',*,*,#4283,.F.);
#6075=ORIENTED_EDGE('',*,*,#4284,.T.);
#6076=ORIENTED_EDGE('',*,*,#4280,.T.);
#6077=ORIENTED_EDGE('',*,*,#4285,.T.);
#6078=ORIENTED_EDGE('',*,*,#4286,.F.);
#6079=ORIENTED_EDGE('',*,*,#4287,.T.);
#6080=ORIENTED_EDGE('',*,*,#4283,.T.);
#6081=ORIENTED_EDGE('',*,*,#4288,.T.);
#6082=ORIENTED_EDGE('',*,*,#4289,.F.);
#6083=ORIENTED_EDGE('',*,*,#4290,.T.);
#6084=ORIENTED_EDGE('',*,*,#4286,.T.);
#6085=ORIENTED_EDGE('',*,*,#4291,.T.);
#6086=ORIENTED_EDGE('',*,*,#4292,.F.);
#6087=ORIENTED_EDGE('',*,*,#4293,.T.);
#6088=ORIENTED_EDGE('',*,*,#4289,.T.);
#6089=ORIENTED_EDGE('',*,*,#4294,.T.);
#6090=ORIENTED_EDGE('',*,*,#4295,.F.);
#6091=ORIENTED_EDGE('',*,*,#4296,.T.);
#6092=ORIENTED_EDGE('',*,*,#4292,.T.);
#6093=ORIENTED_EDGE('',*,*,#4297,.T.);
#6094=ORIENTED_EDGE('',*,*,#4298,.F.);
#6095=ORIENTED_EDGE('',*,*,#4299,.T.);
#6096=ORIENTED_EDGE('',*,*,#4295,.T.);
#6097=ORIENTED_EDGE('',*,*,#4300,.T.);
#6098=ORIENTED_EDGE('',*,*,#4301,.F.);
#6099=ORIENTED_EDGE('',*,*,#4302,.T.);
#6100=ORIENTED_EDGE('',*,*,#4298,.T.);
#6101=ORIENTED_EDGE('',*,*,#4303,.T.);
#6102=ORIENTED_EDGE('',*,*,#4304,.F.);
#6103=ORIENTED_EDGE('',*,*,#4305,.T.);
#6104=ORIENTED_EDGE('',*,*,#4301,.T.);
#6105=ORIENTED_EDGE('',*,*,#4306,.T.);
#6106=ORIENTED_EDGE('',*,*,#4307,.F.);
#6107=ORIENTED_EDGE('',*,*,#4308,.T.);
#6108=ORIENTED_EDGE('',*,*,#4304,.T.);
#6109=ORIENTED_EDGE('',*,*,#4309,.T.);
#6110=ORIENTED_EDGE('',*,*,#4310,.F.);
#6111=ORIENTED_EDGE('',*,*,#4311,.T.);
#6112=ORIENTED_EDGE('',*,*,#4307,.T.);
#6113=ORIENTED_EDGE('',*,*,#4312,.T.);
#6114=ORIENTED_EDGE('',*,*,#4313,.F.);
#6115=ORIENTED_EDGE('',*,*,#4314,.T.);
#6116=ORIENTED_EDGE('',*,*,#4315,.T.);
#6117=ORIENTED_EDGE('',*,*,#4316,.F.);
#6118=ORIENTED_EDGE('',*,*,#4317,.F.);
#6119=ORIENTED_EDGE('',*,*,#4318,.T.);
#6120=ORIENTED_EDGE('',*,*,#4313,.T.);
#6121=ORIENTED_EDGE('',*,*,#4319,.F.);
#6122=ORIENTED_EDGE('',*,*,#4320,.F.);
#6123=ORIENTED_EDGE('',*,*,#4321,.T.);
#6124=ORIENTED_EDGE('',*,*,#4317,.T.);
#6125=ORIENTED_EDGE('',*,*,#4322,.F.);
#6126=ORIENTED_EDGE('',*,*,#4323,.F.);
#6127=ORIENTED_EDGE('',*,*,#4324,.T.);
#6128=ORIENTED_EDGE('',*,*,#4320,.T.);
#6129=ORIENTED_EDGE('',*,*,#4325,.F.);
#6130=ORIENTED_EDGE('',*,*,#4326,.F.);
#6131=ORIENTED_EDGE('',*,*,#4327,.T.);
#6132=ORIENTED_EDGE('',*,*,#4323,.T.);
#6133=ORIENTED_EDGE('',*,*,#4328,.F.);
#6134=ORIENTED_EDGE('',*,*,#4329,.F.);
#6135=ORIENTED_EDGE('',*,*,#4330,.T.);
#6136=ORIENTED_EDGE('',*,*,#4326,.T.);
#6137=ORIENTED_EDGE('',*,*,#4331,.F.);
#6138=ORIENTED_EDGE('',*,*,#4332,.F.);
#6139=ORIENTED_EDGE('',*,*,#4333,.T.);
#6140=ORIENTED_EDGE('',*,*,#4329,.T.);
#6141=ORIENTED_EDGE('',*,*,#4334,.F.);
#6142=ORIENTED_EDGE('',*,*,#4335,.F.);
#6143=ORIENTED_EDGE('',*,*,#4336,.T.);
#6144=ORIENTED_EDGE('',*,*,#4332,.T.);
#6145=ORIENTED_EDGE('',*,*,#4337,.F.);
#6146=ORIENTED_EDGE('',*,*,#4338,.F.);
#6147=ORIENTED_EDGE('',*,*,#4339,.T.);
#6148=ORIENTED_EDGE('',*,*,#4335,.T.);
#6149=ORIENTED_EDGE('',*,*,#4340,.F.);
#6150=ORIENTED_EDGE('',*,*,#4341,.F.);
#6151=ORIENTED_EDGE('',*,*,#4342,.T.);
#6152=ORIENTED_EDGE('',*,*,#4338,.T.);
#6153=ORIENTED_EDGE('',*,*,#4343,.F.);
#6154=ORIENTED_EDGE('',*,*,#4344,.F.);
#6155=ORIENTED_EDGE('',*,*,#4345,.T.);
#6156=ORIENTED_EDGE('',*,*,#4341,.T.);
#6157=ORIENTED_EDGE('',*,*,#4346,.F.);
#6158=ORIENTED_EDGE('',*,*,#4347,.F.);
#6159=ORIENTED_EDGE('',*,*,#4348,.T.);
#6160=ORIENTED_EDGE('',*,*,#4344,.T.);
#6161=ORIENTED_EDGE('',*,*,#4349,.F.);
#6162=ORIENTED_EDGE('',*,*,#4350,.F.);
#6163=ORIENTED_EDGE('',*,*,#4351,.T.);
#6164=ORIENTED_EDGE('',*,*,#4347,.T.);
#6165=ORIENTED_EDGE('',*,*,#4352,.F.);
#6166=ORIENTED_EDGE('',*,*,#4353,.F.);
#6167=ORIENTED_EDGE('',*,*,#4354,.T.);
#6168=ORIENTED_EDGE('',*,*,#4350,.T.);
#6169=ORIENTED_EDGE('',*,*,#4355,.F.);
#6170=ORIENTED_EDGE('',*,*,#4356,.F.);
#6171=ORIENTED_EDGE('',*,*,#4357,.T.);
#6172=ORIENTED_EDGE('',*,*,#4353,.T.);
#6173=ORIENTED_EDGE('',*,*,#4358,.F.);
#6174=ORIENTED_EDGE('',*,*,#4359,.F.);
#6175=ORIENTED_EDGE('',*,*,#4360,.T.);
#6176=ORIENTED_EDGE('',*,*,#4356,.T.);
#6177=ORIENTED_EDGE('',*,*,#4361,.F.);
#6178=ORIENTED_EDGE('',*,*,#4362,.F.);
#6179=ORIENTED_EDGE('',*,*,#4363,.T.);
#6180=ORIENTED_EDGE('',*,*,#4359,.T.);
#6181=ORIENTED_EDGE('',*,*,#4364,.F.);
#6182=ORIENTED_EDGE('',*,*,#4365,.F.);
#6183=ORIENTED_EDGE('',*,*,#4366,.T.);
#6184=ORIENTED_EDGE('',*,*,#4362,.T.);
#6185=ORIENTED_EDGE('',*,*,#4367,.F.);
#6186=ORIENTED_EDGE('',*,*,#4368,.F.);
#6187=ORIENTED_EDGE('',*,*,#4369,.T.);
#6188=ORIENTED_EDGE('',*,*,#4365,.T.);
#6189=ORIENTED_EDGE('',*,*,#4370,.F.);
#6190=ORIENTED_EDGE('',*,*,#4371,.F.);
#6191=ORIENTED_EDGE('',*,*,#4372,.T.);
#6192=ORIENTED_EDGE('',*,*,#4368,.T.);
#6193=ORIENTED_EDGE('',*,*,#4373,.F.);
#6194=ORIENTED_EDGE('',*,*,#4374,.F.);
#6195=ORIENTED_EDGE('',*,*,#4375,.T.);
#6196=ORIENTED_EDGE('',*,*,#4371,.T.);
#6197=ORIENTED_EDGE('',*,*,#4376,.F.);
#6198=ORIENTED_EDGE('',*,*,#4377,.F.);
#6199=ORIENTED_EDGE('',*,*,#4378,.T.);
#6200=ORIENTED_EDGE('',*,*,#4374,.T.);
#6201=ORIENTED_EDGE('',*,*,#4379,.F.);
#6202=ORIENTED_EDGE('',*,*,#4380,.F.);
#6203=ORIENTED_EDGE('',*,*,#4381,.T.);
#6204=ORIENTED_EDGE('',*,*,#4377,.T.);
#6205=ORIENTED_EDGE('',*,*,#4382,.F.);
#6206=ORIENTED_EDGE('',*,*,#4383,.F.);
#6207=ORIENTED_EDGE('',*,*,#4384,.T.);
#6208=ORIENTED_EDGE('',*,*,#4380,.T.);
#6209=ORIENTED_EDGE('',*,*,#4385,.F.);
#6210=ORIENTED_EDGE('',*,*,#4386,.F.);
#6211=ORIENTED_EDGE('',*,*,#4387,.T.);
#6212=ORIENTED_EDGE('',*,*,#4383,.T.);
#6213=ORIENTED_EDGE('',*,*,#4388,.F.);
#6214=ORIENTED_EDGE('',*,*,#4389,.F.);
#6215=ORIENTED_EDGE('',*,*,#4390,.T.);
#6216=ORIENTED_EDGE('',*,*,#4386,.T.);
#6217=ORIENTED_EDGE('',*,*,#4391,.F.);
#6218=ORIENTED_EDGE('',*,*,#4392,.F.);
#6219=ORIENTED_EDGE('',*,*,#4393,.T.);
#6220=ORIENTED_EDGE('',*,*,#4389,.T.);
#6221=ORIENTED_EDGE('',*,*,#4394,.F.);
#6222=ORIENTED_EDGE('',*,*,#4395,.F.);
#6223=ORIENTED_EDGE('',*,*,#4396,.T.);
#6224=ORIENTED_EDGE('',*,*,#4392,.T.);
#6225=ORIENTED_EDGE('',*,*,#4397,.F.);
#6226=ORIENTED_EDGE('',*,*,#4398,.F.);
#6227=ORIENTED_EDGE('',*,*,#4399,.T.);
#6228=ORIENTED_EDGE('',*,*,#4395,.T.);
#6229=ORIENTED_EDGE('',*,*,#4400,.F.);
#6230=ORIENTED_EDGE('',*,*,#4401,.F.);
#6231=ORIENTED_EDGE('',*,*,#4402,.T.);
#6232=ORIENTED_EDGE('',*,*,#4398,.T.);
#6233=ORIENTED_EDGE('',*,*,#4403,.F.);
#6234=ORIENTED_EDGE('',*,*,#4404,.F.);
#6235=ORIENTED_EDGE('',*,*,#4315,.F.);
#6236=ORIENTED_EDGE('',*,*,#4405,.F.);
#6237=ORIENTED_EDGE('',*,*,#4406,.F.);
#6238=ORIENTED_EDGE('',*,*,#4407,.F.);
#6239=ORIENTED_EDGE('',*,*,#4408,.T.);
#6240=ORIENTED_EDGE('',*,*,#4409,.F.);
#6241=ORIENTED_EDGE('',*,*,#4408,.F.);
#6242=ORIENTED_EDGE('',*,*,#4405,.T.);
#6243=ORIENTED_EDGE('',*,*,#4314,.F.);
#6244=ORIENTED_EDGE('',*,*,#4318,.F.);
#6245=ORIENTED_EDGE('',*,*,#4321,.F.);
#6246=ORIENTED_EDGE('',*,*,#4324,.F.);
#6247=ORIENTED_EDGE('',*,*,#4327,.F.);
#6248=ORIENTED_EDGE('',*,*,#4330,.F.);
#6249=ORIENTED_EDGE('',*,*,#4333,.F.);
#6250=ORIENTED_EDGE('',*,*,#4336,.F.);
#6251=ORIENTED_EDGE('',*,*,#4339,.F.);
#6252=ORIENTED_EDGE('',*,*,#4342,.F.);
#6253=ORIENTED_EDGE('',*,*,#4345,.F.);
#6254=ORIENTED_EDGE('',*,*,#4348,.F.);
#6255=ORIENTED_EDGE('',*,*,#4351,.F.);
#6256=ORIENTED_EDGE('',*,*,#4354,.F.);
#6257=ORIENTED_EDGE('',*,*,#4357,.F.);
#6258=ORIENTED_EDGE('',*,*,#4360,.F.);
#6259=ORIENTED_EDGE('',*,*,#4363,.F.);
#6260=ORIENTED_EDGE('',*,*,#4366,.F.);
#6261=ORIENTED_EDGE('',*,*,#4369,.F.);
#6262=ORIENTED_EDGE('',*,*,#4372,.F.);
#6263=ORIENTED_EDGE('',*,*,#4375,.F.);
#6264=ORIENTED_EDGE('',*,*,#4378,.F.);
#6265=ORIENTED_EDGE('',*,*,#4381,.F.);
#6266=ORIENTED_EDGE('',*,*,#4384,.F.);
#6267=ORIENTED_EDGE('',*,*,#4387,.F.);
#6268=ORIENTED_EDGE('',*,*,#4390,.F.);
#6269=ORIENTED_EDGE('',*,*,#4393,.F.);
#6270=ORIENTED_EDGE('',*,*,#4396,.F.);
#6271=ORIENTED_EDGE('',*,*,#4399,.F.);
#6272=ORIENTED_EDGE('',*,*,#4402,.F.);
#6273=ORIENTED_EDGE('',*,*,#4410,.F.);
#6274=ORIENTED_EDGE('',*,*,#4411,.F.);
#6275=ORIENTED_EDGE('',*,*,#4223,.F.);
#6276=ORIENTED_EDGE('',*,*,#4227,.F.);
#6277=ORIENTED_EDGE('',*,*,#4230,.F.);
#6278=ORIENTED_EDGE('',*,*,#4233,.F.);
#6279=ORIENTED_EDGE('',*,*,#4236,.F.);
#6280=ORIENTED_EDGE('',*,*,#4239,.F.);
#6281=ORIENTED_EDGE('',*,*,#4242,.F.);
#6282=ORIENTED_EDGE('',*,*,#4245,.F.);
#6283=ORIENTED_EDGE('',*,*,#4248,.F.);
#6284=ORIENTED_EDGE('',*,*,#4251,.F.);
#6285=ORIENTED_EDGE('',*,*,#4254,.F.);
#6286=ORIENTED_EDGE('',*,*,#4257,.F.);
#6287=ORIENTED_EDGE('',*,*,#4260,.F.);
#6288=ORIENTED_EDGE('',*,*,#4263,.F.);
#6289=ORIENTED_EDGE('',*,*,#4266,.F.);
#6290=ORIENTED_EDGE('',*,*,#4269,.F.);
#6291=ORIENTED_EDGE('',*,*,#4272,.F.);
#6292=ORIENTED_EDGE('',*,*,#4275,.F.);
#6293=ORIENTED_EDGE('',*,*,#4278,.F.);
#6294=ORIENTED_EDGE('',*,*,#4281,.F.);
#6295=ORIENTED_EDGE('',*,*,#4284,.F.);
#6296=ORIENTED_EDGE('',*,*,#4287,.F.);
#6297=ORIENTED_EDGE('',*,*,#4290,.F.);
#6298=ORIENTED_EDGE('',*,*,#4293,.F.);
#6299=ORIENTED_EDGE('',*,*,#4296,.F.);
#6300=ORIENTED_EDGE('',*,*,#4299,.F.);
#6301=ORIENTED_EDGE('',*,*,#4302,.F.);
#6302=ORIENTED_EDGE('',*,*,#4305,.F.);
#6303=ORIENTED_EDGE('',*,*,#4308,.F.);
#6304=ORIENTED_EDGE('',*,*,#4311,.F.);
#6305=ORIENTED_EDGE('',*,*,#4412,.F.);
#6306=ORIENTED_EDGE('',*,*,#4401,.T.);
#6307=ORIENTED_EDGE('',*,*,#4413,.F.);
#6308=ORIENTED_EDGE('',*,*,#4414,.F.);
#6309=ORIENTED_EDGE('',*,*,#4410,.T.);
#6310=ORIENTED_EDGE('',*,*,#4404,.T.);
#6311=ORIENTED_EDGE('',*,*,#4407,.T.);
#6312=ORIENTED_EDGE('',*,*,#4415,.F.);
#6313=ORIENTED_EDGE('',*,*,#4312,.F.);
#6314=ORIENTED_EDGE('',*,*,#4309,.F.);
#6315=ORIENTED_EDGE('',*,*,#4306,.F.);
#6316=ORIENTED_EDGE('',*,*,#4303,.F.);
#6317=ORIENTED_EDGE('',*,*,#4300,.F.);
#6318=ORIENTED_EDGE('',*,*,#4297,.F.);
#6319=ORIENTED_EDGE('',*,*,#4294,.F.);
#6320=ORIENTED_EDGE('',*,*,#4291,.F.);
#6321=ORIENTED_EDGE('',*,*,#4288,.F.);
#6322=ORIENTED_EDGE('',*,*,#4285,.F.);
#6323=ORIENTED_EDGE('',*,*,#4282,.F.);
#6324=ORIENTED_EDGE('',*,*,#4279,.F.);
#6325=ORIENTED_EDGE('',*,*,#4276,.F.);
#6326=ORIENTED_EDGE('',*,*,#4273,.F.);
#6327=ORIENTED_EDGE('',*,*,#4270,.F.);
#6328=ORIENTED_EDGE('',*,*,#4267,.F.);
#6329=ORIENTED_EDGE('',*,*,#4264,.F.);
#6330=ORIENTED_EDGE('',*,*,#4261,.F.);
#6331=ORIENTED_EDGE('',*,*,#4258,.F.);
#6332=ORIENTED_EDGE('',*,*,#4255,.F.);
#6333=ORIENTED_EDGE('',*,*,#4252,.F.);
#6334=ORIENTED_EDGE('',*,*,#4249,.F.);
#6335=ORIENTED_EDGE('',*,*,#4246,.F.);
#6336=ORIENTED_EDGE('',*,*,#4243,.F.);
#6337=ORIENTED_EDGE('',*,*,#4240,.F.);
#6338=ORIENTED_EDGE('',*,*,#4237,.F.);
#6339=ORIENTED_EDGE('',*,*,#4234,.F.);
#6340=ORIENTED_EDGE('',*,*,#4231,.F.);
#6341=ORIENTED_EDGE('',*,*,#4228,.F.);
#6342=ORIENTED_EDGE('',*,*,#4225,.F.);
#6343=ORIENTED_EDGE('',*,*,#4416,.F.);
#6344=ORIENTED_EDGE('',*,*,#4413,.T.);
#6345=ORIENTED_EDGE('',*,*,#4403,.T.);
#6346=ORIENTED_EDGE('',*,*,#4400,.T.);
#6347=ORIENTED_EDGE('',*,*,#4397,.T.);
#6348=ORIENTED_EDGE('',*,*,#4394,.T.);
#6349=ORIENTED_EDGE('',*,*,#4391,.T.);
#6350=ORIENTED_EDGE('',*,*,#4388,.T.);
#6351=ORIENTED_EDGE('',*,*,#4385,.T.);
#6352=ORIENTED_EDGE('',*,*,#4382,.T.);
#6353=ORIENTED_EDGE('',*,*,#4379,.T.);
#6354=ORIENTED_EDGE('',*,*,#4376,.T.);
#6355=ORIENTED_EDGE('',*,*,#4373,.T.);
#6356=ORIENTED_EDGE('',*,*,#4370,.T.);
#6357=ORIENTED_EDGE('',*,*,#4367,.T.);
#6358=ORIENTED_EDGE('',*,*,#4364,.T.);
#6359=ORIENTED_EDGE('',*,*,#4361,.T.);
#6360=ORIENTED_EDGE('',*,*,#4358,.T.);
#6361=ORIENTED_EDGE('',*,*,#4355,.T.);
#6362=ORIENTED_EDGE('',*,*,#4352,.T.);
#6363=ORIENTED_EDGE('',*,*,#4349,.T.);
#6364=ORIENTED_EDGE('',*,*,#4346,.T.);
#6365=ORIENTED_EDGE('',*,*,#4343,.T.);
#6366=ORIENTED_EDGE('',*,*,#4340,.T.);
#6367=ORIENTED_EDGE('',*,*,#4337,.T.);
#6368=ORIENTED_EDGE('',*,*,#4334,.T.);
#6369=ORIENTED_EDGE('',*,*,#4331,.T.);
#6370=ORIENTED_EDGE('',*,*,#4328,.T.);
#6371=ORIENTED_EDGE('',*,*,#4325,.T.);
#6372=ORIENTED_EDGE('',*,*,#4322,.T.);
#6373=ORIENTED_EDGE('',*,*,#4319,.T.);
#6374=ORIENTED_EDGE('',*,*,#4316,.T.);
#6375=ORIENTED_EDGE('',*,*,#4310,.T.);
#6376=ORIENTED_EDGE('',*,*,#4415,.T.);
#6377=ORIENTED_EDGE('',*,*,#4406,.T.);
#6378=ORIENTED_EDGE('',*,*,#4412,.T.);
#6379=ORIENTED_EDGE('',*,*,#4417,.F.);
#6380=ORIENTED_EDGE('',*,*,#4418,.T.);
#6381=ORIENTED_EDGE('',*,*,#4419,.T.);
#6382=ORIENTED_EDGE('',*,*,#4420,.F.);
#6383=ORIENTED_EDGE('',*,*,#4421,.F.);
#6384=ORIENTED_EDGE('',*,*,#4422,.T.);
#6385=ORIENTED_EDGE('',*,*,#4423,.T.);
#6386=ORIENTED_EDGE('',*,*,#4418,.F.);
#6387=ORIENTED_EDGE('',*,*,#4424,.F.);
#6388=ORIENTED_EDGE('',*,*,#4425,.T.);
#6389=ORIENTED_EDGE('',*,*,#4426,.T.);
#6390=ORIENTED_EDGE('',*,*,#4422,.F.);
#6391=ORIENTED_EDGE('',*,*,#4427,.F.);
#6392=ORIENTED_EDGE('',*,*,#4428,.T.);
#6393=ORIENTED_EDGE('',*,*,#4429,.T.);
#6394=ORIENTED_EDGE('',*,*,#4425,.F.);
#6395=ORIENTED_EDGE('',*,*,#4430,.F.);
#6396=ORIENTED_EDGE('',*,*,#4431,.T.);
#6397=ORIENTED_EDGE('',*,*,#4432,.T.);
#6398=ORIENTED_EDGE('',*,*,#4428,.F.);
#6399=ORIENTED_EDGE('',*,*,#4433,.F.);
#6400=ORIENTED_EDGE('',*,*,#4420,.T.);
#6401=ORIENTED_EDGE('',*,*,#4434,.T.);
#6402=ORIENTED_EDGE('',*,*,#4431,.F.);
#6403=ORIENTED_EDGE('',*,*,#4434,.F.);
#6404=ORIENTED_EDGE('',*,*,#4419,.F.);
#6405=ORIENTED_EDGE('',*,*,#4423,.F.);
#6406=ORIENTED_EDGE('',*,*,#4426,.F.);
#6407=ORIENTED_EDGE('',*,*,#4429,.F.);
#6408=ORIENTED_EDGE('',*,*,#4432,.F.);
#6409=ORIENTED_EDGE('',*,*,#4435,.T.);
#6410=ORIENTED_EDGE('',*,*,#4411,.T.);
#6411=ORIENTED_EDGE('',*,*,#4414,.T.);
#6412=ORIENTED_EDGE('',*,*,#4416,.T.);
#6413=ORIENTED_EDGE('',*,*,#4224,.F.);
#6414=ORIENTED_EDGE('',*,*,#4435,.F.);
#6415=ORIENTED_EDGE('',*,*,#4436,.T.);
#6416=ORIENTED_EDGE('',*,*,#4437,.T.);
#6417=ORIENTED_EDGE('',*,*,#4436,.F.);
#6418=ORIENTED_EDGE('',*,*,#4437,.F.);
#6419=ORIENTED_EDGE('',*,*,#4417,.T.);
#6420=ORIENTED_EDGE('',*,*,#4433,.T.);
#6421=ORIENTED_EDGE('',*,*,#4430,.T.);
#6422=ORIENTED_EDGE('',*,*,#4427,.T.);
#6423=ORIENTED_EDGE('',*,*,#4424,.T.);
#6424=ORIENTED_EDGE('',*,*,#4421,.T.);
#6425=ORIENTED_EDGE('',*,*,#4409,.T.);
#6623=CYLINDRICAL_SURFACE('',#7637,0.14635);
#6624=CYLINDRICAL_SURFACE('',#7639,0.14635);
#6625=CYLINDRICAL_SURFACE('',#7640,0.14635);
#6626=CYLINDRICAL_SURFACE('',#7641,0.14635);
#6627=CYLINDRICAL_SURFACE('',#7642,0.14635);
#6628=CYLINDRICAL_SURFACE('',#7643,0.14635);
#6629=CYLINDRICAL_SURFACE('',#7644,0.14635);
#6630=CYLINDRICAL_SURFACE('',#7645,0.14635);
#6631=CYLINDRICAL_SURFACE('',#7646,0.14635);
#6632=CYLINDRICAL_SURFACE('',#7647,0.14635);
#6633=CYLINDRICAL_SURFACE('',#7648,0.14635);
#6634=CYLINDRICAL_SURFACE('',#7649,0.14635);
#6635=CYLINDRICAL_SURFACE('',#7650,0.14635);
#6636=CYLINDRICAL_SURFACE('',#7651,0.14635);
#6637=CYLINDRICAL_SURFACE('',#7652,0.14635);
#6638=CYLINDRICAL_SURFACE('',#7653,0.14635);
#6639=CYLINDRICAL_SURFACE('',#7654,0.14635);
#6640=CYLINDRICAL_SURFACE('',#7655,0.14635);
#6641=CYLINDRICAL_SURFACE('',#7656,0.14635);
#6642=CYLINDRICAL_SURFACE('',#7657,0.14635);
#6643=CYLINDRICAL_SURFACE('',#7658,0.14635);
#6644=CYLINDRICAL_SURFACE('',#7659,0.14635);
#6645=CYLINDRICAL_SURFACE('',#7660,0.14635);
#6646=CYLINDRICAL_SURFACE('',#7661,0.14635);
#6647=CYLINDRICAL_SURFACE('',#7662,0.14635);
#6648=CYLINDRICAL_SURFACE('',#7663,0.14635);
#6649=CYLINDRICAL_SURFACE('',#7664,0.14635);
#6650=CYLINDRICAL_SURFACE('',#7665,0.14635);
#6651=CYLINDRICAL_SURFACE('',#7666,0.14635);
#6652=CYLINDRICAL_SURFACE('',#7667,0.14635);
#6653=CYLINDRICAL_SURFACE('',#7668,0.117775);
#6654=CYLINDRICAL_SURFACE('',#7670,0.117775);
#6655=CYLINDRICAL_SURFACE('',#7671,0.117775);
#6656=CYLINDRICAL_SURFACE('',#7672,0.117775);
#6657=CYLINDRICAL_SURFACE('',#7673,0.117775);
#6658=CYLINDRICAL_SURFACE('',#7674,0.117775);
#6659=CYLINDRICAL_SURFACE('',#7675,0.117775);
#6660=CYLINDRICAL_SURFACE('',#7676,0.117775);
#6661=CYLINDRICAL_SURFACE('',#7677,0.117775);
#6662=CYLINDRICAL_SURFACE('',#7678,0.117775);
#6663=CYLINDRICAL_SURFACE('',#7679,0.117775);
#6664=CYLINDRICAL_SURFACE('',#7680,0.117775);
#6665=CYLINDRICAL_SURFACE('',#7681,0.117775);
#6666=CYLINDRICAL_SURFACE('',#7682,0.117775);
#6667=CYLINDRICAL_SURFACE('',#7683,0.117775);
#6668=CYLINDRICAL_SURFACE('',#7684,0.117775);
#6669=CYLINDRICAL_SURFACE('',#7685,0.117775);
#6670=CYLINDRICAL_SURFACE('',#7686,0.117775);
#6671=CYLINDRICAL_SURFACE('',#7687,0.117775);
#6672=CYLINDRICAL_SURFACE('',#7688,0.117775);
#6673=CYLINDRICAL_SURFACE('',#7689,0.117775);
#6674=CYLINDRICAL_SURFACE('',#7690,0.117775);
#6675=CYLINDRICAL_SURFACE('',#7691,0.117775);
#6676=CYLINDRICAL_SURFACE('',#7692,0.117775);
#6677=CYLINDRICAL_SURFACE('',#7693,0.117775);
#6678=CYLINDRICAL_SURFACE('',#7694,0.117775);
#6679=CYLINDRICAL_SURFACE('',#7695,0.117775);
#6680=CYLINDRICAL_SURFACE('',#7696,0.117775);
#6681=CYLINDRICAL_SURFACE('',#7697,0.117775);
#6682=CYLINDRICAL_SURFACE('',#7698,0.117775);
#6683=CYLINDRICAL_SURFACE('',#7702,0.117775);
#6684=CYLINDRICAL_SURFACE('',#7704,0.14635);
#6685=CYLINDRICAL_SURFACE('',#7714,0.275);
#7001=ADVANCED_FACE('',(#1122),#6623,.T.);
#7002=ADVANCED_FACE('',(#1123),#6624,.T.);
#7003=ADVANCED_FACE('',(#1124),#6625,.T.);
#7004=ADVANCED_FACE('',(#1125),#6626,.T.);
#7005=ADVANCED_FACE('',(#1126),#6627,.T.);
#7006=ADVANCED_FACE('',(#1127),#6628,.T.);
#7007=ADVANCED_FACE('',(#1128),#6629,.T.);
#7008=ADVANCED_FACE('',(#1129),#6630,.T.);
#7009=ADVANCED_FACE('',(#1130),#6631,.T.);
#7010=ADVANCED_FACE('',(#1131),#6632,.T.);
#7011=ADVANCED_FACE('',(#1132),#6633,.T.);
#7012=ADVANCED_FACE('',(#1133),#6634,.T.);
#7013=ADVANCED_FACE('',(#1134),#6635,.T.);
#7014=ADVANCED_FACE('',(#1135),#6636,.T.);
#7015=ADVANCED_FACE('',(#1136),#6637,.T.);
#7016=ADVANCED_FACE('',(#1137),#6638,.T.);
#7017=ADVANCED_FACE('',(#1138),#6639,.T.);
#7018=ADVANCED_FACE('',(#1139),#6640,.T.);
#7019=ADVANCED_FACE('',(#1140),#6641,.T.);
#7020=ADVANCED_FACE('',(#1141),#6642,.T.);
#7021=ADVANCED_FACE('',(#1142),#6643,.T.);
#7022=ADVANCED_FACE('',(#1143),#6644,.T.);
#7023=ADVANCED_FACE('',(#1144),#6645,.T.);
#7024=ADVANCED_FACE('',(#1145),#6646,.T.);
#7025=ADVANCED_FACE('',(#1146),#6647,.T.);
#7026=ADVANCED_FACE('',(#1147),#6648,.T.);
#7027=ADVANCED_FACE('',(#1148),#6649,.T.);
#7028=ADVANCED_FACE('',(#1149),#6650,.T.);
#7029=ADVANCED_FACE('',(#1150),#6651,.T.);
#7030=ADVANCED_FACE('',(#1151),#6652,.T.);
#7031=ADVANCED_FACE('',(#1152),#6653,.T.);
#7032=ADVANCED_FACE('',(#1153),#6654,.T.);
#7033=ADVANCED_FACE('',(#1154),#6655,.T.);
#7034=ADVANCED_FACE('',(#1155),#6656,.T.);
#7035=ADVANCED_FACE('',(#1156),#6657,.T.);
#7036=ADVANCED_FACE('',(#1157),#6658,.T.);
#7037=ADVANCED_FACE('',(#1158),#6659,.T.);
#7038=ADVANCED_FACE('',(#1159),#6660,.T.);
#7039=ADVANCED_FACE('',(#1160),#6661,.T.);
#7040=ADVANCED_FACE('',(#1161),#6662,.T.);
#7041=ADVANCED_FACE('',(#1162),#6663,.T.);
#7042=ADVANCED_FACE('',(#1163),#6664,.T.);
#7043=ADVANCED_FACE('',(#1164),#6665,.T.);
#7044=ADVANCED_FACE('',(#1165),#6666,.T.);
#7045=ADVANCED_FACE('',(#1166),#6667,.T.);
#7046=ADVANCED_FACE('',(#1167),#6668,.T.);
#7047=ADVANCED_FACE('',(#1168),#6669,.T.);
#7048=ADVANCED_FACE('',(#1169),#6670,.T.);
#7049=ADVANCED_FACE('',(#1170),#6671,.T.);
#7050=ADVANCED_FACE('',(#1171),#6672,.T.);
#7051=ADVANCED_FACE('',(#1172),#6673,.T.);
#7052=ADVANCED_FACE('',(#1173),#6674,.T.);
#7053=ADVANCED_FACE('',(#1174),#6675,.T.);
#7054=ADVANCED_FACE('',(#1175),#6676,.T.);
#7055=ADVANCED_FACE('',(#1176),#6677,.T.);
#7056=ADVANCED_FACE('',(#1177),#6678,.T.);
#7057=ADVANCED_FACE('',(#1178),#6679,.T.);
#7058=ADVANCED_FACE('',(#1179),#6680,.T.);
#7059=ADVANCED_FACE('',(#1180),#6681,.T.);
#7060=ADVANCED_FACE('',(#1181),#6682,.T.);
#7061=ADVANCED_FACE('',(#1182),#661,.T.);
#7062=ADVANCED_FACE('',(#1183),#167,.F.);
#7063=ADVANCED_FACE('',(#1184),#6683,.T.);
#7064=ADVANCED_FACE('',(#1185),#168,.F.);
#7065=ADVANCED_FACE('',(#1186),#6684,.T.);
#7066=ADVANCED_FACE('',(#1187),#801,.F.);
#7067=ADVANCED_FACE('',(#1188),#802,.F.);
#7068=ADVANCED_FACE('',(#1189),#803,.F.);
#7069=ADVANCED_FACE('',(#1190),#804,.F.);
#7070=ADVANCED_FACE('',(#1191),#805,.F.);
#7071=ADVANCED_FACE('',(#1192),#806,.F.);
#7072=ADVANCED_FACE('',(#1193),#807,.F.);
#7073=ADVANCED_FACE('',(#1194,#654),#808,.T.);
#7074=ADVANCED_FACE('',(#1195),#6685,.T.);
#7075=ADVANCED_FACE('',(#1196,#655),#809,.F.);
#7076=ADVANCED_FACE('',(#1197),#810,.T.);
#7110=CLOSED_SHELL('',(#7001,#7002,#7003,#7004,#7005,#7006,#7007,#7008,
#7009,#7010,#7011,#7012,#7013,#7014,#7015,#7016,#7017,#7018,#7019,#7020,
#7021,#7022,#7023,#7024,#7025,#7026,#7027,#7028,#7029,#7030,#7031,#7032,
#7033,#7034,#7035,#7036,#7037,#7038,#7039,#7040,#7041,#7042,#7043,#7044,
#7045,#7046,#7047,#7048,#7049,#7050,#7051,#7052,#7053,#7054,#7055,#7056,
#7057,#7058,#7059,#7060,#7061,#7062,#7063,#7064,#7065,#7066,#7067,#7068,
#7069,#7070,#7071,#7072,#7073,#7074,#7075,#7076));
#7636=AXIS2_PLACEMENT_3D('',#14484,#8942,#8943);
#7637=AXIS2_PLACEMENT_3D('',#14485,#8944,#8945);
#7638=AXIS2_PLACEMENT_3D('',#14501,#8947,#8948);
#7639=AXIS2_PLACEMENT_3D('',#14509,#8949,#8950);
#7640=AXIS2_PLACEMENT_3D('',#14557,#8952,#8953);
#7641=AXIS2_PLACEMENT_3D('',#14605,#8955,#8956);
#7642=AXIS2_PLACEMENT_3D('',#14656,#8958,#8959);
#7643=AXIS2_PLACEMENT_3D('',#14704,#8961,#8962);
#7644=AXIS2_PLACEMENT_3D('',#14752,#8964,#8965);
#7645=AXIS2_PLACEMENT_3D('',#14800,#8967,#8968);
#7646=AXIS2_PLACEMENT_3D('',#14854,#8970,#8971);
#7647=AXIS2_PLACEMENT_3D('',#14902,#8973,#8974);
#7648=AXIS2_PLACEMENT_3D('',#14950,#8976,#8977);
#7649=AXIS2_PLACEMENT_3D('',#15004,#8979,#8980);
#7650=AXIS2_PLACEMENT_3D('',#15052,#8982,#8983);
#7651=AXIS2_PLACEMENT_3D('',#15100,#8985,#8986);
#7652=AXIS2_PLACEMENT_3D('',#15148,#8988,#8989);
#7653=AXIS2_PLACEMENT_3D('',#15202,#8991,#8992);
#7654=AXIS2_PLACEMENT_3D('',#15250,#8994,#8995);
#7655=AXIS2_PLACEMENT_3D('',#15298,#8997,#8998);
#7656=AXIS2_PLACEMENT_3D('',#15352,#9000,#9001);
#7657=AXIS2_PLACEMENT_3D('',#15400,#9003,#9004);
#7658=AXIS2_PLACEMENT_3D('',#15448,#9006,#9007);
#7659=AXIS2_PLACEMENT_3D('',#15502,#9009,#9010);
#7660=AXIS2_PLACEMENT_3D('',#15550,#9012,#9013);
#7661=AXIS2_PLACEMENT_3D('',#15598,#9015,#9016);
#7662=AXIS2_PLACEMENT_3D('',#15646,#9018,#9019);
#7663=AXIS2_PLACEMENT_3D('',#15700,#9021,#9022);
#7664=AXIS2_PLACEMENT_3D('',#15748,#9024,#9025);
#7665=AXIS2_PLACEMENT_3D('',#15796,#9027,#9028);
#7666=AXIS2_PLACEMENT_3D('',#15850,#9030,#9031);
#7667=AXIS2_PLACEMENT_3D('',#15898,#9033,#9034);
#7668=AXIS2_PLACEMENT_3D('',#15946,#9036,#9037);
#7669=AXIS2_PLACEMENT_3D('',#15962,#9039,#9040);
#7670=AXIS2_PLACEMENT_3D('',#15972,#9041,#9042);
#7671=AXIS2_PLACEMENT_3D('',#15996,#9044,#9045);
#7672=AXIS2_PLACEMENT_3D('',#16020,#9047,#9048);
#7673=AXIS2_PLACEMENT_3D('',#16045,#9050,#9051);
#7674=AXIS2_PLACEMENT_3D('',#16070,#9053,#9054);
#7675=AXIS2_PLACEMENT_3D('',#16094,#9056,#9057);
#7676=AXIS2_PLACEMENT_3D('',#16119,#9059,#9060);
#7677=AXIS2_PLACEMENT_3D('',#16144,#9062,#9063);
#7678=AXIS2_PLACEMENT_3D('',#16168,#9065,#9066);
#7679=AXIS2_PLACEMENT_3D('',#16192,#9068,#9069);
#7680=AXIS2_PLACEMENT_3D('',#16217,#9071,#9072);
#7681=AXIS2_PLACEMENT_3D('',#16242,#9074,#9075);
#7682=AXIS2_PLACEMENT_3D('',#16266,#9077,#9078);
#7683=AXIS2_PLACEMENT_3D('',#16291,#9080,#9081);
#7684=AXIS2_PLACEMENT_3D('',#16316,#9083,#9084);
#7685=AXIS2_PLACEMENT_3D('',#16340,#9086,#9087);
#7686=AXIS2_PLACEMENT_3D('',#16365,#9089,#9090);
#7687=AXIS2_PLACEMENT_3D('',#16390,#9092,#9093);
#7688=AXIS2_PLACEMENT_3D('',#16414,#9095,#9096);
#7689=AXIS2_PLACEMENT_3D('',#16438,#9098,#9099);
#7690=AXIS2_PLACEMENT_3D('',#16463,#9101,#9102);
#7691=AXIS2_PLACEMENT_3D('',#16488,#9104,#9105);
#7692=AXIS2_PLACEMENT_3D('',#16512,#9107,#9108);
#7693=AXIS2_PLACEMENT_3D('',#16537,#9110,#9111);
#7694=AXIS2_PLACEMENT_3D('',#16562,#9113,#9114);
#7695=AXIS2_PLACEMENT_3D('',#16586,#9116,#9117);
#7696=AXIS2_PLACEMENT_3D('',#16611,#9119,#9120);
#7697=AXIS2_PLACEMENT_3D('',#16635,#9122,#9123);
#7698=AXIS2_PLACEMENT_3D('',#16660,#9125,#9126);
#7699=AXIS2_PLACEMENT_3D('',#16684,#9128,#9129);
#7700=AXIS2_PLACEMENT_3D('',#16846,#9130,#9131);
#7701=AXIS2_PLACEMENT_3D('',#16865,#9133,#9134);
#7702=AXIS2_PLACEMENT_3D('',#17727,#9135,#9136);
#7703=AXIS2_PLACEMENT_3D('',#17738,#9137,#9138);
#7704=AXIS2_PLACEMENT_3D('',#18605,#9139,#9140);
#7705=AXIS2_PLACEMENT_3D('',#18606,#9141,#9142);
#7706=AXIS2_PLACEMENT_3D('',#18615,#9147,#9148);
#7707=AXIS2_PLACEMENT_3D('',#18621,#9152,#9153);
#7708=AXIS2_PLACEMENT_3D('',#18627,#9157,#9158);
#7709=AXIS2_PLACEMENT_3D('',#18633,#9162,#9163);
#7710=AXIS2_PLACEMENT_3D('',#18639,#9167,#9168);
#7711=AXIS2_PLACEMENT_3D('',#18642,#9171,#9172);
#7712=AXIS2_PLACEMENT_3D('',#18643,#9173,#9174);
#7713=AXIS2_PLACEMENT_3D('',#18645,#9175,#9176);
#7714=AXIS2_PLACEMENT_3D('',#18646,#9177,#9178);
#7715=AXIS2_PLACEMENT_3D('',#18649,#9180,#9181);
#7716=AXIS2_PLACEMENT_3D('',#18650,#9182,#9183);
#7717=AXIS2_PLACEMENT_3D('',#18651,#9184,#9185);
#8942=DIRECTION('axis',(0.,0.,1.));
#8943=DIRECTION('refdir',(1.,0.,0.));
#8944=DIRECTION('center_axis',(0.,0.,1.));
#8945=DIRECTION('ref_axis',(1.,0.,0.));
#8946=DIRECTION('',(0.,0.,-1.));
#8947=DIRECTION('center_axis',(0.,0.,-1.));
#8948=DIRECTION('ref_axis',(1.,0.,0.));
#8949=DIRECTION('center_axis',(0.,0.,1.));
#8950=DIRECTION('ref_axis',(1.,0.,0.));
#8951=DIRECTION('',(0.,0.,-1.));
#8952=DIRECTION('center_axis',(0.,0.,1.));
#8953=DIRECTION('ref_axis',(1.,0.,0.));
#8954=DIRECTION('',(0.,0.,-1.));
#8955=DIRECTION('center_axis',(0.,0.,1.));
#8956=DIRECTION('ref_axis',(1.,0.,0.));
#8957=DIRECTION('',(0.,0.,-1.));
#8958=DIRECTION('center_axis',(0.,0.,1.));
#8959=DIRECTION('ref_axis',(1.,0.,0.));
#8960=DIRECTION('',(0.,0.,-1.));
#8961=DIRECTION('center_axis',(0.,0.,1.));
#8962=DIRECTION('ref_axis',(1.,0.,0.));
#8963=DIRECTION('',(0.,0.,-1.));
#8964=DIRECTION('center_axis',(0.,0.,1.));
#8965=DIRECTION('ref_axis',(1.,0.,0.));
#8966=DIRECTION('',(0.,0.,-1.));
#8967=DIRECTION('center_axis',(0.,0.,1.));
#8968=DIRECTION('ref_axis',(1.,0.,0.));
#8969=DIRECTION('',(0.,0.,-1.));
#8970=DIRECTION('center_axis',(0.,0.,1.));
#8971=DIRECTION('ref_axis',(1.,0.,0.));
#8972=DIRECTION('',(0.,0.,-1.));
#8973=DIRECTION('center_axis',(0.,0.,1.));
#8974=DIRECTION('ref_axis',(1.,0.,0.));
#8975=DIRECTION('',(0.,0.,-1.));
#8976=DIRECTION('center_axis',(0.,0.,1.));
#8977=DIRECTION('ref_axis',(1.,0.,0.));
#8978=DIRECTION('',(0.,0.,-1.));
#8979=DIRECTION('center_axis',(0.,0.,1.));
#8980=DIRECTION('ref_axis',(1.,0.,0.));
#8981=DIRECTION('',(0.,0.,-1.));
#8982=DIRECTION('center_axis',(0.,0.,1.));
#8983=DIRECTION('ref_axis',(1.,0.,0.));
#8984=DIRECTION('',(0.,0.,-1.));
#8985=DIRECTION('center_axis',(0.,0.,1.));
#8986=DIRECTION('ref_axis',(1.,0.,0.));
#8987=DIRECTION('',(0.,0.,-1.));
#8988=DIRECTION('center_axis',(0.,0.,1.));
#8989=DIRECTION('ref_axis',(1.,0.,0.));
#8990=DIRECTION('',(0.,0.,-1.));
#8991=DIRECTION('center_axis',(0.,0.,1.));
#8992=DIRECTION('ref_axis',(1.,0.,0.));
#8993=DIRECTION('',(0.,0.,-1.));
#8994=DIRECTION('center_axis',(0.,0.,1.));
#8995=DIRECTION('ref_axis',(1.,0.,0.));
#8996=DIRECTION('',(0.,0.,-1.));
#8997=DIRECTION('center_axis',(0.,0.,1.));
#8998=DIRECTION('ref_axis',(1.,0.,0.));
#8999=DIRECTION('',(0.,0.,-1.));
#9000=DIRECTION('center_axis',(0.,0.,1.));
#9001=DIRECTION('ref_axis',(1.,0.,0.));
#9002=DIRECTION('',(0.,0.,-1.));
#9003=DIRECTION('center_axis',(0.,0.,1.));
#9004=DIRECTION('ref_axis',(1.,0.,0.));
#9005=DIRECTION('',(0.,0.,-1.));
#9006=DIRECTION('center_axis',(0.,0.,1.));
#9007=DIRECTION('ref_axis',(1.,0.,0.));
#9008=DIRECTION('',(0.,0.,-1.));
#9009=DIRECTION('center_axis',(0.,0.,1.));
#9010=DIRECTION('ref_axis',(1.,0.,0.));
#9011=DIRECTION('',(0.,0.,-1.));
#9012=DIRECTION('center_axis',(0.,0.,1.));
#9013=DIRECTION('ref_axis',(1.,0.,0.));
#9014=DIRECTION('',(0.,0.,-1.));
#9015=DIRECTION('center_axis',(0.,0.,1.));
#9016=DIRECTION('ref_axis',(1.,0.,0.));
#9017=DIRECTION('',(0.,0.,-1.));
#9018=DIRECTION('center_axis',(0.,0.,1.));
#9019=DIRECTION('ref_axis',(1.,0.,0.));
#9020=DIRECTION('',(0.,0.,-1.));
#9021=DIRECTION('center_axis',(0.,0.,1.));
#9022=DIRECTION('ref_axis',(1.,0.,0.));
#9023=DIRECTION('',(0.,0.,-1.));
#9024=DIRECTION('center_axis',(0.,0.,1.));
#9025=DIRECTION('ref_axis',(1.,0.,0.));
#9026=DIRECTION('',(0.,0.,-1.));
#9027=DIRECTION('center_axis',(0.,0.,1.));
#9028=DIRECTION('ref_axis',(1.,0.,0.));
#9029=DIRECTION('',(0.,0.,-1.));
#9030=DIRECTION('center_axis',(0.,0.,1.));
#9031=DIRECTION('ref_axis',(1.,0.,0.));
#9032=DIRECTION('',(0.,0.,-1.));
#9033=DIRECTION('center_axis',(0.,0.,1.));
#9034=DIRECTION('ref_axis',(1.,0.,0.));
#9035=DIRECTION('',(0.,0.,-1.));
#9036=DIRECTION('center_axis',(0.,0.,1.));
#9037=DIRECTION('ref_axis',(1.,-2.42503376499884E-13,0.));
#9038=DIRECTION('',(0.,0.,1.));
#9039=DIRECTION('center_axis',(0.,0.,-1.));
#9040=DIRECTION('ref_axis',(1.,-2.42503376499884E-13,0.));
#9041=DIRECTION('center_axis',(0.,0.,1.));
#9042=DIRECTION('ref_axis',(1.,-2.42503376499884E-13,0.));
#9043=DIRECTION('',(0.,0.,1.));
#9044=DIRECTION('center_axis',(0.,0.,1.));
#9045=DIRECTION('ref_axis',(1.,-2.42503376499884E-13,0.));
#9046=DIRECTION('',(0.,0.,1.));
#9047=DIRECTION('center_axis',(0.,0.,1.));
#9048=DIRECTION('ref_axis',(1.,-2.42503376499884E-13,0.));
#9049=DIRECTION('',(0.,0.,1.));
#9050=DIRECTION('center_axis',(0.,0.,1.));
#9051=DIRECTION('ref_axis',(1.,-2.42503376499884E-13,0.));
#9052=DIRECTION('',(0.,0.,1.));
#9053=DIRECTION('center_axis',(0.,0.,1.));
#9054=DIRECTION('ref_axis',(1.,-2.42503376499884E-13,0.));
#9055=DIRECTION('',(0.,0.,1.));
#9056=DIRECTION('center_axis',(0.,0.,1.));
#9057=DIRECTION('ref_axis',(1.,-2.42503376499884E-13,0.));
#9058=DIRECTION('',(0.,0.,1.));
#9059=DIRECTION('center_axis',(0.,0.,1.));
#9060=DIRECTION('ref_axis',(1.,-2.42503376499884E-13,0.));
#9061=DIRECTION('',(0.,0.,1.));
#9062=DIRECTION('center_axis',(0.,0.,1.));
#9063=DIRECTION('ref_axis',(1.,-2.42503376499884E-13,0.));
#9064=DIRECTION('',(0.,0.,1.));
#9065=DIRECTION('center_axis',(0.,0.,1.));
#9066=DIRECTION('ref_axis',(1.,-2.42503376499884E-13,0.));
#9067=DIRECTION('',(0.,0.,1.));
#9068=DIRECTION('center_axis',(0.,0.,1.));
#9069=DIRECTION('ref_axis',(1.,-2.42503376499884E-13,0.));
#9070=DIRECTION('',(0.,0.,1.));
#9071=DIRECTION('center_axis',(0.,0.,1.));
#9072=DIRECTION('ref_axis',(1.,-2.42503376499884E-13,0.));
#9073=DIRECTION('',(0.,0.,1.));
#9074=DIRECTION('center_axis',(0.,0.,1.));
#9075=DIRECTION('ref_axis',(1.,-2.42503376499884E-13,0.));
#9076=DIRECTION('',(0.,0.,1.));
#9077=DIRECTION('center_axis',(0.,0.,1.));
#9078=DIRECTION('ref_axis',(1.,-2.42503376499884E-13,0.));
#9079=DIRECTION('',(0.,0.,1.));
#9080=DIRECTION('center_axis',(0.,0.,1.));
#9081=DIRECTION('ref_axis',(1.,-2.42503376499884E-13,0.));
#9082=DIRECTION('',(0.,0.,1.));
#9083=DIRECTION('center_axis',(0.,0.,1.));
#9084=DIRECTION('ref_axis',(1.,-2.42503376499884E-13,0.));
#9085=DIRECTION('',(0.,0.,1.));
#9086=DIRECTION('center_axis',(0.,0.,1.));
#9087=DIRECTION('ref_axis',(1.,-2.42503376499884E-13,0.));
#9088=DIRECTION('',(0.,0.,1.));
#9089=DIRECTION('center_axis',(0.,0.,1.));
#9090=DIRECTION('ref_axis',(1.,-2.42503376499884E-13,0.));
#9091=DIRECTION('',(0.,0.,1.));
#9092=DIRECTION('center_axis',(0.,0.,1.));
#9093=DIRECTION('ref_axis',(1.,-2.42503376499884E-13,0.));
#9094=DIRECTION('',(0.,0.,1.));
#9095=DIRECTION('center_axis',(0.,0.,1.));
#9096=DIRECTION('ref_axis',(1.,-2.42503376499884E-13,0.));
#9097=DIRECTION('',(0.,0.,1.));
#9098=DIRECTION('center_axis',(0.,0.,1.));
#9099=DIRECTION('ref_axis',(1.,-2.42503376499884E-13,0.));
#9100=DIRECTION('',(0.,0.,1.));
#9101=DIRECTION('center_axis',(0.,0.,1.));
#9102=DIRECTION('ref_axis',(1.,-2.42503376499884E-13,0.));
#9103=DIRECTION('',(0.,0.,1.));
#9104=DIRECTION('center_axis',(0.,0.,1.));
#9105=DIRECTION('ref_axis',(1.,-2.42503376499884E-13,0.));
#9106=DIRECTION('',(0.,0.,1.));
#9107=DIRECTION('center_axis',(0.,0.,1.));
#9108=DIRECTION('ref_axis',(1.,-2.42503376499884E-13,0.));
#9109=DIRECTION('',(0.,0.,1.));
#9110=DIRECTION('center_axis',(0.,0.,1.));
#9111=DIRECTION('ref_axis',(1.,-2.42503376499884E-13,0.));
#9112=DIRECTION('',(0.,0.,1.));
#9113=DIRECTION('center_axis',(0.,0.,1.));
#9114=DIRECTION('ref_axis',(1.,-2.42503376499884E-13,0.));
#9115=DIRECTION('',(0.,0.,1.));
#9116=DIRECTION('center_axis',(0.,0.,1.));
#9117=DIRECTION('ref_axis',(1.,-2.42503376499884E-13,0.));
#9118=DIRECTION('',(0.,0.,1.));
#9119=DIRECTION('center_axis',(0.,0.,1.));
#9120=DIRECTION('ref_axis',(1.,-2.42503376499884E-13,0.));
#9121=DIRECTION('',(0.,0.,1.));
#9122=DIRECTION('center_axis',(0.,0.,1.));
#9123=DIRECTION('ref_axis',(1.,-2.42503376499884E-13,0.));
#9124=DIRECTION('',(0.,0.,1.));
#9125=DIRECTION('center_axis',(0.,0.,1.));
#9126=DIRECTION('ref_axis',(1.,-2.42503376499884E-13,0.));
#9127=DIRECTION('',(0.,0.,1.));
#9128=DIRECTION('center_axis',(0.,0.,-1.));
#9129=DIRECTION('ref_axis',(1.,0.,0.));
#9130=DIRECTION('center_axis',(0.,0.,-1.));
#9131=DIRECTION('ref_axis',(1.,0.,0.));
#9132=DIRECTION('',(0.707106781186547,8.65956056235493E-17,0.707106781186548));
#9133=DIRECTION('center_axis',(0.,0.,1.));
#9134=DIRECTION('ref_axis',(1.,0.,0.));
#9135=DIRECTION('center_axis',(0.,0.,1.));
#9136=DIRECTION('ref_axis',(1.,-2.42503376499884E-13,0.));
#9137=DIRECTION('center_axis',(0.,0.,-1.));
#9138=DIRECTION('ref_axis',(1.,-2.42503376499884E-13,0.));
#9139=DIRECTION('center_axis',(0.,0.,1.));
#9140=DIRECTION('ref_axis',(1.,0.,0.));
#9141=DIRECTION('center_axis',(-1.92296268638356E-16,-1.,0.));
#9142=DIRECTION('ref_axis',(1.,-1.92296268638356E-16,0.));
#9143=DIRECTION('',(1.,-1.92296268638356E-16,0.));
#9144=DIRECTION('',(0.,0.,1.));
#9145=DIRECTION('',(1.,-1.92296268638356E-16,0.));
#9146=DIRECTION('',(0.,0.,1.));
#9147=DIRECTION('center_axis',(-0.866025403784439,-0.5,0.));
#9148=DIRECTION('ref_axis',(0.5,-0.866025403784439,0.));
#9149=DIRECTION('',(0.5,-0.866025403784439,0.));
#9150=DIRECTION('',(0.,0.,1.));
#9151=DIRECTION('',(0.5,-0.866025403784439,0.));
#9152=DIRECTION('center_axis',(-0.866025403784439,0.5,0.));
#9153=DIRECTION('ref_axis',(-0.5,-0.866025403784439,0.));
#9154=DIRECTION('',(-0.5,-0.866025403784439,0.));
#9155=DIRECTION('',(0.,0.,1.));
#9156=DIRECTION('',(-0.5,-0.866025403784438,0.));
#9157=DIRECTION('center_axis',(1.92296268638356E-16,1.,0.));
#9158=DIRECTION('ref_axis',(-1.,1.92296268638356E-16,0.));
#9159=DIRECTION('',(-1.,1.92296268638356E-16,0.));
#9160=DIRECTION('',(0.,0.,1.));
#9161=DIRECTION('',(-1.,1.92296268638356E-16,0.));
#9162=DIRECTION('center_axis',(0.866025403784439,0.5,0.));
#9163=DIRECTION('ref_axis',(-0.5,0.866025403784439,0.));
#9164=DIRECTION('',(-0.5,0.866025403784439,0.));
#9165=DIRECTION('',(0.,0.,1.));
#9166=DIRECTION('',(-0.5,0.866025403784439,0.));
#9167=DIRECTION('center_axis',(0.866025403784439,-0.5,0.));
#9168=DIRECTION('ref_axis',(0.5,0.866025403784439,0.));
#9169=DIRECTION('',(0.5,0.866025403784439,0.));
#9170=DIRECTION('',(0.5,0.866025403784439,0.));
#9171=DIRECTION('center_axis',(0.,0.,1.));
#9172=DIRECTION('ref_axis',(1.,0.,0.));
#9173=DIRECTION('center_axis',(0.,0.,1.));
#9174=DIRECTION('ref_axis',(1.,0.,0.));
#9175=DIRECTION('center_axis',(0.,0.,1.));
#9176=DIRECTION('ref_axis',(1.,0.,0.));
#9177=DIRECTION('center_axis',(0.,0.,1.));
#9178=DIRECTION('ref_axis',(1.,0.,0.));
#9179=DIRECTION('',(0.,0.,-1.));
#9180=DIRECTION('center_axis',(0.,0.,1.));
#9181=DIRECTION('ref_axis',(1.,0.,0.));
#9182=DIRECTION('center_axis',(0.,0.,1.));
#9183=DIRECTION('ref_axis',(1.,0.,0.));
#9184=DIRECTION('center_axis',(0.,0.,1.));
#9185=DIRECTION('ref_axis',(1.,0.,0.));
#14484=CARTESIAN_POINT('',(0.,0.,0.));
#14485=CARTESIAN_POINT('Origin',(0.,0.,0.));
#14486=CARTESIAN_POINT('',(-0.14652705620645,9.44412402177196E-5,0.0160655045842905));
#14487=CARTESIAN_POINT('',(-0.146479946776166,0.000162062070299865,0.00893449541571059));
#14488=CARTESIAN_POINT('',(-0.14635,-1.79227059055215E-17,0.));
#14489=CARTESIAN_POINT('',(0.0634007094575209,0.131904027763685,0.));
#14490=CARTESIAN_POINT('Ctrl Pts',(-0.14652705620645,9.44412402177196E-5,
0.0160655045842905));
#14491=CARTESIAN_POINT('Ctrl Pts',(-0.146560923555419,0.00502618404349199,
0.0157963945919035));
#14492=CARTESIAN_POINT('Ctrl Pts',(-0.146333578783787,0.00995455679532004,
0.0155272845995164));
#14493=CARTESIAN_POINT('Ctrl Pts',(-0.14583475180505,0.0148550342388422,
0.0152581746071293));
#14494=CARTESIAN_POINT('Ctrl Pts',(-0.140929468554047,0.0630445487404258,
0.0126118447280274));
#14495=CARTESIAN_POINT('Ctrl Pts',(-0.10977174472993,0.108536575508351,
0.0099655148489255));
#14496=CARTESIAN_POINT('Ctrl Pts',(-0.0666135938566871,0.13056551637767,
0.00731918496982359));
#14497=CARTESIAN_POINT('Ctrl Pts',(-0.0268248419338395,0.150874636338504,
0.00487945664654906));
#14498=CARTESIAN_POINT('Ctrl Pts',(0.0231637104697219,0.151241233100125,
0.00243972832327453));
#14499=CARTESIAN_POINT('Ctrl Pts',(0.0635546915223951,0.132092229195826,
-2.16840434497101E-19));
#14500=CARTESIAN_POINT('',(-0.0634007094575146,0.131904027763688,0.));
#14501=CARTESIAN_POINT('Origin',(0.,0.,0.));
#14502=CARTESIAN_POINT('Ctrl Pts',(-0.0634007094575145,0.131904027763688,
-3.88578058618805E-16));
#14503=CARTESIAN_POINT('Ctrl Pts',(-0.107282641710421,0.110811831533068,
0.00264738937425961));
#14504=CARTESIAN_POINT('Ctrl Pts',(-0.139432201149969,0.0662847592091173,
0.00529477874851962));
#14505=CARTESIAN_POINT('Ctrl Pts',(-0.145436119191498,0.0182745223106641,
0.00794216812277962));
#14506=CARTESIAN_POINT('Ctrl Pts',(-0.146186273512714,0.0122759249909008,
0.00827294388708994));
#14507=CARTESIAN_POINT('Ctrl Pts',(-0.146528267289359,0.00622295186417552,
0.00860371965140026));
#14508=CARTESIAN_POINT('Ctrl Pts',(-0.146479946776166,0.000162062070299865,
0.00893449541571059));
#14509=CARTESIAN_POINT('Origin',(0.,0.,0.));
#14510=CARTESIAN_POINT('',(-0.146148830924315,7.59978318484386E-5,0.0660655045842905));
#14511=CARTESIAN_POINT('',(-0.146133770585873,6.2751561688711E-5,0.0589344954157103));
#14512=CARTESIAN_POINT('',(-0.14635,-1.79227059055215E-17,0.));
#14513=CARTESIAN_POINT('Ctrl Pts',(-0.146148830924315,7.59978318484386E-5,
0.0660655045842905));
#14514=CARTESIAN_POINT('Ctrl Pts',(-0.146240443598182,0.0195917497831913,
0.0650077071998482));
#14515=CARTESIAN_POINT('Ctrl Pts',(-0.142607114239671,0.0390747476468127,
0.0639499098154059));
#14516=CARTESIAN_POINT('Ctrl Pts',(-0.135087779856993,0.056920264102034,
0.0628921124309636));
#14517=CARTESIAN_POINT('Ctrl Pts',(-0.116276389754784,0.10156503643559,
0.0602457825518617));
#14518=CARTESIAN_POINT('Ctrl Pts',(-0.073143724514267,0.135961331060063,
0.0575994526727599));
#14519=CARTESIAN_POINT('Ctrl Pts',(-0.025432083612881,0.144366623974243,
0.054953122793658));
#14520=CARTESIAN_POINT('Ctrl Pts',(0.0222795572885053,0.152771916888423,
0.0523067929145561));
#14521=CARTESIAN_POINT('Ctrl Pts',(0.0745701738507606,0.135186208092309,
0.0496604630354541));
#14522=CARTESIAN_POINT('Ctrl Pts',(0.107505148494886,0.0996564726649905,
0.0470141331563522));
#14523=CARTESIAN_POINT('Ctrl Pts',(0.140440123139012,0.0641267372376721,
0.0443678032772503));
#14524=CARTESIAN_POINT('Ctrl Pts',(0.154019455865009,0.010652975179149,
0.0417214733981484));
#14525=CARTESIAN_POINT('Ctrl Pts',(0.14202839331759,-0.0362847016460775,
0.0390751435190465));
#14526=CARTESIAN_POINT('Ctrl Pts',(0.130037330770172,-0.0832223784713041,
0.0364288136399446));
#14527=CARTESIAN_POINT('Ctrl Pts',(0.0924758729493388,-0.123623970063234,
0.0337824837608427));
#14528=CARTESIAN_POINT('Ctrl Pts',(0.0465351214488668,-0.139005253038876,
0.0311361538817407));
#14529=CARTESIAN_POINT('Ctrl Pts',(0.000594369948394902,-0.154386536014517,
0.0284898240026388));
#14530=CARTESIAN_POINT('Ctrl Pts',(-0.0537256752317158,-0.144747510373871,
0.025843494123537));
#14531=CARTESIAN_POINT('Ctrl Pts',(-0.0915592764828275,-0.114484496435928,
0.0231971642444351));
#14532=CARTESIAN_POINT('Ctrl Pts',(-0.125545511528741,-0.0872989822136326,
0.0208199443577202));
#14533=CARTESIAN_POINT('Ctrl Pts',(-0.146227884351973,-0.0434707826450544,
0.0184427244710054));
#14534=CARTESIAN_POINT('Ctrl Pts',(-0.14652705620645,9.44412402177196E-5,
0.0160655045842905));
#14535=CARTESIAN_POINT('Ctrl Pts',(-0.146479946776166,0.000162062070299865,
0.00893449541571059));
#14536=CARTESIAN_POINT('Ctrl Pts',(-0.146141530330399,-0.0422858476614564,
0.0112511090256603));
#14537=CARTESIAN_POINT('Ctrl Pts',(-0.126658161292025,-0.0851220706608281,
0.0135677226356099));
#14538=CARTESIAN_POINT('Ctrl Pts',(-0.0941604943243988,-0.112386678841155,
0.0158843362455596));
#14539=CARTESIAN_POINT('Ctrl Pts',(-0.0570226747722624,-0.143544241621566,
0.0185317256198196));
#14540=CARTESIAN_POINT('Ctrl Pts',(-0.00288875902448078,-0.154365965709432,
0.0211791149940796));
#14541=CARTESIAN_POINT('Ctrl Pts',(0.0434083729543798,-0.140002007265973,
0.0238265043683396));
#14542=CARTESIAN_POINT('Ctrl Pts',(0.0897055049332404,-0.125638048822514,
0.0264738937425996));
#14543=CARTESIAN_POINT('Ctrl Pts',(0.12816585314318,-0.0860884078477292,
0.0291212831168596));
#14544=CARTESIAN_POINT('Ctrl Pts',(0.141191617966992,-0.0394144013492358,
0.0317686724911196));
#14545=CARTESIAN_POINT('Ctrl Pts',(0.154217382790803,0.00725960514925768,
0.0344160618653796));
#14546=CARTESIAN_POINT('Ctrl Pts',(0.141808564228487,0.0610579771714599,
0.0370634512396396));
#14547=CARTESIAN_POINT('Ctrl Pts',(0.109639063769471,0.0973098477439542,
0.0397108406138996));
#14548=CARTESIAN_POINT('Ctrl Pts',(0.0774695633104545,0.133561718316448,
0.0423582299881596));
#14549=CARTESIAN_POINT('Ctrl Pts',(0.0255393809547383,0.152267087439235,
0.0450056193624196));
#14550=CARTESIAN_POINT('Ctrl Pts',(-0.0223595433272462,0.144872892294413,
0.0476530087366796));
#14551=CARTESIAN_POINT('Ctrl Pts',(-0.070258467609231,0.137478697149591,
0.0503003981109396));
#14552=CARTESIAN_POINT('Ctrl Pts',(-0.114126133817484,0.10398493773716,
0.0529477874851996));
#14553=CARTESIAN_POINT('Ctrl Pts',(-0.133871661545403,0.059725601630819,
0.0555951768594596));
#14554=CARTESIAN_POINT('Ctrl Pts',(-0.142173753131161,0.0411165744656389,
0.0567082830448765));
#14555=CARTESIAN_POINT('Ctrl Pts',(-0.146211489678532,0.0206043892842972,
0.0578213892302934));
#14556=CARTESIAN_POINT('Ctrl Pts',(-0.146133770585873,6.2751561688711E-5,
0.0589344954157103));
#14557=CARTESIAN_POINT('Origin',(0.,0.,0.));
#14558=CARTESIAN_POINT('',(-0.146252097264499,-0.000124487410312429,0.116065504584291));
#14559=CARTESIAN_POINT('',(-0.146276374479508,-0.000129480650117819,0.10893449541571));
#14560=CARTESIAN_POINT('',(-0.14635,-1.79227059055215E-17,0.));
#14561=CARTESIAN_POINT('Ctrl Pts',(-0.146252097264499,-0.000124487410312429,
0.116065504584291));
#14562=CARTESIAN_POINT('Ctrl Pts',(-0.145977101830714,0.0338815411246725,
0.114219019807793));
#14563=CARTESIAN_POINT('Ctrl Pts',(-0.134160879762789,0.0680598926014691,
0.112372535031295));
#14564=CARTESIAN_POINT('Ctrl Pts',(-0.112484833627769,0.0939988017516943,
0.110526050254798));
#14565=CARTESIAN_POINT('Ctrl Pts',(-0.0814193359437304,0.131173714423195,
0.107879720375696));
#14566=CARTESIAN_POINT('Ctrl Pts',(-0.0301019434218634,0.151424966146533,
0.105233390496594));
#14567=CARTESIAN_POINT('Ctrl Pts',(0.0179785702873004,0.145483266051774,
0.102587060617492));
#14568=CARTESIAN_POINT('Ctrl Pts',(0.0660590839964643,0.139541565957016,
0.0999407307383904));
#14569=CARTESIAN_POINT('Ctrl Pts',(0.110902718892925,0.107406914044162,
0.0972944008592884));
#14570=CARTESIAN_POINT('Ctrl Pts',(0.131983829661647,0.0637877973597534,
0.0946480709801865));
#14571=CARTESIAN_POINT('Ctrl Pts',(0.15306494043037,0.0201686806753445,
0.0920017411010846));
#14572=CARTESIAN_POINT('Ctrl Pts',(0.150383527071356,-0.0349349007806195,
0.0893554112219828));
#14573=CARTESIAN_POINT('Ctrl Pts',(0.125166930059577,-0.0763010783846813,
0.0867090813428809));
#14574=CARTESIAN_POINT('Ctrl Pts',(0.0999503330477985,-0.117667255988743,
0.084062751463779));
#14575=CARTESIAN_POINT('Ctrl Pts',(0.0521985523832557,-0.145296029740903,
0.081416421584677));
#14576=CARTESIAN_POINT('Ctrl Pts',(0.00376830011669856,-0.146541450754272,
0.0787700917055751));
#14577=CARTESIAN_POINT('Ctrl Pts',(-0.0446619521498586,-0.147786871767642,
0.0761237618264732));
#14578=CARTESIAN_POINT('Ctrl Pts',(-0.09377067601843,-0.122648940042221,
0.0734774319473713));
#14579=CARTESIAN_POINT('Ctrl Pts',(-0.121079980470766,-0.0826333491581908,
0.0708311020682694));
#14580=CARTESIAN_POINT('Ctrl Pts',(-0.137473143648068,-0.0586128871159229,
0.0692425695736098));
#14581=CARTESIAN_POINT('Ctrl Pts',(-0.146011252866834,-0.02923151094855,
0.0676540370789502));
#14582=CARTESIAN_POINT('Ctrl Pts',(-0.146148830924315,7.59978318484386E-5,
0.0660655045842905));
#14583=CARTESIAN_POINT('Ctrl Pts',(-0.146133770585873,6.2751561688711E-5,
0.0589344954157103));
#14584=CARTESIAN_POINT('Ctrl Pts',(-0.146026644150963,-0.0282514289199324,
0.0604687786045534));
#14585=CARTESIAN_POINT('Ctrl Pts',(-0.138100435392092,-0.0566215672018456,
0.0620030617933965));
#14586=CARTESIAN_POINT('Ctrl Pts',(-0.122745086057252,-0.0801407530065182,
0.0635373449822396));
#14587=CARTESIAN_POINT('Ctrl Pts',(-0.0962495935935968,-0.120722858737265,
0.0661847343564996));
#14588=CARTESIAN_POINT('Ctrl Pts',(-0.0476352194187008,-0.146862157398507,
0.0688321237307596));
#14589=CARTESIAN_POINT('Ctrl Pts',(0.00082938917649622,-0.146587691816784,
0.0714795131050196));
#14590=CARTESIAN_POINT('Ctrl Pts',(0.0492939977716932,-0.146313226235061,
0.0741269024792796));
#14591=CARTESIAN_POINT('Ctrl Pts',(0.0976088407871913,-0.119624996410372,
0.0767742918535397));
#14592=CARTESIAN_POINT('Ctrl Pts',(0.123643642180798,-0.0787464320231966,
0.0794216812277997));
#14593=CARTESIAN_POINT('Ctrl Pts',(0.149678443574405,-0.0378678676360213,
0.0820690706020596));
#14594=CARTESIAN_POINT('Ctrl Pts',(0.153433203346121,0.0172010313136401,
0.0847164599763195));
#14595=CARTESIAN_POINT('Ctrl Pts',(0.133187835944515,0.06123527443138,0.0873638493505795));
#14596=CARTESIAN_POINT('Ctrl Pts',(0.11294246854291,0.10526951754912,0.0900112387248395));
#14597=CARTESIAN_POINT('Ctrl Pts',(0.0686969739679828,0.138269104834938,
0.0926586280990997));
#14598=CARTESIAN_POINT('Ctrl Pts',(0.0207181735233275,0.145118849380084,
0.0953060174733597));
#14599=CARTESIAN_POINT('Ctrl Pts',(-0.027260626921328,0.151968593925229,
0.0979534068476197));
#14600=CARTESIAN_POINT('Ctrl Pts',(-0.0789727332357116,0.132668495729702,
0.10060079622188));
#14601=CARTESIAN_POINT('Ctrl Pts',(-0.110731403441959,0.0960588230543748,
0.10324818559614));
#14602=CARTESIAN_POINT('Ctrl Pts',(-0.133469481440122,0.0698475998711364,
0.105143622202663));
#14603=CARTESIAN_POINT('Ctrl Pts',(-0.145979327216774,0.0347634013028336,
0.107039058809187));
#14604=CARTESIAN_POINT('Ctrl Pts',(-0.146276374479508,-0.000129480650117819,
0.10893449541571));
#14605=CARTESIAN_POINT('Origin',(0.,0.,0.));
#14606=CARTESIAN_POINT('',(-0.146589818999335,-3.81787486967988E-6,0.166065504584291));
#14607=CARTESIAN_POINT('',(-0.146589453522336,1.04004190909306E-5,0.15893449541571));
#14608=CARTESIAN_POINT('',(-0.14635,-1.79227059055215E-17,0.));
#14609=CARTESIAN_POINT('Ctrl Pts',(-0.146589818999335,-3.81787486967988E-6,
0.166065504584291));
#14610=CARTESIAN_POINT('Ctrl Pts',(-0.146571339149733,0.0482382848470949,
0.163430332415738));
#14611=CARTESIAN_POINT('Ctrl Pts',(-0.120433071521034,0.0964975486977609,
0.160795160247185));
#14612=CARTESIAN_POINT('Ctrl Pts',(-0.0800107885095625,0.122828684230981,
0.158159988078632));
#14613=CARTESIAN_POINT('Ctrl Pts',(-0.0394173515450545,0.149271309704865,
0.15551365819953));
#14614=CARTESIAN_POINT('Ctrl Pts',(0.0155813181737399,0.153599719825856,
0.152867328320428));
#14615=CARTESIAN_POINT('Ctrl Pts',(0.0598114643267532,0.133832733731537,
0.150220998441327));
#14616=CARTESIAN_POINT('Ctrl Pts',(0.104041610479766,0.114065747637217,
0.147574668562225));
#14617=CARTESIAN_POINT('Ctrl Pts',(0.137503233066998,0.0702033653275883,
0.144928338683123));
#14618=CARTESIAN_POINT('Ctrl Pts',(0.144880420813362,0.0223220882221681,
0.142282008804021));
#14619=CARTESIAN_POINT('Ctrl Pts',(0.152257608559726,-0.0255591888832524,
0.139635678924919));
#14620=CARTESIAN_POINT('Ctrl Pts',(0.133550361465222,-0.077459360784464,
0.136989349045817));
#14621=CARTESIAN_POINT('Ctrl Pts',(0.0973212811704284,-0.109622900294719,
0.134343019166715));
#14622=CARTESIAN_POINT('Ctrl Pts',(0.0610922008756344,-0.141786439804975,
0.131696689287613));
#14623=CARTESIAN_POINT('Ctrl Pts',(0.00734128738055008,-0.154213346924274,
0.129050359408511));
#14624=CARTESIAN_POINT('Ctrl Pts',(-0.0393288211819405,-0.141215634503184,
0.126404029529409));
#14625=CARTESIAN_POINT('Ctrl Pts',(-0.0859989297444312,-0.128217922082094,
0.123757699650308));
#14626=CARTESIAN_POINT('Ctrl Pts',(-0.125588233374328,-0.0897955901206149,
0.121111369771206));
#14627=CARTESIAN_POINT('Ctrl Pts',(-0.139976083766172,-0.043535137330043,
0.118465039892104));
#14628=CARTESIAN_POINT('Ctrl Pts',(-0.144324767489921,-0.0295530571287048,
0.117665194789499));
#14629=CARTESIAN_POINT('Ctrl Pts',(-0.146371217526823,-0.0148549394177889,
0.116865349686895));
#14630=CARTESIAN_POINT('Ctrl Pts',(-0.146252097264499,-0.000124487410312429,
0.116065504584291));
#14631=CARTESIAN_POINT('Ctrl Pts',(-0.146276374479508,-0.000129480650117819,
0.10893449541571));
#14632=CARTESIAN_POINT('Ctrl Pts',(-0.14639421831063,-0.0139720956278579,
0.109686448183447));
#14633=CARTESIAN_POINT('Ctrl Pts',(-0.14458995413065,-0.0277846002915201,
0.110438400951183));
#14634=CARTESIAN_POINT('Ctrl Pts',(-0.140739671041232,-0.041001045008257,
0.11119035371892));
#14635=CARTESIAN_POINT('Ctrl Pts',(-0.127184034336146,-0.0875319932404337,
0.11383774309318));
#14636=CARTESIAN_POINT('Ctrl Pts',(-0.0882675268278623,-0.12667464254966,
0.11648513246744));
#14637=CARTESIAN_POINT('Ctrl Pts',(-0.0418159243469935,-0.140499695546946,
0.1191325218417));
#14638=CARTESIAN_POINT('Ctrl Pts',(0.00463567813387508,-0.154324748544231,
0.12177991121596));
#14639=CARTESIAN_POINT('Ctrl Pts',(0.0586223755873289,-0.142832205229577,
0.12442730059022));
#14640=CARTESIAN_POINT('Ctrl Pts',(0.0954154960694136,-0.111286216216264,
0.12707468996448));
#14641=CARTESIAN_POINT('Ctrl Pts',(0.132208616551499,-0.0797402272029501,
0.12972207933874));
#14642=CARTESIAN_POINT('Ctrl Pts',(0.151808160062214,-0.0281407924909768,
0.132369468712999));
#14643=CARTESIAN_POINT('Ctrl Pts',(0.145236524363737,0.0198768833792122,
0.135016858087259));
#14644=CARTESIAN_POINT('Ctrl Pts',(0.138664888665259,0.0678945592494009,
0.13766424746152));
#14645=CARTESIAN_POINT('Ctrl Pts',(0.105922073757589,0.112330476277805,
0.14031163683578));
#14646=CARTESIAN_POINT('Ctrl Pts',(0.062005973158836,0.132830708741579,
0.14295902621004));
#14647=CARTESIAN_POINT('Ctrl Pts',(0.0180898725600832,0.153330941205352,
0.1456064155843));
#14648=CARTESIAN_POINT('Ctrl Pts',(-0.0369995137297515,0.149895489104495,
0.14825380495856));
#14649=CARTESIAN_POINT('Ctrl Pts',(-0.0780284182758478,0.124097962381086,
0.15090119433282));
#14650=CARTESIAN_POINT('Ctrl Pts',(-0.119057322821944,0.0983004356576776,
0.153548583707079));
#14651=CARTESIAN_POINT('Ctrl Pts',(-0.146025745624302,0.0501408343117172,
0.15619597308134));
#14652=CARTESIAN_POINT('Ctrl Pts',(-0.14658076309025,0.00167873146180186,
0.1588433624556));
#14653=CARTESIAN_POINT('Ctrl Pts',(-0.146587131676737,0.00112264969450139,
0.15887374010897));
#14654=CARTESIAN_POINT('Ctrl Pts',(-0.146590022522527,0.000566528098114988,
0.15890411776234));
#14655=CARTESIAN_POINT('Ctrl Pts',(-0.146589453522336,1.04004190909306E-5,
0.15893449541571));
#14656=CARTESIAN_POINT('Origin',(0.,0.,0.));
#14657=CARTESIAN_POINT('',(-0.146263250741535,0.000126870157254357,0.21606550458429));
#14658=CARTESIAN_POINT('',(-0.146245769975643,0.000123264779366826,0.20893449541571));
#14659=CARTESIAN_POINT('',(-0.14635,-1.79227059055215E-17,0.));
#14660=CARTESIAN_POINT('Ctrl Pts',(-0.146263250741535,0.000126870157254357,
0.21606550458429));
#14661=CARTESIAN_POINT('Ctrl Pts',(-0.146381923100139,0.0144435832128767,
0.215287974902784));
#14662=CARTESIAN_POINT('Ctrl Pts',(-0.144450237714319,0.0287289633064517,
0.214510445221278));
#14663=CARTESIAN_POINT('Ctrl Pts',(-0.140337374518256,0.0423560295890773,
0.213732915539772));
#14664=CARTESIAN_POINT('Ctrl Pts',(-0.126339204386259,0.0887358830222778,
0.21108658566067));
#14665=CARTESIAN_POINT('Ctrl Pts',(-0.0870745347363382,0.127489909020004,
0.208440255781569));
#14666=CARTESIAN_POINT('Ctrl Pts',(-0.0405154226099946,0.140879780169064,
0.205793925902467));
#14667=CARTESIAN_POINT('Ctrl Pts',(0.00604368951634975,0.154269651318124,
0.203147596023365));
#14668=CARTESIAN_POINT('Ctrl Pts',(0.0598972441191175,0.142295367618517,
0.200501266144263));
#14669=CARTESIAN_POINT('Ctrl Pts',(0.0963956219934077,0.110437747119808,
0.197854936265161));
#14670=CARTESIAN_POINT('Ctrl Pts',(0.132893999867697,0.0785801266211,0.195208606386059));
#14671=CARTESIAN_POINT('Ctrl Pts',(0.15203720101351,0.0268391693232909,
0.192562276506957));
#14672=CARTESIAN_POINT('Ctrl Pts',(0.145063081087281,-0.0211024746124516,
0.189915946627855));
#14673=CARTESIAN_POINT('Ctrl Pts',(0.138088961161051,-0.0690441185481943,
0.187269616748753));
#14674=CARTESIAN_POINT('Ctrl Pts',(0.10499752016278,-0.11318644912187,0.184623286869651));
#14675=CARTESIAN_POINT('Ctrl Pts',(0.060935231264163,-0.133324827106958,
0.181976956990549));
#14676=CARTESIAN_POINT('Ctrl Pts',(0.0168729423655461,-0.153463205092045,
0.179330627111448));
#14677=CARTESIAN_POINT('Ctrl Pts',(-0.0381601944334158,-0.149597630488544,
0.176684297232346));
#14678=CARTESIAN_POINT('Ctrl Pts',(-0.0789746466099193,-0.123497437688695,
0.174037967353244));
#14679=CARTESIAN_POINT('Ctrl Pts',(-0.119961184605052,-0.0972871987457574,
0.171380479763593));
#14680=CARTESIAN_POINT('Ctrl Pts',(-0.146608455341797,-0.0486544490602708,
0.168722992173942));
#14681=CARTESIAN_POINT('Ctrl Pts',(-0.146589818999335,-3.81787486967988E-6,
0.166065504584291));
#14682=CARTESIAN_POINT('Ctrl Pts',(-0.146589453522336,1.04004190909306E-5,
0.15893449541571));
#14683=CARTESIAN_POINT('Ctrl Pts',(-0.146540434588914,-0.0478995759235739,
0.1615515071366));
#14684=CARTESIAN_POINT('Ctrl Pts',(-0.120813506558866,-0.0958546957256878,
0.16416851885749));
#14685=CARTESIAN_POINT('Ctrl Pts',(-0.0808500697395765,-0.122278388912248,
0.16678553057838));
#14686=CARTESIAN_POINT('Ctrl Pts',(-0.0404227467934142,-0.149008802082514,
0.16943291995264));
#14687=CARTESIAN_POINT('Ctrl Pts',(0.0145735112284506,-0.153705024069172,
0.1720803093269));
#14688=CARTESIAN_POINT('Ctrl Pts',(0.0589475933459444,-0.134215943447351,
0.17472769870116));
#14689=CARTESIAN_POINT('Ctrl Pts',(0.103321675463438,-0.11472686282553,
0.17737508807542));
#14690=CARTESIAN_POINT('Ctrl Pts',(0.137073581676561,-0.0710524795952304,
0.18002247744968));
#14691=CARTESIAN_POINT('Ctrl Pts',(0.144743205110219,-0.0231979049720499,
0.18266986682394));
#14692=CARTESIAN_POINT('Ctrl Pts',(0.152412828543877,0.024656669651131,
0.1853172561982));
#14693=CARTESIAN_POINT('Ctrl Pts',(0.13400016919807,0.0766914356671922,
0.18796464557246));
#14694=CARTESIAN_POINT('Ctrl Pts',(0.0979391709064228,0.109071797518936,
0.19061203494672));
#14695=CARTESIAN_POINT('Ctrl Pts',(0.0618781726147763,0.141452159370678,
0.19325942432098));
#14696=CARTESIAN_POINT('Ctrl Pts',(0.00816883537729064,0.154178117058104,
0.195906813695239));
#14697=CARTESIAN_POINT('Ctrl Pts',(-0.0385872054932313,0.1414205281901,
0.198554203069499));
#14698=CARTESIAN_POINT('Ctrl Pts',(-0.0853432463637543,0.128662939322095,
0.201201592443759));
#14699=CARTESIAN_POINT('Ctrl Pts',(-0.125145990867313,0.0904218038986596,
0.20384898181802));
#14700=CARTESIAN_POINT('Ctrl Pts',(-0.139763737461459,0.0442135263146365,
0.20649637119228));
#14701=CARTESIAN_POINT('Ctrl Pts',(-0.144251162244238,0.030028291356252,
0.207309079266757));
#14702=CARTESIAN_POINT('Ctrl Pts',(-0.146365162502875,0.0150922359825044,
0.208121787341234));
#14703=CARTESIAN_POINT('Ctrl Pts',(-0.146245769975643,0.000123264779366826,
0.20893449541571));
#14704=CARTESIAN_POINT('Origin',(0.,0.,0.));
#14705=CARTESIAN_POINT('',(-0.146142672279203,-7.01165389862951E-5,0.266065504584291));
#14706=CARTESIAN_POINT('',(-0.146150215784492,-7.74481165901552E-5,0.258934495415711));
#14707=CARTESIAN_POINT('',(-0.14635,-1.79227059055215E-17,0.));
#14708=CARTESIAN_POINT('Ctrl Pts',(-0.146142672279203,-7.01165389862951E-5,
0.266065504584291));
#14709=CARTESIAN_POINT('Ctrl Pts',(-0.146017527260215,0.028828671850369,
0.264499287510729));
#14710=CARTESIAN_POINT('Ctrl Pts',(-0.137733916992107,0.0577936173630845,
0.262933070437168));
#14711=CARTESIAN_POINT('Ctrl Pts',(-0.121770841384076,0.0816117278206753,
0.261366853363607));
#14712=CARTESIAN_POINT('Ctrl Pts',(-0.0947991242083451,0.121855560193383,
0.258720523484505));
#14713=CARTESIAN_POINT('Ctrl Pts',(-0.0459036471244643,0.147405924851771,
0.256074193605403));
#14714=CARTESIAN_POINT('Ctrl Pts',(0.0025353607453442,0.146568017913755,
0.253427863726301));
#14715=CARTESIAN_POINT('Ctrl Pts',(0.050974368615152,0.145730110975738,
0.250781533847199));
#14716=CARTESIAN_POINT('Ctrl Pts',(0.0989569072708876,0.118503932441319,
0.248135203968097));
#14717=CARTESIAN_POINT('Ctrl Pts',(0.124520613871998,0.0773513325689396,
0.245488874088995));
#14718=CARTESIAN_POINT('Ctrl Pts',(0.150084320473109,0.0361987326965595,
0.242842544209893));
#14719=CARTESIAN_POINT('Ctrl Pts',(0.153229195019594,-0.0188802885137813,
0.240196214330791));
#14720=CARTESIAN_POINT('Ctrl Pts',(0.132515778953886,-0.0626751965094481,
0.237549884451689));
#14721=CARTESIAN_POINT('Ctrl Pts',(0.111802362888177,-0.106470104505115,
0.234903554572587));
#14722=CARTESIAN_POINT('Ctrl Pts',(0.0672306562102751,-0.138980899286108,
0.232257224693486));
#14723=CARTESIAN_POINT('Ctrl Pts',(0.0192018303028616,-0.145326878595667,
0.229610894814384));
#14724=CARTESIAN_POINT('Ctrl Pts',(-0.0288269956045516,-0.151672857905225,
0.226964564935282));
#14725=CARTESIAN_POINT('Ctrl Pts',(-0.0803129407414762,-0.131854021743351,
0.22431823505618));
#14726=CARTESIAN_POINT('Ctrl Pts',(-0.111690078002902,-0.0949417632280756,
0.221671905177078));
#14727=CARTESIAN_POINT('Ctrl Pts',(-0.133848162215005,-0.0688748557907962,
0.219803104979482));
#14728=CARTESIAN_POINT('Ctrl Pts',(-0.145978020566425,-0.0342834897603843,
0.217934304781886));
#14729=CARTESIAN_POINT('Ctrl Pts',(-0.146263250741535,0.000126870157254357,
0.21606550458429));
#14730=CARTESIAN_POINT('Ctrl Pts',(-0.146245769975643,0.000123264779366826,
0.20893449541571));
#14731=CARTESIAN_POINT('Ctrl Pts',(-0.145976242399967,-0.03366905549635,
0.210769176715493));
#14732=CARTESIAN_POINT('Ctrl Pts',(-0.134324750276972,-0.067629123606452,
0.212603858015276));
#14733=CARTESIAN_POINT('Ctrl Pts',(-0.112902327433,-0.0934976078712483,
0.214438539315059));
#14734=CARTESIAN_POINT('Ctrl Pts',(-0.0819904221256615,-0.130825044728502,
0.217085928689319));
#14735=CARTESIAN_POINT('Ctrl Pts',(-0.0307338628262512,-0.151304498698398,
0.21973331806358));
#14736=CARTESIAN_POINT('Ctrl Pts',(0.0173892134168267,-0.145555327884408,
0.22238070743784));
#14737=CARTESIAN_POINT('Ctrl Pts',(0.0655122896599044,-0.139806157070418,
0.2250280968121));
#14738=CARTESIAN_POINT('Ctrl Pts',(0.11050188284665,-0.107828361472542,
0.22767548618636));
#14739=CARTESIAN_POINT('Ctrl Pts',(0.131750448317205,-0.0642694140823833,
0.23032287556062));
#14740=CARTESIAN_POINT('Ctrl Pts',(0.15299901378776,-0.020710466692225,
0.232970264934879));
#14741=CARTESIAN_POINT('Ctrl Pts',(0.150506551542124,0.0344296324902152,
0.23561765430914));
#14742=CARTESIAN_POINT('Ctrl Pts',(0.125414737320077,0.0758938856636754,
0.2382650436834));
#14743=CARTESIAN_POINT('Ctrl Pts',(0.10032292309803,0.117358138837136,0.24091243305766));
#14744=CARTESIAN_POINT('Ctrl Pts',(0.0526317568995709,0.145146546001616,
0.24355982243192));
#14745=CARTESIAN_POINT('Ctrl Pts',(0.00418624259284972,0.146530589268381,
0.24620721180618));
#14746=CARTESIAN_POINT('Ctrl Pts',(-0.0442592717138715,0.147914632535146,
0.24885460118044));
#14747=CARTESIAN_POINT('Ctrl Pts',(-0.0934591341288551,0.122894311904195,
0.2515019905547));
#14748=CARTESIAN_POINT('Ctrl Pts',(-0.120877280418781,0.082930219442967,
0.25414937992896));
#14749=CARTESIAN_POINT('Ctrl Pts',(-0.137396572682769,0.0588520590724165,
0.255744418424543));
#14750=CARTESIAN_POINT('Ctrl Pts',(-0.146009100715185,0.0293493086505574,
0.257339456920127));
#14751=CARTESIAN_POINT('Ctrl Pts',(-0.146150215784492,-7.74481165901552E-5,
0.258934495415711));
#14752=CARTESIAN_POINT('Origin',(0.,0.,0.));
#14753=CARTESIAN_POINT('',(-0.146519404976022,-8.97763884284003E-5,0.316065504584291));
#14754=CARTESIAN_POINT('',(-0.146528765763263,-8.45393868379275E-5,0.30893449541571));
#14755=CARTESIAN_POINT('',(-0.14635,-1.79227059055215E-17,0.));
#14756=CARTESIAN_POINT('Ctrl Pts',(-0.146519404976022,-8.97763884284003E-5,
0.316065504584291));
#14757=CARTESIAN_POINT('Ctrl Pts',(-0.146208092107557,0.043076445171776,
0.313710600118674));
#14758=CARTESIAN_POINT('Ctrl Pts',(-0.125958424314353,0.0864965766126209,
0.311355695653057));
#14759=CARTESIAN_POINT('Ctrl Pts',(-0.0925183485457987,0.1137056160074,
0.309000791187441));
#14760=CARTESIAN_POINT('Ctrl Pts',(-0.0549399784004991,0.144281843189175,
0.306354461308339));
#14761=CARTESIAN_POINT('Ctrl Pts',(-0.00070450021881692,0.154386382754941,
0.303708131429237));
#14762=CARTESIAN_POINT('Ctrl Pts',(0.0453636543616171,0.139394227973128,
0.301061801550135));
#14763=CARTESIAN_POINT('Ctrl Pts',(0.0914318089420511,0.124402073191315,
0.298415471671033));
#14764=CARTESIAN_POINT('Ctrl Pts',(0.129332639921237,0.0843132240619223,
0.295769141791931));
#14765=CARTESIAN_POINT('Ctrl Pts',(0.141718340675246,0.0374769775398043,
0.293122811912829));
#14766=CARTESIAN_POINT('Ctrl Pts',(0.154104041429255,-0.00935926898231351,
0.290476482033727));
#14767=CARTESIAN_POINT('Ctrl Pts',(0.140974611958088,-0.0629429128971569,
0.287830152154626));
#14768=CARTESIAN_POINT('Ctrl Pts',(0.108339598692885,-0.0987478773661917,
0.285183822275524));
#14769=CARTESIAN_POINT('Ctrl Pts',(0.0757045854276824,-0.134552841835227,
0.282537492396422));
#14770=CARTESIAN_POINT('Ctrl Pts',(0.0235639883684441,-0.152579126858453,
0.27989116251732));
#14771=CARTESIAN_POINT('Ctrl Pts',(-0.0242166208952047,-0.144575818177467,
0.277244832638218));
#14772=CARTESIAN_POINT('Ctrl Pts',(-0.0719972301588528,-0.136572509496481,
0.274598502759116));
#14773=CARTESIAN_POINT('Ctrl Pts',(-0.115417851626912,-0.102539607111283,
0.271952172880014));
#14774=CARTESIAN_POINT('Ctrl Pts',(-0.13460418372715,-0.0580545058751705,
0.269305843000912));
#14775=CARTESIAN_POINT('Ctrl Pts',(-0.142435181350113,-0.0398976888130428,
0.268225730195372));
#14776=CARTESIAN_POINT('Ctrl Pts',(-0.146228976240411,-0.0199996345674016,
0.267145617389831));
#14777=CARTESIAN_POINT('Ctrl Pts',(-0.146142672279203,-7.01165389862951E-5,
0.266065504584291));
#14778=CARTESIAN_POINT('Ctrl Pts',(-0.146150215784492,-7.74481165901552E-5,
0.258934495415711));
#14779=CARTESIAN_POINT('Ctrl Pts',(-0.146243318595233,-0.0194921979337541,
0.259986846294387));
#14780=CARTESIAN_POINT('Ctrl Pts',(-0.142648899141753,-0.0388738684647463,
0.261039197173063));
#14781=CARTESIAN_POINT('Ctrl Pts',(-0.135204796371803,-0.0566427511368837,
0.26209154805174));
#14782=CARTESIAN_POINT('Ctrl Pts',(-0.116477735870028,-0.101343764964001,
0.264738937426));
#14783=CARTESIAN_POINT('Ctrl Pts',(-0.0733871847016099,-0.135837928326728,
0.26738632680026));
#14784=CARTESIAN_POINT('Ctrl Pts',(-0.0256708287318585,-0.144325142544676,
0.27003371617452));
#14785=CARTESIAN_POINT('Ctrl Pts',(0.0220455272378925,-0.152812356762624,
0.27268110554878));
#14786=CARTESIAN_POINT('Ctrl Pts',(0.0743876880089763,-0.135292621835792,
0.27532849492304));
#14787=CARTESIAN_POINT('Ctrl Pts',(0.10738025529095,-0.0997908762961729,
0.2779758842973));
#14788=CARTESIAN_POINT('Ctrl Pts',(0.140372822572925,-0.0642891307565533,
0.280623273671559));
#14789=CARTESIAN_POINT('Ctrl Pts',(0.154015796365789,-0.010805374604146,
0.283270663045819));
#14790=CARTESIAN_POINT('Ctrl Pts',(0.142059993874458,0.0361620845457957,
0.285918052420079));
#14791=CARTESIAN_POINT('Ctrl Pts',(0.130104191383128,0.0831295436957373,
0.288565441794339));
#14792=CARTESIAN_POINT('Ctrl Pts',(0.0925496126076039,0.123580705843213,
0.291212831168599));
#14793=CARTESIAN_POINT('Ctrl Pts',(0.0465981836912963,0.138986860871753,
0.29386022054286));
#14794=CARTESIAN_POINT('Ctrl Pts',(0.000646754774988913,0.154393015900293,
0.296507609917119));
#14795=CARTESIAN_POINT('Ctrl Pts',(-0.0537015242821025,0.144754163809898,
0.29915499929138));
#14796=CARTESIAN_POINT('Ctrl Pts',(-0.0915523499663989,0.114485393976436,
0.30180238866564));
#14797=CARTESIAN_POINT('Ctrl Pts',(-0.125542580994678,0.0873038870745135,
0.30417975758233));
#14798=CARTESIAN_POINT('Ctrl Pts',(-0.146229051243382,0.0434861464246214,
0.30655712649902));
#14799=CARTESIAN_POINT('Ctrl Pts',(-0.146528765763263,-8.45393868379275E-5,
0.30893449541571));
#14800=CARTESIAN_POINT('Origin',(0.,0.,0.));
#14801=CARTESIAN_POINT('',(-0.146416087288192,0.000126442170093593,0.366065504584291));
#14802=CARTESIAN_POINT('',(-0.146408012399712,0.000128195943346294,0.358934495415711));
#14803=CARTESIAN_POINT('',(-0.14635,-1.79227059055215E-17,0.));
#14804=CARTESIAN_POINT('Ctrl Pts',(-0.146416087288192,0.000126442170093593,
0.366065504584291));
#14805=CARTESIAN_POINT('Ctrl Pts',(-0.146499294961499,0.00925816812376314,
0.365568242605721));
#14806=CARTESIAN_POINT('Ctrl Pts',(-0.145718277739785,0.0183757049974218,
0.365070980627151));
#14807=CARTESIAN_POINT('Ctrl Pts',(-0.144021710151773,0.0273195705351122,
0.364573718648581));
#14808=CARTESIAN_POINT('Ctrl Pts',(-0.134992913071845,0.0749170536065741,
0.361927388769479));
#14809=CARTESIAN_POINT('Ctrl Pts',(-0.100034284522917,0.117595890322328,
0.359281058890377));
#14810=CARTESIAN_POINT('Ctrl Pts',(-0.0551469387876206,0.135821305661589,
0.356634729011275));
#14811=CARTESIAN_POINT('Ctrl Pts',(-0.0102595930523245,0.15404672100085,
0.353988399132173));
#14812=CARTESIAN_POINT('Ctrl Pts',(0.0445564698693406,0.147818714963618,
0.351342069253072));
#14813=CARTESIAN_POINT('Ctrl Pts',(0.0842110755700531,0.119987943896873,
0.34869573937397));
#14814=CARTESIAN_POINT('Ctrl Pts',(0.123865681270766,0.0921571728301272,
0.346049409494868));
#14815=CARTESIAN_POINT('Ctrl Pts',(0.148358829750526,0.0427236367338667,
0.343403079615766));
#14816=CARTESIAN_POINT('Ctrl Pts',(0.146479621605269,-0.00568615719458776,
0.340756749736664));
#14817=CARTESIAN_POINT('Ctrl Pts',(0.144600413460012,-0.0540959511230416,
0.338110419857562));
#14818=CARTESIAN_POINT('Ctrl Pts',(0.116348848689739,-0.101482002883689,
0.33546408997846));
#14819=CARTESIAN_POINT('Ctrl Pts',(0.0746561129649502,-0.126154971072205,
0.332817760099358));
#14820=CARTESIAN_POINT('Ctrl Pts',(0.0329633772401616,-0.150827939260721,
0.330171430220256));
#14821=CARTESIAN_POINT('Ctrl Pts',(-0.0221705294391424,-0.152787823877104,
0.327525100341154));
#14822=CARTESIAN_POINT('Ctrl Pts',(-0.0655099505772086,-0.131137554898038,
0.324878770462052));
#14823=CARTESIAN_POINT('Ctrl Pts',(-0.108849371715275,-0.109487285918972,
0.322232440582951));
#14824=CARTESIAN_POINT('Ctrl Pts',(-0.140394307312104,-0.0642268633444555,
0.319586110703849));
#14825=CARTESIAN_POINT('Ctrl Pts',(-0.14570614405606,-0.0160726946583056,
0.316939780824747));
#14826=CARTESIAN_POINT('Ctrl Pts',(-0.146291106736525,-0.0107697471190636,
0.316648355411261));
#14827=CARTESIAN_POINT('Ctrl Pts',(-0.146557930734812,-0.0054317060295066,
0.316356929997776));
#14828=CARTESIAN_POINT('Ctrl Pts',(-0.146519404976022,-8.97763884284003E-5,
0.316065504584291));
#14829=CARTESIAN_POINT('Ctrl Pts',(-0.146528765763263,-8.45393868379275E-5,
0.30893449541571));
#14830=CARTESIAN_POINT('Ctrl Pts',(-0.146562807199252,-0.00503327764821679,
0.30920451587328));
#14831=CARTESIAN_POINT('Ctrl Pts',(-0.14633385314783,-0.00997882882536714,
0.30947453633085));
#14832=CARTESIAN_POINT('Ctrl Pts',(-0.145831525524598,-0.0148964553326841,
0.309744556788419));
#14833=CARTESIAN_POINT('Ctrl Pts',(-0.140906503086998,-0.0631108472318147,
0.312391946162679));
#14834=CARTESIAN_POINT('Ctrl Pts',(-0.109703085900295,-0.108640943453547,
0.31503933553694));
#14835=CARTESIAN_POINT('Ctrl Pts',(-0.0665140418604196,-0.13063162118607,
0.3176867249112));
#14836=CARTESIAN_POINT('Ctrl Pts',(-0.0233249978205455,-0.152622298918592,
0.32033411428546));
#14837=CARTESIAN_POINT('Ctrl Pts',(0.0318496730725009,-0.151073558161906,
0.322981503659719));
#14838=CARTESIAN_POINT('Ctrl Pts',(0.0737371373950496,-0.126694801736668,
0.325628893033979));
#14839=CARTESIAN_POINT('Ctrl Pts',(0.115624601717599,-0.10231604531143,
0.328276282408239));
#14840=CARTESIAN_POINT('Ctrl Pts',(0.144224859469651,-0.0551072732176397,
0.3309236717825));
#14841=CARTESIAN_POINT('Ctrl Pts',(0.146437523492708,-0.0066925280449658,
0.33357106115676));
#14842=CARTESIAN_POINT('Ctrl Pts',(0.148650187515766,0.0417222171277085,
0.33621845053102));
#14843=CARTESIAN_POINT('Ctrl Pts',(0.124475257809829,0.0913429353792657,
0.33886583990528));
#14844=CARTESIAN_POINT('Ctrl Pts',(0.0849860939726622,0.119440788885456,
0.34151322927954));
#14845=CARTESIAN_POINT('Ctrl Pts',(0.0454969301354961,0.147538642391646,
0.344160618653799));
#14846=CARTESIAN_POINT('Ctrl Pts',(-0.00930646783289898,0.154113631152469,
0.346808008028059));
#14847=CARTESIAN_POINT('Ctrl Pts',(-0.0543213285795041,0.136154072578339,
0.349455397402319));
#14848=CARTESIAN_POINT('Ctrl Pts',(-0.0993361893261098,0.11819451400421,
0.352102786776579));
#14849=CARTESIAN_POINT('Ctrl Pts',(-0.134562512850926,0.0757004080951257,
0.35475017615084));
#14850=CARTESIAN_POINT('Ctrl Pts',(-0.143864833510727,0.0281362381501331,
0.3573975655251));
#14851=CARTESIAN_POINT('Ctrl Pts',(-0.145664973529558,0.0189318504589563,
0.357909875488637));
#14852=CARTESIAN_POINT('Ctrl Pts',(-0.146494308508217,0.00953759842677947,
0.358422185452174));
#14853=CARTESIAN_POINT('Ctrl Pts',(-0.146408012399712,0.000128195943346294,
0.358934495415711));
#14854=CARTESIAN_POINT('Origin',(0.,0.,0.));
#14855=CARTESIAN_POINT('',(-0.146110491840834,1.12683595067248E-5,0.416065504584291));
#14856=CARTESIAN_POINT('',(-0.146109756335714,8.81622270207575E-6,0.40893449541571));
#14857=CARTESIAN_POINT('',(-0.14635,-1.79227059055215E-17,0.));
#14858=CARTESIAN_POINT('Ctrl Pts',(-0.146110491840834,1.12683595067248E-5,
0.416065504584291));
#14859=CARTESIAN_POINT('Ctrl Pts',(-0.146126798292857,0.0237518011834032,
0.414779555213666));
#14860=CARTESIAN_POINT('Ctrl Pts',(-0.140669750958991,0.0474852665485293,
0.413493605843041));
#14861=CARTESIAN_POINT('Ctrl Pts',(-0.129698698951591,0.0683144158983218,
0.412207656472415));
#14862=CARTESIAN_POINT('Ctrl Pts',(-0.107121587134001,0.111178312051432,
0.409561326593314));
#14863=CARTESIAN_POINT('Ctrl Pts',(-0.0611933749717542,0.141742803557285,
0.406914996714211));
#14864=CARTESIAN_POINT('Ctrl Pts',(-0.0129361277491455,0.146018041789781,
0.40426866683511));
#14865=CARTESIAN_POINT('Ctrl Pts',(0.0353211194734639,0.150293280022276,
0.401622336956008));
#14866=CARTESIAN_POINT('Ctrl Pts',(0.0859074017564354,0.128279264981412,
0.398976007076906));
#14867=CARTESIAN_POINT('Ctrl Pts',(0.115668581836909,0.0900521576926538,
0.396329677197804));
#14868=CARTESIAN_POINT('Ctrl Pts',(0.145429761917382,0.0518250504038959,
0.393683347318702));
#14869=CARTESIAN_POINT('Ctrl Pts',(0.154365839795359,-0.0026151491327561,
0.3910370174396));
#14870=CARTESIAN_POINT('Ctrl Pts',(0.138386632036901,-0.0483503050946702,
0.388390687560498));
#14871=CARTESIAN_POINT('Ctrl Pts',(0.122407424278443,-0.094085461056585,
0.385744357681396));
#14872=CARTESIAN_POINT('Ctrl Pts',(0.0815129308835505,-0.131115573443762,
0.383098027802294));
#14873=CARTESIAN_POINT('Ctrl Pts',(0.0344212048624006,-0.142491377230642,
0.380451697923192));
#14874=CARTESIAN_POINT('Ctrl Pts',(-0.0126705211587486,-0.153867181017521,
0.37780536804409));
#14875=CARTESIAN_POINT('Ctrl Pts',(-0.0659594798061549,-0.139588676204105,
0.375159038164988));
#14876=CARTESIAN_POINT('Ctrl Pts',(-0.101054476324393,-0.106191359083811,
0.372512708285887));
#14877=CARTESIAN_POINT('Ctrl Pts',(-0.129554902927378,-0.0790696072742943,
0.370363640385355));
#14878=CARTESIAN_POINT('Ctrl Pts',(-0.146056480184715,-0.0393390709180539,
0.368214572484823));
#14879=CARTESIAN_POINT('Ctrl Pts',(-0.146416087288192,0.000126442170093593,
0.366065504584291));
#14880=CARTESIAN_POINT('Ctrl Pts',(-0.146408012399712,0.000128195943346294,
0.358934495415711));
#14881=CARTESIAN_POINT('Ctrl Pts',(-0.146048368712081,-0.0390859965171687,
0.361069574826434));
#14882=CARTESIAN_POINT('Ctrl Pts',(-0.1297855810823,-0.0785633296797545,
0.363204654237157));
#14883=CARTESIAN_POINT('Ctrl Pts',(-0.101613371150224,-0.105657280969165,
0.36533973364788));
#14884=CARTESIAN_POINT('Ctrl Pts',(-0.066681270335132,-0.139252396162569,
0.36798712302214));
#14885=CARTESIAN_POINT('Ctrl Pts',(-0.0134387509101597,-0.153808392568477,
0.370634512396399));
#14886=CARTESIAN_POINT('Ctrl Pts',(0.0337263783221333,-0.142657876135818,
0.373281901770659));
#14887=CARTESIAN_POINT('Ctrl Pts',(0.0808915075544263,-0.13150735970316,
0.375929291144919));
#14888=CARTESIAN_POINT('Ctrl Pts',(0.12197924659404,-0.0946503304319347,
0.378576680519179));
#14889=CARTESIAN_POINT('Ctrl Pts',(0.138169300408926,-0.0489692009616054,
0.38122406989344));
#14890=CARTESIAN_POINT('Ctrl Pts',(0.154359354223812,-0.00328807149127619,
0.3838714592677));
#14891=CARTESIAN_POINT('Ctrl Pts',(0.14565172281397,0.0512171581781573,
0.38651884864196));
#14892=CARTESIAN_POINT('Ctrl Pts',(0.11603494864959,0.0895802930905963,
0.38916623801622));
#14893=CARTESIAN_POINT('Ctrl Pts',(0.0864181744852101,0.127943428003035,
0.39181362739048));
#14894=CARTESIAN_POINT('Ctrl Pts',(0.0358922575662923,0.15016446815848,
0.394461016764739));
#14895=CARTESIAN_POINT('Ctrl Pts',(-0.0123993367959677,0.146065035738641,
0.397108406138999));
#14896=CARTESIAN_POINT('Ctrl Pts',(-0.0606909311582276,0.141965603318802,
0.399755795513259));
#14897=CARTESIAN_POINT('Ctrl Pts',(-0.106748202963829,0.111545698323679,
0.40240318488752));
#14898=CARTESIAN_POINT('Ctrl Pts',(-0.129474555904152,0.0687391998188283,
0.40505057426178));
#14899=CARTESIAN_POINT('Ctrl Pts',(-0.140588317483115,0.0478057390183907,
0.406345214646423));
#14900=CARTESIAN_POINT('Ctrl Pts',(-0.146122589096428,0.0239100770892618,
0.407639855031067));
#14901=CARTESIAN_POINT('Ctrl Pts',(-0.146109756335714,8.81622270207575E-6,
0.40893449541571));
#14902=CARTESIAN_POINT('Origin',(0.,0.,0.));
#14903=CARTESIAN_POINT('',(-0.146374718215768,-0.000132229735885947,0.466065504584291));
#14904=CARTESIAN_POINT('',(-0.146375609273197,-0.000132432188538665,0.458934495415711));
#14905=CARTESIAN_POINT('',(-0.14635,-1.79227059055215E-17,0.));
#14906=CARTESIAN_POINT('Ctrl Pts',(-0.146374718215768,-0.000132229735885947,
0.466065504584291));
#14907=CARTESIAN_POINT('Ctrl Pts',(-0.146022504084922,0.0379941335185874,
0.46399086782161));
#14908=CARTESIAN_POINT('Ctrl Pts',(-0.130761950520226,0.0763703265456945,
0.46191623105893));
#14909=CARTESIAN_POINT('Ctrl Pts',(-0.103994021541854,0.103314352404769,
0.45984159429625));
#14910=CARTESIAN_POINT('Ctrl Pts',(-0.0698498419286355,0.137683154682254,
0.457195264417148));
#14911=CARTESIAN_POINT('Ctrl Pts',(-0.0169824611430249,0.153451124186949,
0.454548934538046));
#14912=CARTESIAN_POINT('Ctrl Pts',(0.030409888879481,0.143401013202843,
0.451902604658944));
#14913=CARTESIAN_POINT('Ctrl Pts',(0.0778022389019875,0.133350902218736,
0.449256274779842));
#14914=CARTESIAN_POINT('Ctrl Pts',(0.119719558161389,0.0974827107458278,
0.44660994490074));
#14915=CARTESIAN_POINT('Ctrl Pts',(0.136975630157447,0.0522138743269898,
0.443963615021638));
#14916=CARTESIAN_POINT('Ctrl Pts',(0.154231702153504,0.00694503790815254,
0.441317285142536));
#14917=CARTESIAN_POINT('Ctrl Pts',(0.146826526886218,-0.0477244434566137,
0.438670955263434));
#14918=CARTESIAN_POINT('Ctrl Pts',(0.118149569579287,-0.0867714880447125,
0.436024625384332));
#14919=CARTESIAN_POINT('Ctrl Pts',(0.0894726122723542,-0.125818532632812,
0.43337829550523));
#14920=CARTESIAN_POINT('Ctrl Pts',(0.0395238729257754,-0.149243140444243,
0.430731965626129));
#14921=CARTESIAN_POINT('Ctrl Pts',(-0.00883432462988853,-0.146323499949933,
0.428085635747027));
#14922=CARTESIAN_POINT('Ctrl Pts',(-0.0571925221855517,-0.143403859455623,
0.425439305867925));
#14923=CARTESIAN_POINT('Ctrl Pts',(-0.1039601779503,-0.114139970655572,
0.422792975988823));
#14924=CARTESIAN_POINT('Ctrl Pts',(-0.127731000096207,-0.0719263758553634,
0.420146646109721));
#14925=CARTESIAN_POINT('Ctrl Pts',(-0.139950702323481,-0.0502259249733931,
0.418786265601244));
#14926=CARTESIAN_POINT('Ctrl Pts',(-0.146093241566443,-0.0251033736724598,
0.417425885092767));
#14927=CARTESIAN_POINT('Ctrl Pts',(-0.146110491840834,1.12683595067248E-5,
0.416065504584291));
#14928=CARTESIAN_POINT('Ctrl Pts',(-0.146109756335714,8.81622270207575E-6,
0.40893449541571));
#14929=CARTESIAN_POINT('Ctrl Pts',(-0.146096347589706,-0.0249652282079418,
0.410287244405327));
#14930=CARTESIAN_POINT('Ctrl Pts',(-0.140026707259891,-0.049945385460595,
0.411639993394943));
#14931=CARTESIAN_POINT('Ctrl Pts',(-0.127937780377622,-0.0715588049813403,
0.412992742384559));
#14932=CARTESIAN_POINT('Ctrl Pts',(-0.104279217835726,-0.113857219262079,
0.415640131758819));
#14933=CARTESIAN_POINT('Ctrl Pts',(-0.0575666586768896,-0.14326095580898,
0.41828752113308));
#14934=CARTESIAN_POINT('Ctrl Pts',(-0.00919685447762893,-0.146301592903247,
0.42093491050734));
#14935=CARTESIAN_POINT('Ctrl Pts',(0.039172949721632,-0.149342229997515,
0.4235822998816));
#14936=CARTESIAN_POINT('Ctrl Pts',(0.089199998961318,-0.126019767639148,
0.426229689255859));
#14937=CARTESIAN_POINT('Ctrl Pts',(0.117969334952632,-0.0870170915920772,
0.428877078630119));
#14938=CARTESIAN_POINT('Ctrl Pts',(0.146738670943946,-0.0480144155450057,
0.431524468004379));
#14939=CARTESIAN_POINT('Ctrl Pts',(0.154250293686888,0.00666847419077017,
0.43417185737864));
#14940=CARTESIAN_POINT('Ctrl Pts',(0.137063494116028,0.051984005222912,
0.4368192467529));
#14941=CARTESIAN_POINT('Ctrl Pts',(0.119876694545168,0.0972995362550541,
0.43946663612716));
#14942=CARTESIAN_POINT('Ctrl Pts',(0.0779914726605056,0.133247708583562,
0.442114025501419));
#14943=CARTESIAN_POINT('Ctrl Pts',(0.0305934116013849,0.143362412733947,
0.444761414875679));
#14944=CARTESIAN_POINT('Ctrl Pts',(-0.0168046494577345,0.153477116884331,
0.447408804249939));
#14945=CARTESIAN_POINT('Ctrl Pts',(-0.0697155496913122,0.137758352856595,
0.4500561936242));
#14946=CARTESIAN_POINT('Ctrl Pts',(-0.103903378920715,0.103406122000434,
0.45270358299846));
#14947=CARTESIAN_POINT('Ctrl Pts',(-0.130724942802416,0.0764555792150183,
0.45478055380421));
#14948=CARTESIAN_POINT('Ctrl Pts',(-0.146022533856355,0.0380362146017157,
0.45685752460996));
#14949=CARTESIAN_POINT('Ctrl Pts',(-0.146375609273197,-0.000132432188538665,
0.458934495415711));
#14950=CARTESIAN_POINT('Origin',(0.,0.,0.));
#14951=CARTESIAN_POINT('',(-0.146548608312775,6.99729089778146E-5,0.516065504584291));
#14952=CARTESIAN_POINT('',(-0.146550766805835,6.86360251013434E-5,0.508934495415711));
#14953=CARTESIAN_POINT('',(-0.14635,-1.79227059055215E-17,0.));
#14954=CARTESIAN_POINT('Ctrl Pts',(-0.146548608312775,6.99729089778146E-5,
0.516065504584291));
#14955=CARTESIAN_POINT('Ctrl Pts',(-0.146572081366671,0.00404546554386884,
0.515848510308657));
#14956=CARTESIAN_POINT('Ctrl Pts',(-0.146424333269732,0.00801918670503405,
0.515631516033023));
#14957=CARTESIAN_POINT('Ctrl Pts',(-0.146099725131082,0.0119784074854107,
0.51541452175739));
#14958=CARTESIAN_POINT('Ctrl Pts',(-0.142141002193345,0.06026265009261,
0.512768191878288));
#14959=CARTESIAN_POINT('Ctrl Pts',(-0.111878319621163,0.106390286678145,
0.510121861999186));
#14960=CARTESIAN_POINT('Ctrl Pts',(-0.069163383343408,0.129247972261684,
0.507475532120084));
#14961=CARTESIAN_POINT('Ctrl Pts',(-0.0264484470656534,0.152105657845224,
0.504829202240982));
#14962=CARTESIAN_POINT('Ctrl Pts',(0.0287187429176733,0.151693392426768,
0.50218287236188));
#14963=CARTESIAN_POINT('Ctrl Pts',(0.07108729581893,0.128199876374419,0.499536542482778));
#14964=CARTESIAN_POINT('Ctrl Pts',(0.113455848720186,0.10470636032207,0.496890212603677));
#14965=CARTESIAN_POINT('Ctrl Pts',(0.143025764539373,0.0581315936358261,
0.494243882724575));
#14966=CARTESIAN_POINT('Ctrl Pts',(0.146262427589597,0.00979357977770552,
0.491597552845473));
#14967=CARTESIAN_POINT('Ctrl Pts',(0.149499090639821,-0.0385444340804161,
0.488951222966371));
#14968=CARTESIAN_POINT('Ctrl Pts',(0.126402500921083,-0.0886456951104151,
0.486304893087269));
#14969=CARTESIAN_POINT('Ctrl Pts',(0.087544330920799,-0.117578067907642,
0.483658563208167));
#14970=CARTESIAN_POINT('Ctrl Pts',(0.0486861609205161,-0.146510440704867,
0.481012233329065));
#14971=CARTESIAN_POINT('Ctrl Pts',(-0.00593358936131212,-0.154273925269321,
0.478365903449963));
#14972=CARTESIAN_POINT('Ctrl Pts',(-0.0513146009011563,-0.137315052574797,
0.475719573570861));
#14973=CARTESIAN_POINT('Ctrl Pts',(-0.0966956124410008,-0.120356179880273,
0.473073243691759));
#14974=CARTESIAN_POINT('Ctrl Pts',(-0.132837885238862,-0.078674949926771,
0.470426913812657));
#14975=CARTESIAN_POINT('Ctrl Pts',(-0.14319853241738,-0.0313495174248821,
0.467780583933555));
#14976=CARTESIAN_POINT('Ctrl Pts',(-0.145436768368387,-0.0211256884885646,
0.467208890817134));
#14977=CARTESIAN_POINT('Ctrl Pts',(-0.146471775395962,-0.0106384445195334,
0.466637197700712));
#14978=CARTESIAN_POINT('Ctrl Pts',(-0.146374718215768,-0.000132229735885947,
0.466065504584291));
#14979=CARTESIAN_POINT('Ctrl Pts',(-0.146375609273197,-0.000132432188538665,
0.458934495415711));
#14980=CARTESIAN_POINT('Ctrl Pts',(-0.146472577787773,-0.0106150565970108,
0.45950491398422));
#14981=CARTESIAN_POINT('Ctrl Pts',(-0.145442327125792,-0.021078770125739,
0.46007533255273));
#14982=CARTESIAN_POINT('Ctrl Pts',(-0.143213999951756,-0.0312807998000163,
0.460645751121239));
#14983=CARTESIAN_POINT('Ctrl Pts',(-0.132872033528166,-0.0786297930597184,
0.463293140495499));
#14984=CARTESIAN_POINT('Ctrl Pts',(-0.0967233424557573,-0.120342081894533,
0.465940529869759));
#14985=CARTESIAN_POINT('Ctrl Pts',(-0.0513258840937604,-0.13731129538499,
0.46858791924402));
#14986=CARTESIAN_POINT('Ctrl Pts',(-0.00592842573176499,-0.154280508875447,
0.47123530861828));
#14987=CARTESIAN_POINT('Ctrl Pts',(0.0487177999198187,-0.146506647021548,
0.47388269799254));
#14988=CARTESIAN_POINT('Ctrl Pts',(0.0875820145025328,-0.117550537871965,
0.476530087366799));
#14989=CARTESIAN_POINT('Ctrl Pts',(0.126446229085248,-0.0885944287223814,
0.47917747674106));
#14990=CARTESIAN_POINT('Ctrl Pts',(0.149528432599094,-0.0384560722771122,
0.481824866115319));
#14991=CARTESIAN_POINT('Ctrl Pts',(0.146255790172295,0.0098985887573764,
0.484472255489579));
#14992=CARTESIAN_POINT('Ctrl Pts',(0.142983147745498,0.0582532497918637,
0.487119644863839));
#14993=CARTESIAN_POINT('Ctrl Pts',(0.113355659378058,0.10482421541557,0.4897670342381));
#14994=CARTESIAN_POINT('Ctrl Pts',(0.0709442366160257,0.128279591164298,
0.49241442361236));
#14995=CARTESIAN_POINT('Ctrl Pts',(0.0285328138539934,0.151734966913027,
0.49506181298662));
#14996=CARTESIAN_POINT('Ctrl Pts',(-0.0266625433026316,0.152074752786777,
0.497709202360879));
#14997=CARTESIAN_POINT('Ctrl Pts',(-0.0693595260588707,0.129143309401606,
0.500356591735139));
#14998=CARTESIAN_POINT('Ctrl Pts',(-0.11205650881511,0.106211866016435,
0.503003981109399));
#14999=CARTESIAN_POINT('Ctrl Pts',(-0.142255117170964,0.060009193372344,
0.505651370483659));
#15000=CARTESIAN_POINT('Ctrl Pts',(-0.146122837288996,0.0116984888307781,
0.50829875985792));
#15001=CARTESIAN_POINT('Ctrl Pts',(-0.146432431239741,0.00783142983325791,
0.508510671710517));
#15002=CARTESIAN_POINT('Ctrl Pts',(-0.14657331536999,0.00395086404934249,
0.508722583563114));
#15003=CARTESIAN_POINT('Ctrl Pts',(-0.146550766805835,6.86360251013434E-5,
0.508934495415711));
#15004=CARTESIAN_POINT('Origin',(0.,0.,0.));
#15005=CARTESIAN_POINT('',(-0.146165204287215,8.83645032875094E-5,0.566065504584291));
#15006=CARTESIAN_POINT('',(-0.146168951232552,9.12430751481418E-5,0.558934495415711));
#15007=CARTESIAN_POINT('',(-0.14635,-1.79227059055215E-17,0.));
#15008=CARTESIAN_POINT('Ctrl Pts',(-0.146165204287215,8.83645032875094E-5,
0.566065504584291));
#15009=CARTESIAN_POINT('Ctrl Pts',(-0.146267412293664,0.0186373661349918,
0.565059822916602));
#15010=CARTESIAN_POINT('Ctrl Pts',(-0.142994166834961,0.0371516370495788,
0.564054141248913));
#15011=CARTESIAN_POINT('Ctrl Pts',(-0.136179985035193,0.0542551712289143,
0.563048459581224));
#15012=CARTESIAN_POINT('Ctrl Pts',(-0.118249288396568,0.0992610562830057,
0.560402129702122));
#15013=CARTESIAN_POINT('Ctrl Pts',(-0.0758005933416487,0.134498778989873,
0.55775579982302));
#15014=CARTESIAN_POINT('Ctrl Pts',(-0.0282633354322908,0.143839479279877,
0.555109469943918));
#15015=CARTESIAN_POINT('Ctrl Pts',(0.0192739224770691,0.153180179569881,
0.552463140064816));
#15016=CARTESIAN_POINT('Ctrl Pts',(0.0718997432408687,0.136623857443018,
0.549816810185715));
#15017=CARTESIAN_POINT('Ctrl Pts',(0.105526460745998,0.101748602013432,
0.547170480306613));
#15018=CARTESIAN_POINT('Ctrl Pts',(0.139153178251127,0.0668733465838454,
0.544524150427511));
#15019=CARTESIAN_POINT('Ctrl Pts',(0.153780792497586,0.0136791578515372,
0.541877820548409));
#15020=CARTESIAN_POINT('Ctrl Pts',(0.142714014311998,-0.0334861471092027,
0.539231490669307));
#15021=CARTESIAN_POINT('Ctrl Pts',(0.13164723612641,-0.0806514520699426,
0.536585160790205));
#15022=CARTESIAN_POINT('Ctrl Pts',(0.0948860655087725,-0.121787873259113,
0.533938830911103));
#15023=CARTESIAN_POINT('Ctrl Pts',(0.0492566686055307,-0.138066623508903,
0.531292501032001));
#15024=CARTESIAN_POINT('Ctrl Pts',(0.00362727170228945,-0.154345373758693,
0.528646171152899));
#15025=CARTESIAN_POINT('Ctrl Pts',(-0.050870351486557,-0.145766453069103,
0.525999841273797));
#15026=CARTESIAN_POINT('Ctrl Pts',(-0.089291781429334,-0.116256568409877,
0.523353511394695));
#15027=CARTESIAN_POINT('Ctrl Pts',(-0.124562723435938,-0.0891664410515947,
0.520924175791227));
#15028=CARTESIAN_POINT('Ctrl Pts',(-0.146285818313441,-0.0444372186796531,
0.518494840187759));
#15029=CARTESIAN_POINT('Ctrl Pts',(-0.146548608312775,6.99729089778146E-5,
0.516065504584291));
#15030=CARTESIAN_POINT('Ctrl Pts',(-0.146550766805835,6.86360251013434E-5,
0.508934495415711));
#15031=CARTESIAN_POINT('Ctrl Pts',(-0.146291618860727,-0.0445493453248537,
0.511369972937373));
#15032=CARTESIAN_POINT('Ctrl Pts',(-0.124445252016267,-0.0893868858389474,
0.513805450459036));
#15033=CARTESIAN_POINT('Ctrl Pts',(-0.0890226177929609,-0.116463349340462,
0.516240927980699));
#15034=CARTESIAN_POINT('Ctrl Pts',(-0.0505178462986829,-0.145895746531099,
0.518888317354959));
#15035=CARTESIAN_POINT('Ctrl Pts',(0.00402852857008221,-0.154341804473332,
0.52153570672922));
#15036=CARTESIAN_POINT('Ctrl Pts',(0.0496314652424392,-0.137932794781367,
0.52418309610348));
#15037=CARTESIAN_POINT('Ctrl Pts',(0.0952344019147948,-0.121523785089403,
0.52683048547774));
#15038=CARTESIAN_POINT('Ctrl Pts',(0.131893900390741,-0.0802597077632436,
0.529477874851999));
#15039=CARTESIAN_POINT('Ctrl Pts',(0.14281802728161,-0.0330416298281342,
0.532125264226259));
#15040=CARTESIAN_POINT('Ctrl Pts',(0.153742154172479,0.0141764481069759,
0.53477265360052));
#15041=CARTESIAN_POINT('Ctrl Pts',(0.138930909478268,0.0673485266510362,
0.53742004297478));
#15042=CARTESIAN_POINT('Ctrl Pts',(0.105168604077417,0.102119062543277,
0.54006743234904));
#15043=CARTESIAN_POINT('Ctrl Pts',(0.0714062986765666,0.136889598435517,
0.5427148217233));
#15044=CARTESIAN_POINT('Ctrl Pts',(0.018692932569077,0.153258591675938,
0.545362211097559));
#15045=CARTESIAN_POINT('Ctrl Pts',(-0.0288260648428939,0.143728202535144,
0.548009600471819));
#15046=CARTESIAN_POINT('Ctrl Pts',(-0.0763450622548654,0.13419781339435,
0.550656989846079));
#15047=CARTESIAN_POINT('Ctrl Pts',(-0.118669690971318,0.0987680418723385,
0.55330437922034));
#15048=CARTESIAN_POINT('Ctrl Pts',(-0.136413096952957,0.0536675432455532,
0.5559517685946));
#15049=CARTESIAN_POINT('Ctrl Pts',(-0.143076734904351,0.036729792140314,
0.556946010868304));
#15050=CARTESIAN_POINT('Ctrl Pts',(-0.146273385252938,0.0184280612467595,
0.557940253142007));
#15051=CARTESIAN_POINT('Ctrl Pts',(-0.146168951232552,9.12430751481418E-5,
0.558934495415711));
#15052=CARTESIAN_POINT('Origin',(0.,0.,0.));
#15053=CARTESIAN_POINT('',(-0.146227179098081,-0.000117664897458569,0.616065504584291));
#15054=CARTESIAN_POINT('',(-0.146218520919543,-0.000115076211918358,0.608934495415711));
#15055=CARTESIAN_POINT('',(-0.14635,-1.79227059055215E-17,0.));
#15056=CARTESIAN_POINT('Ctrl Pts',(-0.146227179098081,-0.000117664897458569,
0.616065504584291));
#15057=CARTESIAN_POINT('Ctrl Pts',(-0.145977603365176,0.0329427899635141,
0.614271135524546));
#15058=CARTESIAN_POINT('Ctrl Pts',(-0.134874795495675,0.0661550248562671,
0.612476766464802));
#15059=CARTESIAN_POINT('Ctrl Pts',(-0.114309815624116,0.091770790457776,
0.610682397405058));
#15060=CARTESIAN_POINT('Ctrl Pts',(-0.0839806476072558,0.129548841477563,
0.608036067525956));
#15061=CARTESIAN_POINT('Ctrl Pts',(-0.0330710111925292,0.150804375664025,
0.605389737646855));
#15062=CARTESIAN_POINT('Ctrl Pts',(0.0151169520838501,0.145808400611758,
0.602743407767753));
#15063=CARTESIAN_POINT('Ctrl Pts',(0.0633049153602295,0.140812425559491,
0.600097077888651));
#15064=CARTESIAN_POINT('Ctrl Pts',(0.108771205498262,0.109564941268491,
0.597450748009549));
#15065=CARTESIAN_POINT('Ctrl Pts',(0.130705186191441,0.0663684129079872,
0.594804418130447));
#15066=CARTESIAN_POINT('Ctrl Pts',(0.152639166884621,0.023171884547483,
0.592158088251345));
#15067=CARTESIAN_POINT('Ctrl Pts',(0.151040838132949,-0.0319736878825246,
0.589511758372243));
#15068=CARTESIAN_POINT('Ctrl Pts',(0.126641780152193,-0.0738273082886534,
0.586865428493141));
#15069=CARTESIAN_POINT('Ctrl Pts',(0.102242722171437,-0.115680928694782,
0.584219098614039));
#15070=CARTESIAN_POINT('Ctrl Pts',(0.0550429349615966,-0.14424259707703,
0.581572768734937));
#15071=CARTESIAN_POINT('Ctrl Pts',(0.00664650371163741,-0.14643918846291,
0.578926438855836));
#15072=CARTESIAN_POINT('Ctrl Pts',(-0.0417499275383225,-0.148635779848789,
0.576280108976733));
#15073=CARTESIAN_POINT('Ctrl Pts',(-0.0913430028284016,-0.1244672942383,
0.573633779097631));
#15074=CARTESIAN_POINT('Ctrl Pts',(-0.119433191362276,-0.0849960277323969,
0.570987449218529));
#15075=CARTESIAN_POINT('Ctrl Pts',(-0.136848298201485,-0.0605249807527623,
0.569346801007117));
#15076=CARTESIAN_POINT('Ctrl Pts',(-0.145998464265635,-0.0301720919893573,
0.567706152795704));
#15077=CARTESIAN_POINT('Ctrl Pts',(-0.146165204287215,8.83645032875094E-5,
0.566065504584291));
#15078=CARTESIAN_POINT('Ctrl Pts',(-0.146168951232552,9.12430751481418E-5,
0.558934495415711));
#15079=CARTESIAN_POINT('Ctrl Pts',(-0.145995306636495,-0.0303977620653178,
0.560587642516267));
#15080=CARTESIAN_POINT('Ctrl Pts',(-0.136695352934655,-0.0609837708898569,
0.562240789616823));
#15081=CARTESIAN_POINT('Ctrl Pts',(-0.119031718004195,-0.0855580991331628,
0.563893936717379));
#15082=CARTESIAN_POINT('Ctrl Pts',(-0.090744749826965,-0.124912017153538,
0.566541326091639));
#15083=CARTESIAN_POINT('Ctrl Pts',(-0.0410086302256792,-0.148848627462727,
0.5691887154659));
#15084=CARTESIAN_POINT('Ctrl Pts',(0.00739494322942312,-0.146403732988417,
0.57183610484016));
#15085=CARTESIAN_POINT('Ctrl Pts',(0.0557985166845234,-0.143958838514108,
0.57448349421442));
#15086=CARTESIAN_POINT('Ctrl Pts',(0.10286954399344,-0.1151324392563,0.57713088358868));
#15087=CARTESIAN_POINT('Ctrl Pts',(0.127047076753504,-0.0731285067993286,
0.579778272962939));
#15088=CARTESIAN_POINT('Ctrl Pts',(0.151224609513568,-0.031124574342357,
0.5824256623372));
#15089=CARTESIAN_POINT('Ctrl Pts',(0.15250864772478,0.0240568913137802,
0.58507305171146));
#15090=CARTESIAN_POINT('Ctrl Pts',(0.130311035929276,0.0671399443948921,
0.58772044108572));
#15091=CARTESIAN_POINT('Ctrl Pts',(0.108113424133771,0.110222997476006,
0.59036783045998));
#15092=CARTESIAN_POINT('Ctrl Pts',(0.0624341623315493,0.141207637982093,
0.593015219834239));
#15093=CARTESIAN_POINT('Ctrl Pts',(0.0141966988324609,0.145901308974836,
0.595662609208499));
#15094=CARTESIAN_POINT('Ctrl Pts',(-0.0340407646666261,0.150594979967579,
0.598309998582759));
#15095=CARTESIAN_POINT('Ctrl Pts',(-0.0848364298625779,0.128997681446978,
0.60095738795702));
#15096=CARTESIAN_POINT('Ctrl Pts',(-0.114923272877171,0.091002085522857,
0.60360477733128));
#15097=CARTESIAN_POINT('Ctrl Pts',(-0.135113526827902,0.0655045372973676,
0.60538135002609));
#15098=CARTESIAN_POINT('Ctrl Pts',(-0.14597798884013,0.0326223532682757,
0.6071579227209));
#15099=CARTESIAN_POINT('Ctrl Pts',(-0.146218520919543,-0.000115076211918358,
0.608934495415711));
#15100=CARTESIAN_POINT('Origin',(0.,0.,0.));
#15101=CARTESIAN_POINT('',(-0.146586033401767,-2.15382961294558E-5,0.66606550458429));
#15102=CARTESIAN_POINT('',(-0.146582846697157,-3.00215943766004E-5,0.65893449541571));
#15103=CARTESIAN_POINT('',(-0.14635,-1.79227059055215E-17,0.));
#15104=CARTESIAN_POINT('Ctrl Pts',(-0.146586033401767,-2.15382961294558E-5,
0.66606550458429));
#15105=CARTESIAN_POINT('Ctrl Pts',(-0.146488810225965,0.0472697707580183,
0.663482448132491));
#15106=CARTESIAN_POINT('Ctrl Pts',(-0.121516563758978,0.0946492637554097,
0.660899391680692));
#15107=CARTESIAN_POINT('Ctrl Pts',(-0.0824084263440199,0.121233094478226,
0.658316335228893));
#15108=CARTESIAN_POINT('Ctrl Pts',(-0.0423423130056393,0.148468111155377,
0.655670005349791));
#15109=CARTESIAN_POINT('Ctrl Pts',(0.0125607065496858,0.153876184485078,
0.653023675470689));
#15110=CARTESIAN_POINT('Ctrl Pts',(0.0571706564953393,0.134981954220393,
0.650377345591587));
#15111=CARTESIAN_POINT('Ctrl Pts',(0.101780606440992,0.116087723955709,
0.647731015712485));
#15112=CARTESIAN_POINT('Ctrl Pts',(0.136097486776972,0.0728911900966409,
0.645084685833384));
#15113=CARTESIAN_POINT('Ctrl Pts',(0.144413921474191,0.0251640857912735,
0.642438355954282));
#15114=CARTESIAN_POINT('Ctrl Pts',(0.152730356171409,-0.0225630185140953,
0.63979202607518));
#15115=CARTESIAN_POINT('Ctrl Pts',(0.135046345229863,-0.0748206932657649,
0.637145696196077));
#15116=CARTESIAN_POINT('Ctrl Pts',(0.0994561386758346,-0.10768977857233,
0.634499366316975));
#15117=CARTESIAN_POINT('Ctrl Pts',(0.0638659321218069,-0.140558863878895,
0.631853036437873));
#15118=CARTESIAN_POINT('Ctrl Pts',(0.0103695299552984,-0.154039359740357,
0.629206706558772));
#15119=CARTESIAN_POINT('Ctrl Pts',(-0.0365469229059137,-0.141961031115491,
0.62656037667967));
#15120=CARTESIAN_POINT('Ctrl Pts',(-0.0834633757671259,-0.129882702490626,
0.623914046800568));
#15121=CARTESIAN_POINT('Ctrl Pts',(-0.123799879323041,-0.0922455493794331,
0.621267716921466));
#15122=CARTESIAN_POINT('Ctrl Pts',(-0.139093781291504,-0.0462766888972804,
0.618621387042364));
#15123=CARTESIAN_POINT('Ctrl Pts',(-0.14401750805555,-0.0314774500153124,
0.617769426223006));
#15124=CARTESIAN_POINT('Ctrl Pts',(-0.14634567687575,-0.0158146654998378,
0.616917465403648));
#15125=CARTESIAN_POINT('Ctrl Pts',(-0.146227179098081,-0.000117664897458569,
0.616065504584291));
#15126=CARTESIAN_POINT('Ctrl Pts',(-0.146218520919543,-0.000115076211918358,
0.608934495415711));
#15127=CARTESIAN_POINT('Ctrl Pts',(-0.1463364217222,-0.0161618722236638,
0.60980531209516));
#15128=CARTESIAN_POINT('Ctrl Pts',(-0.143901781624712,-0.032173889023867,
0.61067612877461));
#15129=CARTESIAN_POINT('Ctrl Pts',(-0.138761720114909,-0.0472643972675185,
0.611546945454059));
#15130=CARTESIAN_POINT('Ctrl Pts',(-0.123135303504819,-0.0931413908061287,
0.614194334828319));
#15131=CARTESIAN_POINT('Ctrl Pts',(-0.0825044494514074,-0.130501484555709,
0.616841724202579));
#15132=CARTESIAN_POINT('Ctrl Pts',(-0.0354801761942514,-0.142231836504824,
0.619489113576839));
#15133=CARTESIAN_POINT('Ctrl Pts',(0.0115440970629072,-0.15396218845394,
0.6221365029511));
#15134=CARTESIAN_POINT('Ctrl Pts',(0.0649617895238099,-0.140062798602586,
0.624783892325359));
#15135=CARTESIAN_POINT('Ctrl Pts',(0.100304854137336,-0.106900301471969,
0.627431281699619));
#15136=CARTESIAN_POINT('Ctrl Pts',(0.135647918750861,-0.0737378043413545,
0.630078671073879));
#15137=CARTESIAN_POINT('Ctrl Pts',(0.15291635551701,-0.0213121999314781,
0.63272606044814));
#15138=CARTESIAN_POINT('Ctrl Pts',(0.144200333369931,0.026362891994447,
0.6353734498224));
#15139=CARTESIAN_POINT('Ctrl Pts',(0.135484311222852,0.0740379839203748,
0.63802083919666));
#15140=CARTESIAN_POINT('Ctrl Pts',(0.100783830162543,0.11696256336235,0.640668228570919));
#15141=CARTESIAN_POINT('Ctrl Pts',(0.055993492972559,0.135474968031154,
0.643315617945179));
#15142=CARTESIAN_POINT('Ctrl Pts',(0.0112031557825773,0.153987372699956,
0.64596300731944));
#15143=CARTESIAN_POINT('Ctrl Pts',(-0.04367703753708,0.148087602595587,
0.6486103966937));
#15144=CARTESIAN_POINT('Ctrl Pts',(-0.0835091394177698,0.120478055479053,
0.65125778606796));
#15145=CARTESIAN_POINT('Ctrl Pts',(-0.122009894390588,0.0937913289882395,
0.653816689183877));
#15146=CARTESIAN_POINT('Ctrl Pts',(-0.146451680634158,0.0468218259492564,
0.656375592299793));
#15147=CARTESIAN_POINT('Ctrl Pts',(-0.146582846697157,-3.00215943766004E-5,
0.65893449541571));
#15148=CARTESIAN_POINT('Origin',(0.,0.,0.));
#15149=CARTESIAN_POINT('',(-0.146290249280603,0.000131112932912382,0.716065504584291));
#15150=CARTESIAN_POINT('',(-0.146307221518699,0.000133045872591754,0.708934495415711));
#15151=CARTESIAN_POINT('',(-0.14635,-1.79227059055215E-17,0.));
#15152=CARTESIAN_POINT('Ctrl Pts',(-0.146290249280603,0.000131112932912382,
0.716065504584291));
#15153=CARTESIAN_POINT('Ctrl Pts',(-0.146406294125046,0.0134819654399978,
0.715340090619538));
#15154=CARTESIAN_POINT('Ctrl Pts',(-0.144729088574721,0.0268041890186768,
0.714614676654786));
#15155=CARTESIAN_POINT('Ctrl Pts',(-0.141142411757643,0.0395908011096033,
0.713889262690033));
#15156=CARTESIAN_POINT('Ctrl Pts',(-0.128058117149462,0.0862367098911347,
0.711242932810931));
#15157=CARTESIAN_POINT('Ctrl Pts',(-0.0895623832093418,0.125754646095387,
0.708596602931829));
#15158=CARTESIAN_POINT('Ctrl Pts',(-0.0432753130058998,0.140056628595385,
0.705950273052727));
#15159=CARTESIAN_POINT('Ctrl Pts',(0.00301175719754219,0.154358611095384,
0.703303943173625));
#15160=CARTESIAN_POINT('Ctrl Pts',(0.0570901636643063,0.143444639891129,
0.700657613294523));
#15161=CARTESIAN_POINT('Ctrl Pts',(0.0942073689518517,0.11231021130972,
0.698011283415421));
#15162=CARTESIAN_POINT('Ctrl Pts',(0.131324574239397,0.0811757827283121,
0.695364953536319));
#15163=CARTESIAN_POINT('Ctrl Pts',(0.151480578347723,0.0298208967697505,
0.692718623657217));
#15164=CARTESIAN_POINT('Ctrl Pts',(0.145449661086834,-0.0182485073085286,
0.690072293778115));
#15165=CARTESIAN_POINT('Ctrl Pts',(0.139418743825945,-0.0663179113868083,
0.687425963899014));
#15166=CARTESIAN_POINT('Ctrl Pts',(0.107200905195838,-0.111101833584806,
0.684779634019911));
#15167=CARTESIAN_POINT('Ctrl Pts',(0.0635427568131047,-0.132101968137704,
0.68213330414081));
#15168=CARTESIAN_POINT('Ctrl Pts',(0.0198846084303716,-0.153102102690602,
0.679486974261708));
#15169=CARTESIAN_POINT('Ctrl Pts',(-0.0352138497049885,-0.150318449598402,
0.676840644382606));
#15170=CARTESIAN_POINT('Ctrl Pts',(-0.0765331864534889,-0.125025130675956,
0.674194314503504));
#15171=CARTESIAN_POINT('Ctrl Pts',(-0.117852523201989,-0.0997318117535095,
0.671547984624402));
#15172=CARTESIAN_POINT('Ctrl Pts',(-0.14539273856363,-0.0519288270008166,
0.6689016547453));
#15173=CARTESIAN_POINT('Ctrl Pts',(-0.146548242683733,-0.00349635461217019,
0.666255324866198));
#15174=CARTESIAN_POINT('Ctrl Pts',(-0.146575870647472,-0.00233834005587287,
0.666192051438896));
#15175=CARTESIAN_POINT('Ctrl Pts',(-0.146588414938392,-0.00117996563262623,
0.666128778011593));
#15176=CARTESIAN_POINT('Ctrl Pts',(-0.146586033401767,-2.15382961294558E-5,
0.66606550458429));
#15177=CARTESIAN_POINT('Ctrl Pts',(-0.146582846697157,-3.00215943766004E-5,
0.65893449541571));
#15178=CARTESIAN_POINT('Ctrl Pts',(-0.146587382388275,-0.00165014728799839,
0.659022981674053));
#15179=CARTESIAN_POINT('Ctrl Pts',(-0.146562848415234,-0.00327013229389975,
0.659111467932396));
#15180=CARTESIAN_POINT('Ctrl Pts',(-0.146508820881567,-0.00488913307276392,
0.659199954190739));
#15181=CARTESIAN_POINT('Ctrl Pts',(-0.144892390022949,-0.0533274503793473,
0.661847343564999));
#15182=CARTESIAN_POINT('Ctrl Pts',(-0.116875517863988,-0.100884760863813,
0.66449473293926));
#15183=CARTESIAN_POINT('Ctrl Pts',(-0.0752913709948059,-0.125777373450206,
0.66714212231352));
#15184=CARTESIAN_POINT('Ctrl Pts',(-0.0337072241256252,-0.150669986036599,
0.66978951168778));
#15185=CARTESIAN_POINT('Ctrl Pts',(0.021444197453776,-0.15289790072492,
0.672436901062039));
#15186=CARTESIAN_POINT('Ctrl Pts',(0.0649007096996251,-0.131440618146733,
0.675084290436299));
#15187=CARTESIAN_POINT('Ctrl Pts',(0.108357221945475,-0.109983335568545,
0.677731679810559));
#15188=CARTESIAN_POINT('Ctrl Pts',(0.140118824857774,-0.0648408557238465,
0.68037906918482));
#15189=CARTESIAN_POINT('Ctrl Pts',(0.145637072805965,-0.0166907532130915,
0.68302645855908));
#15190=CARTESIAN_POINT('Ctrl Pts',(0.151155320754156,0.031459349297663,
0.68567384793334));
#15191=CARTESIAN_POINT('Ctrl Pts',(0.130430213738242,0.0826170744744734,
0.688321237307599));
#15192=CARTESIAN_POINT('Ctrl Pts',(0.0929549153570804,0.113349556369966,
0.690968626681859));
#15193=CARTESIAN_POINT('Ctrl Pts',(0.0554796169759186,0.14408203826546,
0.693616016056119));
#15194=CARTESIAN_POINT('Ctrl Pts',(0.00125412722950909,0.154389276879634,
0.69626340543038));
#15195=CARTESIAN_POINT('Ctrl Pts',(-0.0448834941801804,0.139550027475769,
0.69891079480464));
#15196=CARTESIAN_POINT('Ctrl Pts',(-0.0910211155898686,0.124710778071904,
0.7015581841789));
#15197=CARTESIAN_POINT('Ctrl Pts',(-0.129070868662838,0.0847250406500019,
0.704205573553159));
#15198=CARTESIAN_POINT('Ctrl Pts',(-0.141604011991841,0.0379083368947344,
0.706852962927419));
#15199=CARTESIAN_POINT('Ctrl Pts',(-0.144888775625201,0.0256383259412015,
0.707546807090183));
#15200=CARTESIAN_POINT('Ctrl Pts',(-0.146420824649375,0.0128991016161637,
0.708240651252947));
#15201=CARTESIAN_POINT('Ctrl Pts',(-0.146307221518699,0.000133045872591754,
0.708934495415711));
#15202=CARTESIAN_POINT('Origin',(0.,0.,0.));
#15203=CARTESIAN_POINT('',(-0.1461301977291,-5.61458017395017E-5,0.766065504584291));
#15204=CARTESIAN_POINT('',(-0.14612241379348,-4.54149644099216E-5,0.758934495415711));
#15205=CARTESIAN_POINT('',(-0.14635,-1.79227059055215E-17,0.));
#15206=CARTESIAN_POINT('Ctrl Pts',(-0.1461301977291,-5.61458017395017E-5,
0.766065504584291));
#15207=CARTESIAN_POINT('Ctrl Pts',(-0.14603380141711,0.0278870014676159,
0.764551403227483));
#15208=CARTESIAN_POINT('Ctrl Pts',(-0.138327245009168,0.0558793842949389,
0.763037301870675));
#15209=CARTESIAN_POINT('Ctrl Pts',(-0.123350675409043,0.079203679241543,
0.761523200513867));
#15210=CARTESIAN_POINT('Ctrl Pts',(-0.0971747899961838,0.119969628197767,
0.758876870634766));
#15211=CARTESIAN_POINT('Ctrl Pts',(-0.048790709571801,0.146475657227381,
0.756230540755664));
#15212=CARTESIAN_POINT('Ctrl Pts',(-0.000344588961360588,0.146589539830481,
0.753584210876561));
#15213=CARTESIAN_POINT('Ctrl Pts',(0.0481015316490792,0.14670342243358,
0.750937880997459));
#15214=CARTESIAN_POINT('Ctrl Pts',(0.0966096924455767,0.120425158610167,
0.748291551118357));
#15215=CARTESIAN_POINT('Ctrl Pts',(0.122976945064223,0.0797827231418903,
0.745645221239255));
#15216=CARTESIAN_POINT('Ctrl Pts',(0.149344197682869,0.0391402876736125,
0.742998891360154));
#15217=CARTESIAN_POINT('Ctrl Pts',(0.153570542123663,-0.01586631943953,
0.740352561481052));
#15218=CARTESIAN_POINT('Ctrl Pts',(0.133721514043982,-0.0600597087159893,
0.73770623160195));
#15219=CARTESIAN_POINT('Ctrl Pts',(0.113872485964301,-0.104253097992448,
0.735059901722848));
#15220=CARTESIAN_POINT('Ctrl Pts',(0.0699480853641458,-0.137633269432224,
0.732413571843746));
#15221=CARTESIAN_POINT('Ctrl Pts',(0.0220532014503509,-0.144921593405036,
0.729767241964644));
#15222=CARTESIAN_POINT('Ctrl Pts',(-0.0258416824634434,-0.152209917377848,
0.727120912085542));
#15223=CARTESIAN_POINT('Ctrl Pts',(-0.0777070496908773,-0.133406393883698,
0.724474582206441));
#15224=CARTESIAN_POINT('Ctrl Pts',(-0.109803305666473,-0.0971176914572187,
0.721828252327339));
#15225=CARTESIAN_POINT('Ctrl Pts',(-0.133101311474982,-0.0707764758164216,
0.71990733641299));
#15226=CARTESIAN_POINT('Ctrl Pts',(-0.14598295937539,-0.0352223077304616,
0.71798642049864));
#15227=CARTESIAN_POINT('Ctrl Pts',(-0.146290249280603,0.000131112932912382,
0.716065504584291));
#15228=CARTESIAN_POINT('Ctrl Pts',(-0.146307221518699,0.000133045872591754,
0.708934495415711));
#15229=CARTESIAN_POINT('Ctrl Pts',(-0.145987367488279,-0.0358102803178394,
0.710888040627207));
#15230=CARTESIAN_POINT('Ctrl Pts',(-0.132622002370819,-0.0719663061161047,
0.712841585838703));
#15231=CARTESIAN_POINT('Ctrl Pts',(-0.1086007072861,-0.0984612847532928,
0.7147951310502));
#15232=CARTESIAN_POINT('Ctrl Pts',(-0.0760477256663158,-0.134366532557423,
0.71744252042446));
#15233=CARTESIAN_POINT('Ctrl Pts',(-0.0239252288417074,-0.152529358077047,
0.720089909798719));
#15234=CARTESIAN_POINT('Ctrl Pts',(0.0238920022682765,-0.144630254255197,
0.722737299172979));
#15235=CARTESIAN_POINT('Ctrl Pts',(0.071709233378259,-0.136731150433346,
0.725384688547239));
#15236=CARTESIAN_POINT('Ctrl Pts',(0.115221198773618,-0.102770117270024,
0.7280320779215));
#15237=CARTESIAN_POINT('Ctrl Pts',(0.134497183226257,-0.058303052428779,
0.730679467295759));
#15238=CARTESIAN_POINT('Ctrl Pts',(0.153773167678896,-0.0138359875875333,
0.733326856670019));
#15239=CARTESIAN_POINT('Ctrl Pts',(0.148813171188813,0.0411371089316358,
0.735974246044279));
#15240=CARTESIAN_POINT('Ctrl Pts',(0.121889126928366,0.0814357351225549,
0.738621635418539));
#15241=CARTESIAN_POINT('Ctrl Pts',(0.0949650826679194,0.121734361313473,
0.741269024792799));
#15242=CARTESIAN_POINT('Ctrl Pts',(0.0460769906371109,0.147358517176143,
0.74391641416706));
#15243=CARTESIAN_POINT('Ctrl Pts',(-0.00238189178169058,0.146571023090686,
0.74656380354132));
#15244=CARTESIAN_POINT('Ctrl Pts',(-0.0508407742004934,0.14578352900523,
0.74921119291558));
#15245=CARTESIAN_POINT('Ctrl Pts',(-0.0988704470072894,0.118584384971644,
0.751858582289839));
#15246=CARTESIAN_POINT('Ctrl Pts',(-0.124470852918682,0.0774321960944291,
0.754505971664099));
#15247=CARTESIAN_POINT('Ctrl Pts',(-0.138745545153454,0.0544858868428234,
0.75598214624797));
#15248=CARTESIAN_POINT('Ctrl Pts',(-0.146046671909043,0.027201385339783,
0.757458320831841));
#15249=CARTESIAN_POINT('Ctrl Pts',(-0.14612241379348,-4.54149644099216E-5,
0.758934495415711));
#15250=CARTESIAN_POINT('Origin',(0.,0.,0.));
#15251=CARTESIAN_POINT('',(-0.146495788566881,-0.000101744904923998,0.816065504584291));
#15252=CARTESIAN_POINT('',(-0.146473871348434,-0.000110945968026819,0.808934495415711));
#15253=CARTESIAN_POINT('',(-0.14635,-1.79227059055215E-17,0.));
#15254=CARTESIAN_POINT('Ctrl Pts',(-0.146495788566881,-0.000101744904923998,
0.816065504584291));
#15255=CARTESIAN_POINT('Ctrl Pts',(-0.14616118452328,0.0421270051992108,
0.813762715835428));
#15256=CARTESIAN_POINT('Ctrl Pts',(-0.126905337350145,0.0846218946815527,
0.811459927086565));
#15257=CARTESIAN_POINT('Ctrl Pts',(-0.0947343415465314,0.111866064832055,
0.809157138337701));
#15258=CARTESIAN_POINT('Ctrl Pts',(-0.0577639214515077,0.143174651664521,
0.806510808458599));
#15259=CARTESIAN_POINT('Ctrl Pts',(-0.00373742343573488,0.154342745753647,
0.803864478579497));
#15260=CARTESIAN_POINT('Ctrl Pts',(0.0426163743729279,0.140258534729872,
0.801218148700395));
#15261=CARTESIAN_POINT('Ctrl Pts',(0.0889701721815907,0.126174323706097,
0.798571818821294));
#15262=CARTESIAN_POINT('Ctrl Pts',(0.127651269783143,0.0868378075694234,
0.795925488942192));
#15263=CARTESIAN_POINT('Ctrl Pts',(0.140954720244851,0.040253928627653,
0.79327915906309));
#15264=CARTESIAN_POINT('Ctrl Pts',(0.154258170706558,-0.00632995031411615,
0.790632829183988));
#15265=CARTESIAN_POINT('Ctrl Pts',(0.14218397402842,-0.060161192060982,
0.787986499304886));
#15266=CARTESIAN_POINT('Ctrl Pts',(0.110258679990485,-0.0966003903512828,
0.785340169425784));
#15267=CARTESIAN_POINT('Ctrl Pts',(0.0783333859525485,-0.133039588641585,
0.782693839546682));
#15268=CARTESIAN_POINT('Ctrl Pts',(0.0265569945548152,-0.152086743475322,
0.780047509667581));
#15269=CARTESIAN_POINT('Ctrl Pts',(-0.021371625274328,-0.14502367242074,
0.777401179788479));
#15270=CARTESIAN_POINT('Ctrl Pts',(-0.0693002451034712,-0.137960601366157,
0.774754849909377));
#15271=CARTESIAN_POINT('Ctrl Pts',(-0.113381093364023,-0.104787304423254,
0.772108520030274));
#15272=CARTESIAN_POINT('Ctrl Pts',(-0.133437672293631,-0.0606877215103841,
0.769462190151172));
#15273=CARTESIAN_POINT('Ctrl Pts',(-0.1420188514214,-0.0418197768941368,
0.768329961628878));
#15274=CARTESIAN_POINT('Ctrl Pts',(-0.146202281842484,-0.0209517273285418,
0.767197733106584));
#15275=CARTESIAN_POINT('Ctrl Pts',(-0.1461301977291,-5.61458017395017E-5,
0.766065504584291));
#15276=CARTESIAN_POINT('Ctrl Pts',(-0.14612241379348,-4.54149644099216E-5,
0.758934495415711));
#15277=CARTESIAN_POINT('Ctrl Pts',(-0.146182508321779,-0.0216633562673834,
0.760105710206101));
#15278=CARTESIAN_POINT('Ctrl Pts',(-0.141694203021096,-0.0432575645610501,
0.76127692499649));
#15279=CARTESIAN_POINT('Ctrl Pts',(-0.132531725405586,-0.0626424774360703,
0.76244813978688));
#15280=CARTESIAN_POINT('Ctrl Pts',(-0.111821052965107,-0.106459728368519,
0.76509552916114));
#15281=CARTESIAN_POINT('Ctrl Pts',(-0.067228569068158,-0.138988996512573,
0.767742918535399));
#15282=CARTESIAN_POINT('Ctrl Pts',(-0.0191799219195066,-0.145330206128911,
0.770390307909659));
#15283=CARTESIAN_POINT('Ctrl Pts',(0.0288687252291434,-0.151671415745249,
0.773037697283919));
#15284=CARTESIAN_POINT('Ctrl Pts',(0.080373535629496,-0.131824566833873,
0.77568508665818));
#15285=CARTESIAN_POINT('Ctrl Pts',(0.111742660473083,-0.0948805356683208,
0.77833247603244));
#15286=CARTESIAN_POINT('Ctrl Pts',(0.14311178531667,-0.0579365045027684,
0.7809798654067));
#15287=CARTESIAN_POINT('Ctrl Pts',(0.154345224603492,-0.00389529108304171,
0.783627254780959));
#15288=CARTESIAN_POINT('Ctrl Pts',(0.140297486112651,0.0424894529122293,
0.786274644155219));
#15289=CARTESIAN_POINT('Ctrl Pts',(0.126249747621811,0.0888741969075009,
0.788922033529479));
#15290=CARTESIAN_POINT('Ctrl Pts',(0.0869208313533056,0.127602471478316,
0.79156942290374));
#15291=CARTESIAN_POINT('Ctrl Pts',(0.0403254011646538,0.140934737517831,
0.794216812278));
#15292=CARTESIAN_POINT('Ctrl Pts',(-0.00627002902399674,0.154267003557346,
0.79686420165226));
#15293=CARTESIAN_POINT('Ctrl Pts',(-0.0601319731327944,0.142203261065564,
0.799511591026519));
#15294=CARTESIAN_POINT('Ctrl Pts',(-0.0965888940360299,0.110269323781398,
0.802158980400779));
#15295=CARTESIAN_POINT('Ctrl Pts',(-0.127690529151203,0.0830262752573849,
0.804417485405756));
#15296=CARTESIAN_POINT('Ctrl Pts',(-0.146124951115714,0.0413218847513699,
0.806675990410734));
#15297=CARTESIAN_POINT('Ctrl Pts',(-0.146473871348434,-0.000110945968026819,
0.808934495415711));
#15298=CARTESIAN_POINT('Origin',(0.,0.,0.));
#15299=CARTESIAN_POINT('',(-0.146444331750498,0.000119944961782359,0.866065504584291));
#15300=CARTESIAN_POINT('',(-0.146471560192382,0.00011177640072981,0.858934495415711));
#15301=CARTESIAN_POINT('',(-0.14635,-1.79227059055215E-17,0.));
#15302=CARTESIAN_POINT('Ctrl Pts',(-0.146444331750498,0.000119944961782359,
0.866065504584291));
#15303=CARTESIAN_POINT('Ctrl Pts',(-0.146516681599632,0.00829054204730037,
0.865620358322474));
#15304=CARTESIAN_POINT('Ctrl Pts',(-0.145891801779796,0.0164500693154795,
0.865175212060658));
#15305=CARTESIAN_POINT('Ctrl Pts',(-0.14453063157077,0.0244848619971339,
0.864730065798841));
#15306=CARTESIAN_POINT('Ctrl Pts',(-0.136438672357208,0.0722505376181754,
0.862083735919739));
#15307=CARTESIAN_POINT('Ctrl Pts',(-0.102325254887189,0.115607931012472,
0.859437406040638));
#15308=CARTESIAN_POINT('Ctrl Pts',(-0.0578046270350215,0.134711681091902,
0.856791076161536));
#15309=CARTESIAN_POINT('Ctrl Pts',(-0.0132839991828526,0.153815431171333,
0.854144746282434));
#15310=CARTESIAN_POINT('Ctrl Pts',(0.0416438390514653,0.148665537935894,
0.851498416403331));
#15311=CARTESIAN_POINT('Ctrl Pts',(0.081837551941475,0.121619188541491,
0.848852086524229));
#15312=CARTESIAN_POINT('Ctrl Pts',(0.122031264831484,0.0945728391470885,
0.846205756645128));
#15313=CARTESIAN_POINT('Ctrl Pts',(0.147490852377186,0.0456300335937214,
0.843559426766026));
#15314=CARTESIAN_POINT('Ctrl Pts',(0.146563060809277,-0.0028073360113171,
0.840913096886925));
#15315=CARTESIAN_POINT('Ctrl Pts',(0.145635269241369,-0.0512447056163556,
0.838266767007823));
#15316=CARTESIAN_POINT('Ctrl Pts',(0.118320098559852,-0.0991766392730661,
0.835620437128721));
#15317=CARTESIAN_POINT('Ctrl Pts',(0.0771201321287374,-0.124663936845065,
0.832974107249619));
#15318=CARTESIAN_POINT('Ctrl Pts',(0.035920165697623,-0.150151234417064,
0.830327777370517));
#15319=CARTESIAN_POINT('Ctrl Pts',(-0.0191645964830881,-0.153193895904352,
0.827681447491415));
#15320=CARTESIAN_POINT('Ctrl Pts',(-0.0629209921278279,-0.132399247274726,
0.825035117612313));
#15321=CARTESIAN_POINT('Ctrl Pts',(-0.106677387772568,-0.111604598645101,
0.822388787733211));
#15322=CARTESIAN_POINT('Ctrl Pts',(-0.139105416881337,-0.0669726398985626,
0.819742457854109));
#15323=CARTESIAN_POINT('Ctrl Pts',(-0.145362260348583,-0.0189321207373897,
0.817096127975007));
#15324=CARTESIAN_POINT('Ctrl Pts',(-0.146174510965348,-0.0126955988357878,
0.816752586844768));
#15325=CARTESIAN_POINT('Ctrl Pts',(-0.146545706411658,-0.00640163348415362,
0.81640904571453));
#15326=CARTESIAN_POINT('Ctrl Pts',(-0.146495788566881,-0.000101744904923998,
0.816065504584291));
#15327=CARTESIAN_POINT('Ctrl Pts',(-0.146473871348434,-0.000110945968026819,
0.808934495415711));
#15328=CARTESIAN_POINT('Ctrl Pts',(-0.146533950748007,-0.00724512552769256,
0.809323379784994));
#15329=CARTESIAN_POINT('Ctrl Pts',(-0.146057826922151,-0.0143712538186879,
0.809712264154277));
#15330=CARTESIAN_POINT('Ctrl Pts',(-0.145017839345608,-0.0214141189368497,
0.81010114852356));
#15331=CARTESIAN_POINT('Ctrl Pts',(-0.137937966054276,-0.0693594922943736,
0.81274853789782));
#15332=CARTESIAN_POINT('Ctrl Pts',(-0.104726321773939,-0.113446106932874,
0.81539592727208));
#15333=CARTESIAN_POINT('Ctrl Pts',(-0.0605955455659204,-0.133480028752914,
0.818043316646339));
#15334=CARTESIAN_POINT('Ctrl Pts',(-0.0164647693578984,-0.153513950572954,
0.820690706020599));
#15335=CARTESIAN_POINT('Ctrl Pts',(0.0385851387778066,-0.149495179574532,
0.823338095394859));
#15336=CARTESIAN_POINT('Ctrl Pts',(0.0793384931690736,-0.12326451930694,
0.825985484769119));
#15337=CARTESIAN_POINT('Ctrl Pts',(0.120091847560339,-0.0970338590393495,
0.828632874143379));
#15338=CARTESIAN_POINT('Ctrl Pts',(0.146548648207165,-0.0485913095025905,
0.83128026351764));
#15339=CARTESIAN_POINT('Ctrl Pts',(0.146590321408106,-0.000126046730599388,
0.833927652891899));
#15340=CARTESIAN_POINT('Ctrl Pts',(0.146631994609047,0.0483392160413931,
0.836575042266159));
#15341=CARTESIAN_POINT('Ctrl Pts',(0.120258540364101,0.0968271920486179,
0.839222431640419));
#15342=CARTESIAN_POINT('Ctrl Pts',(0.0795503554414038,0.123127897600245,
0.841869821014679));
#15343=CARTESIAN_POINT('Ctrl Pts',(0.0388421705187073,0.149428603151872,
0.844517210388939));
#15344=CARTESIAN_POINT('Ctrl Pts',(-0.0162007450817403,0.153542038247903,
0.8471645997632));
#15345=CARTESIAN_POINT('Ctrl Pts',(-0.0603659086281491,0.133584038319734,
0.84981198913746));
#15346=CARTESIAN_POINT('Ctrl Pts',(-0.104531072174558,0.113626038391565,
0.85245937851172));
#15347=CARTESIAN_POINT('Ctrl Pts',(-0.137818483666928,0.0695966034391962,
0.855106767885979));
#15348=CARTESIAN_POINT('Ctrl Pts',(-0.144980798768897,0.0216634763286692,
0.857754157260239));
#15349=CARTESIAN_POINT('Ctrl Pts',(-0.146045237806912,0.0145398171508471,
0.858147603312063));
#15350=CARTESIAN_POINT('Ctrl Pts',(-0.146532654486068,0.00732993751956911,
0.858541049363887));
#15351=CARTESIAN_POINT('Ctrl Pts',(-0.146471560192382,0.00011177640072981,
0.858934495415711));
#15352=CARTESIAN_POINT('Origin',(0.,0.,0.));
#15353=CARTESIAN_POINT('',(-0.146114231148477,2.69008449349656E-5,0.916065504584291));
#15354=CARTESIAN_POINT('',(-0.146121644853617,4.41067432152685E-5,0.908934495415711));
#15355=CARTESIAN_POINT('',(-0.14635,-1.79227059055215E-17,0.));
#15356=CARTESIAN_POINT('Ctrl Pts',(-0.146114231148477,2.69008449349656E-5,
0.916065504584291));
#15357=CARTESIAN_POINT('Ctrl Pts',(-0.146151635159142,0.0228038459942234,
0.914831670930419));
#15358=CARTESIAN_POINT('Ctrl Pts',(-0.141147538069067,0.0455652341090756,
0.913597837276548));
#15359=CARTESIAN_POINT('Ctrl Pts',(-0.131015765267123,0.0657531838068269,
0.912364003622676));
#15360=CARTESIAN_POINT('Ctrl Pts',(-0.109285110563454,0.109052354902802,
0.909717673743574));
#15361=CARTESIAN_POINT('Ctrl Pts',(-0.0639662294071284,0.140513248471977,
0.907071343864472));
#15362=CARTESIAN_POINT('Ctrl Pts',(-0.015802286694576,0.145735718560985,
0.90442501398537));
#15363=CARTESIAN_POINT('Ctrl Pts',(0.0323616560179757,0.150958188649994,
0.901778684106268));
#15364=CARTESIAN_POINT('Ctrl Pts',(0.0833706602867547,0.129942235258839,
0.899132354227166));
#15365=CARTESIAN_POINT('Ctrl Pts',(0.113877102345416,0.0923071908936453,
0.896486024348064));
#15366=CARTESIAN_POINT('Ctrl Pts',(0.144383544404078,0.0546721465284523,
0.893839694468962));
#15367=CARTESIAN_POINT('Ctrl Pts',(0.15438742425262,0.000418011189221586,
0.891193364589861));
#15368=CARTESIAN_POINT('Ctrl Pts',(0.139309808695705,-0.0456222438118789,
0.888547034710759));
#15369=CARTESIAN_POINT('Ctrl Pts',(0.124232193138789,-0.0916624988129813,
0.885900704831657));
#15370=CARTESIAN_POINT('Ctrl Pts',(0.0840730821764119,-0.129488873475953,
0.883254374952555));
#15371=CARTESIAN_POINT('Ctrl Pts',(0.0372139327097935,-0.141787641004198,
0.880608045073453));
#15372=CARTESIAN_POINT('Ctrl Pts',(-0.00964521675682358,-0.154086408532443,
0.877961715194351));
#15373=CARTESIAN_POINT('Ctrl Pts',(-0.0632044047276821,-0.140857568925962,
0.875315385315249));
#15374=CARTESIAN_POINT('Ctrl Pts',(-0.0989487482345592,-0.108156170198829,
0.872669055436147));
#15375=CARTESIAN_POINT('Ctrl Pts',(-0.128680439645858,-0.0809555616469925,
0.870467871818862));
#15376=CARTESIAN_POINT('Ctrl Pts',(-0.146086572253705,-0.0402824710322022,
0.868266688201576));
#15377=CARTESIAN_POINT('Ctrl Pts',(-0.146444331750498,0.000119944961782359,
0.866065504584291));
#15378=CARTESIAN_POINT('Ctrl Pts',(-0.146471560192382,0.00011177640072981,
0.858934495415711));
#15379=CARTESIAN_POINT('Ctrl Pts',(-0.146121567926216,-0.0412390669452651,
0.861188438738147));
#15380=CARTESIAN_POINT('Ctrl Pts',(-0.127770397964496,-0.0828616943330661,
0.863442382060584));
#15381=CARTESIAN_POINT('Ctrl Pts',(-0.096778382793969,-0.110103055552942,
0.86569632538302));
#15382=CARTESIAN_POINT('Ctrl Pts',(-0.0603764330055066,-0.142099641055337,
0.86834371475728));
#15383=CARTESIAN_POINT('Ctrl Pts',(-0.00653531471701479,-0.154255992791443,
0.870991104131539));
#15384=CARTESIAN_POINT('Ctrl Pts',(0.040082974241256,-0.14100387723139,
0.873638493505799));
#15385=CARTESIAN_POINT('Ctrl Pts',(0.0867012631995282,-0.127751761671338,
0.876285882880059));
#15386=CARTESIAN_POINT('Ctrl Pts',(0.12609672282758,-0.0890911788151255,
0.878933272254319));
#15387=CARTESIAN_POINT('Ctrl Pts',(0.140224208991091,-0.042730661487191,
0.88158066162858));
#15388=CARTESIAN_POINT('Ctrl Pts',(0.154351695154603,0.00362985584074295,
0.88422805100284));
#15389=CARTESIAN_POINT('Ctrl Pts',(0.143211207853577,0.057690307640398,
0.886875440377099));
#15390=CARTESIAN_POINT('Ctrl Pts',(0.111905662524754,0.09468823006692,0.889522829751359));
#15391=CARTESIAN_POINT('Ctrl Pts',(0.0806001171959318,0.131686152493442,
0.892170219125619));
#15392=CARTESIAN_POINT('Ctrl Pts',(0.0291295138393125,0.15162154554683,
0.894817608499879));
#15393=CARTESIAN_POINT('Ctrl Pts',(-0.0189299673197759,0.145362975188259,
0.897464997874139));
#15394=CARTESIAN_POINT('Ctrl Pts',(-0.0669894484788628,0.139104404829688,
0.9001123872484));
#15395=CARTESIAN_POINT('Ctrl Pts',(-0.11163780744042,0.10665187105916,0.902759776622659));
#15396=CARTESIAN_POINT('Ctrl Pts',(-0.132423802349956,0.0628703013313112,
0.905407165996919));
#15397=CARTESIAN_POINT('Ctrl Pts',(-0.141655418982822,0.043425734493323,
0.90658294246985));
#15398=CARTESIAN_POINT('Ctrl Pts',(-0.146180218154578,0.0217465313827003,
0.907758718942781));
#15399=CARTESIAN_POINT('Ctrl Pts',(-0.146121644853617,4.41067432152685E-5,
0.908934495415711));
#15400=CARTESIAN_POINT('Origin',(0.,0.,0.));
#15401=CARTESIAN_POINT('',(-0.146345621585321,-0.000133809880645736,0.966065504584291));
#15402=CARTESIAN_POINT('',(-0.146309694201085,-0.000133223314395004,0.958934495415711));
#15403=CARTESIAN_POINT('',(-0.14635,-1.79227059055215E-17,0.));
#15404=CARTESIAN_POINT('Ctrl Pts',(-0.146345621585321,-0.000133809880645736,
0.966065504584291));
#15405=CARTESIAN_POINT('Ctrl Pts',(-0.146004672532387,0.0370537288701324,
0.964042983538364));
#15406=CARTESIAN_POINT('Ctrl Pts',(-0.131578083002406,0.0744765756810296,
0.962020462492437));
#15407=CARTESIAN_POINT('Ctrl Pts',(-0.106003654037246,0.101251356830495,
0.959997941446511));
#15408=CARTESIAN_POINT('Ctrl Pts',(-0.0725412702228666,0.136284319036219,
0.957351611567409));
#15409=CARTESIAN_POINT('Ctrl Pts',(-0.0199938687303381,0.153087872523943,
0.954705281688306));
#15410=CARTESIAN_POINT('Ctrl Pts',(0.0275867780614433,0.143970766496025,
0.952058951809204));
#15411=CARTESIAN_POINT('Ctrl Pts',(0.0751674248532248,0.134853660468108,
0.949412621930102));
#15412=CARTESIAN_POINT('Ctrl Pts',(0.11778131694426,0.0998158949245492,
0.946766292051));
#15413=CARTESIAN_POINT('Ctrl Pts',(0.135923405490256,0.0548948063954655,
0.944119962171899));
#15414=CARTESIAN_POINT('Ctrl Pts',(0.154065494036253,0.0099737178663825,
0.941473632292797));
#15415=CARTESIAN_POINT('Ctrl Pts',(0.147735779037212,-0.0448306936482241,
0.938827302413695));
#15416=CARTESIAN_POINT('Ctrl Pts',(0.119831470632095,-0.0844335867733556,
0.936180972534593));
#15417=CARTESIAN_POINT('Ctrl Pts',(0.0919271622269763,-0.124036479898489,
0.933534642655491));
#15418=CARTESIAN_POINT('Ctrl Pts',(0.0424482604157787,-0.148437854634144,
0.93088831277639));
#15419=CARTESIAN_POINT('Ctrl Pts',(-0.00595796300272124,-0.146468817862788,
0.928241982897288));
#15420=CARTESIAN_POINT('Ctrl Pts',(-0.0543641864212212,-0.144499781091432,
0.925595653018186));
#15421=CARTESIAN_POINT('Ctrl Pts',(-0.101697731447024,-0.116160332813065,
0.922949323139084));
#15422=CARTESIAN_POINT('Ctrl Pts',(-0.126293289834417,-0.0744218843624929,
0.920302993259982));
#15423=CARTESIAN_POINT('Ctrl Pts',(-0.139421333187579,-0.052143709087005,
0.918890497034752));
#15424=CARTESIAN_POINT('Ctrl Pts',(-0.146071410932229,-0.0260482098028304,
0.917478000809521));
#15425=CARTESIAN_POINT('Ctrl Pts',(-0.146114231148477,2.69008449349656E-5,
0.916065504584291));
#15426=CARTESIAN_POINT('Ctrl Pts',(-0.146121644853617,4.41067432152685E-5,
0.908934495415711));
#15427=CARTESIAN_POINT('Ctrl Pts',(-0.146048333958771,-0.027118852224649,
0.910406108317041));
#15428=CARTESIAN_POINT('Ctrl Pts',(-0.138795050353101,-0.0543181883240968,
0.91187772121837));
#15429=CARTESIAN_POINT('Ctrl Pts',(-0.124603830013468,-0.0772180274565794,
0.9133493341197));
#15430=CARTESIAN_POINT('Ctrl Pts',(-0.0990742319099257,-0.118414180831446,
0.91599672349396));
#15431=CARTESIAN_POINT('Ctrl Pts',(-0.0510914048453256,-0.145695881896007,
0.91864411286822));
#15432=CARTESIAN_POINT('Ctrl Pts',(-0.00263394834681351,-0.146566710184873,
0.92129150224248));
#15433=CARTESIAN_POINT('Ctrl Pts',(0.0458235081516972,-0.147437538473739,
0.92393889161674));
#15434=CARTESIAN_POINT('Ctrl Pts',(0.0947555940841207,-0.121897493986912,
0.926586280990999));
#15435=CARTESIAN_POINT('Ctrl Pts',(0.121748900601314,-0.0816452290135895,
0.929233670365259));
#15436=CARTESIAN_POINT('Ctrl Pts',(0.148742207118509,-0.0413929640402651,
0.931881059739519));
#15437=CARTESIAN_POINT('Ctrl Pts',(0.153796734220472,0.0135715214195569,
0.93452844911378));
#15438=CARTESIAN_POINT('Ctrl Pts',(0.134597248858856,0.0580716696672091,
0.93717583848804));
#15439=CARTESIAN_POINT('Ctrl Pts',(0.115397763497239,0.102571817914861,
0.9398232278623));
#15440=CARTESIAN_POINT('Ctrl Pts',(0.0719442656720451,0.136607628950342,
0.942470617236559));
#15441=CARTESIAN_POINT('Ctrl Pts',(0.0241406894609324,0.144588953003544,
0.945118006610819));
#15442=CARTESIAN_POINT('Ctrl Pts',(-0.023662886750181,0.152570277056746,
0.947765395985079));
#15443=CARTESIAN_POINT('Ctrl Pts',(-0.0758165413472122,0.134497114127667,
0.950412785359339));
#15444=CARTESIAN_POINT('Ctrl Pts',(-0.108431221550465,0.0986479012011113,
0.953060174733599));
#15445=CARTESIAN_POINT('Ctrl Pts',(-0.132554242808212,0.0721325001574252,
0.955018281627637));
#15446=CARTESIAN_POINT('Ctrl Pts',(-0.145988218858404,0.0358924841874147,
0.956976388521674));
#15447=CARTESIAN_POINT('Ctrl Pts',(-0.146309694201085,-0.000133223314395004,
0.958934495415711));
#15448=CARTESIAN_POINT('Origin',(0.,0.,0.));
#15449=CARTESIAN_POINT('',(-0.146565171121453,5.44893591410845E-5,1.01606550458429));
#15450=CARTESIAN_POINT('',(-0.146582076026177,3.15354312248815E-5,1.00893449541571));
#15451=CARTESIAN_POINT('',(-0.14635,-1.79227059055215E-17,0.));
#15452=CARTESIAN_POINT('Ctrl Pts',(-0.146565171121453,5.44893591410845E-5,
1.01606550458429));
#15453=CARTESIAN_POINT('Ctrl Pts',(-0.146579596851449,0.00307427920823236,
1.01590062602541));
#15454=CARTESIAN_POINT('Ctrl Pts',(-0.146494352296349,0.00609323927190738,
1.01573574746653));
#15455=CARTESIAN_POINT('Ctrl Pts',(-0.146306854564556,0.00910583530985269,
1.01557086890765));
#15456=CARTESIAN_POINT('Ctrl Pts',(-0.143297482980539,0.0574585317612167,
1.01292453902855));
#15457=CARTESIAN_POINT('Ctrl Pts',(-0.11394685994478,0.104171803331984,
1.01027820914945));
#15458=CARTESIAN_POINT('Ctrl Pts',(-0.0716892273871119,0.127864250695428,
1.00763187927034));
#15459=CARTESIAN_POINT('Ctrl Pts',(-0.0294315948294418,0.151556698058874,
1.00498554939124));
#15460=CARTESIAN_POINT('Ctrl Pts',(0.0257330472501378,0.152228321214993,
1.00233921951214));
#15461=CARTESIAN_POINT('Ctrl Pts',(0.0685549742796134,0.129571707678744,
0.999692889633039));
#15462=CARTESIAN_POINT('Ctrl Pts',(0.111376901309088,0.106915094142495,
0.997046559753937));
#15463=CARTESIAN_POINT('Ctrl Pts',(0.141856113288459,0.0609302439138786,
0.994400229874835));
#15464=CARTESIAN_POINT('Ctrl Pts',(0.146041795372579,0.0126651464112397,
0.991753899995733));
#15465=CARTESIAN_POINT('Ctrl Pts',(0.150227477456699,-0.0355999510913994,
0.989107570116631));
#15466=CARTESIAN_POINT('Ctrl Pts',(0.128119629645567,-0.0861452958680607,
0.986461240237529));
#15467=CARTESIAN_POINT('Ctrl Pts',(0.0898373616998479,-0.115835488396583,
0.983814910358427));
#15468=CARTESIAN_POINT('Ctrl Pts',(0.051555093754129,-0.145525680925106,
0.981168580479325));
#15469=CARTESIAN_POINT('Ctrl Pts',(-0.00290159432617693,-0.154360721205491,
0.978522250600224));
#15470=CARTESIAN_POINT('Ctrl Pts',(-0.0486070196525971,-0.138296672301818,
0.975875920721122));
#15471=CARTESIAN_POINT('Ctrl Pts',(-0.0943124449790173,-0.122232623398145,
0.97322959084202));
#15472=CARTESIAN_POINT('Ctrl Pts',(-0.131266607551552,-0.081269485310415,
0.970583260962917));
#15473=CARTESIAN_POINT('Ctrl Pts',(-0.142555005769704,-0.0341567308046872,
0.967936931083816));
#15474=CARTESIAN_POINT('Ctrl Pts',(-0.145215975052668,-0.0230510282813687,
0.967313122250641));
#15475=CARTESIAN_POINT('Ctrl Pts',(-0.146450780951306,-0.0116036114945705,
0.966689313417466));
#15476=CARTESIAN_POINT('Ctrl Pts',(-0.146345621585321,-0.000133809880645736,
0.966065504584291));
#15477=CARTESIAN_POINT('Ctrl Pts',(-0.146309694201085,-0.000133223314395004,
0.958934495415711));
#15478=CARTESIAN_POINT('Ctrl Pts',(-0.146422858258782,-0.0128148032088542,
0.959623777895933));
#15479=CARTESIAN_POINT('Ctrl Pts',(-0.14491119500038,-0.0254698272036438,
0.960313060376156));
#15480=CARTESIAN_POINT('Ctrl Pts',(-0.141668994059001,-0.037664762585484,
0.961002342856379));
#15481=CARTESIAN_POINT('Ctrl Pts',(-0.129216380554811,-0.0845029505214961,
0.963649732230639));
#15482=CARTESIAN_POINT('Ctrl Pts',(-0.0912354477369537,-0.12455406346949,
0.966297121604899));
#15483=CARTESIAN_POINT('Ctrl Pts',(-0.0451234138007503,-0.1394726343957,
0.968944510979159));
#15484=CARTESIAN_POINT('Ctrl Pts',(0.00098862013545236,-0.154391205321909,
0.97159190035342));
#15485=CARTESIAN_POINT('Ctrl Pts',(0.055231755190001,-0.144177234226336,
0.974239289727679));
#15486=CARTESIAN_POINT('Ctrl Pts',(0.0927598492034174,-0.113509244531313,
0.976886679101939));
#15487=CARTESIAN_POINT('Ctrl Pts',(0.130287943216833,-0.0828412548362905,
0.979534068476199));
#15488=CARTESIAN_POINT('Ctrl Pts',(0.151100996189117,-0.0317192465418168,
0.982181457850459));
#15489=CARTESIAN_POINT('Ctrl Pts',(0.145665560755875,0.0164402745715088,
0.984828847224719));
#15490=CARTESIAN_POINT('Ctrl Pts',(0.140230125322634,0.0645997956848379,
0.987476236598979));
#15491=CARTESIAN_POINT('Ctrl Pts',(0.108546201483865,0.109796829617019,
0.990123625973239));
#15492=CARTESIAN_POINT('Ctrl Pts',(0.0651266538643092,0.131328813193254,
0.992771015347499));
#15493=CARTESIAN_POINT('Ctrl Pts',(0.0217071062447581,0.152860796769488,
0.995418404721759));
#15494=CARTESIAN_POINT('Ctrl Pts',(-0.0334480651555777,0.15072772998978,
0.998065794096019));
#15495=CARTESIAN_POINT('Ctrl Pts',(-0.0750749586823209,0.125906667008376,
1.00071318347028));
#15496=CARTESIAN_POINT('Ctrl Pts',(-0.116701852209067,0.101085604026969,
1.00336057284454));
#15497=CARTESIAN_POINT('Ctrl Pts',(-0.144800467862219,0.053576544843864,
1.0060079622188));
#15498=CARTESIAN_POINT('Ctrl Pts',(-0.146500196332402,0.00514107896046776,
1.00865535159306));
#15499=CARTESIAN_POINT('Ctrl Pts',(-0.146559936783033,0.00343871495990628,
1.00874839953394));
#15500=CARTESIAN_POINT('Ctrl Pts',(-0.146587066279139,0.00173520655478852,
1.00884144747483));
#15501=CARTESIAN_POINT('Ctrl Pts',(-0.146582076026177,3.15354312248815E-5,
1.00893449541571));
#15502=CARTESIAN_POINT('Origin',(0.,0.,0.));
#15503=CARTESIAN_POINT('',(-0.146184049129756,9.96948043307314E-5,1.06606550458429));
#15504=CARTESIAN_POINT('',(-0.146216477546812,0.000114345603752017,1.05893449541571));
#15505=CARTESIAN_POINT('',(-0.14635,-1.79227059055215E-17,0.));
#15506=CARTESIAN_POINT('Ctrl Pts',(-0.146184049129756,9.96948043307314E-5,
1.06606550458429));
#15507=CARTESIAN_POINT('Ctrl Pts',(-0.146294264763128,0.0176817746259609,
1.06511193863336));
#15508=CARTESIAN_POINT('Ctrl Pts',(-0.143360807533043,0.0352283113603788,
1.06415837268242));
#15509=CARTESIAN_POINT('Ctrl Pts',(-0.13721959397524,0.0515693218739058,
1.06320480673148));
#15510=CARTESIAN_POINT('Ctrl Pts',(-0.120176538991979,0.0969187854681546,
1.06055847685238));
#15511=CARTESIAN_POINT('Ctrl Pts',(-0.0784283132238915,0.132983650068601,
1.05791214697328));
#15512=CARTESIAN_POINT('Ctrl Pts',(-0.0310837364199337,0.143256459747686,
1.05526581709418));
#15513=CARTESIAN_POINT('Ctrl Pts',(0.0162608403840241,0.153529269426771,
1.05261948721508));
#15514=CARTESIAN_POINT('Ctrl Pts',(0.0692017682238519,0.138010024184496,
1.04997315733597));
#15515=CARTESIAN_POINT('Ctrl Pts',(0.103507151520239,0.103802126728842,
1.04732682745687));
#15516=CARTESIAN_POINT('Ctrl Pts',(0.137812534816628,0.0695942292731864,
1.04468049757777));
#15517=CARTESIAN_POINT('Ctrl Pts',(0.153482373569574,0.01669767960415,1.04203416769867));
#15518=CARTESIAN_POINT('Ctrl Pts',(0.143344336052008,-0.0306759392859165,
1.03938783781957));
#15519=CARTESIAN_POINT('Ctrl Pts',(0.133206298534443,-0.0780495581759789,
1.03674150794047));
#15520=CARTESIAN_POINT('Ctrl Pts',(0.0972603847463712,-0.119900246287072,
1.03409517806136));
#15521=CARTESIAN_POINT('Ctrl Pts',(0.0519596049571008,-0.137072285243832,
1.03144884818226));
#15522=CARTESIAN_POINT('Ctrl Pts',(0.00665882516783032,-0.154244324200591,
1.02880251830316));
#15523=CARTESIAN_POINT('Ctrl Pts',(-0.0479968206226384,-0.146737714003016,
1.02615618842406));
#15524=CARTESIAN_POINT('Ctrl Pts',(-0.0869905834517384,-0.11798834823825,
1.02350985854496));
#15525=CARTESIAN_POINT('Ctrl Pts',(-0.123554854979944,-0.0910302005802824,
1.02102840722473));
#15526=CARTESIAN_POINT('Ctrl Pts',(-0.146348061346918,-0.0453938791777224,
1.01854695590451));
#15527=CARTESIAN_POINT('Ctrl Pts',(-0.146565171121453,5.44893591410845E-5,
1.01606550458429));
#15528=CARTESIAN_POINT('Ctrl Pts',(-0.146582076026177,3.15354312248815E-5,
1.00893449541571));
#15529=CARTESIAN_POINT('Ctrl Pts',(-0.146445084172466,-0.0467374494427972,
1.01148883684909));
#15530=CARTESIAN_POINT('Ctrl Pts',(-0.122102455869861,-0.0936290599181376,
1.01404317828246));
#15531=CARTESIAN_POINT('Ctrl Pts',(-0.0837162036049941,-0.120334265578335,
1.01659751971584));
#15532=CARTESIAN_POINT('Ctrl Pts',(-0.0439316411201867,-0.14801227165006,
1.0192449090901));
#15533=CARTESIAN_POINT('Ctrl Pts',(0.0109383251366414,-0.154006411209824,
1.02189229846436));
#15534=CARTESIAN_POINT('Ctrl Pts',(0.0557604321169594,-0.135571060438576,
1.02453968783862));
#15535=CARTESIAN_POINT('Ctrl Pts',(0.100582539097277,-0.11713570966733,
1.02718707721288));
#15536=CARTESIAN_POINT('Ctrl Pts',(0.135356786801084,-0.0742708685650716,
1.02983446658714));
#15537=CARTESIAN_POINT('Ctrl Pts',(0.144154783532934,-0.0266108361928598,
1.0324818559614));
#15538=CARTESIAN_POINT('Ctrl Pts',(0.152952780264784,0.0210491961793507,
1.03512924533566));
#15539=CARTESIAN_POINT('Ctrl Pts',(0.135774526024679,0.0735044198215165,
1.03777663470992));
#15540=CARTESIAN_POINT('Ctrl Pts',(0.100488543649143,0.106727647840587,
1.04042402408418));
#15541=CARTESIAN_POINT('Ctrl Pts',(0.0652025612736062,0.139950875859659,
1.04307141345844));
#15542=CARTESIAN_POINT('Ctrl Pts',(0.0118088507626404,0.153942108255635,
1.0457188028327));
#15543=CARTESIAN_POINT('Ctrl Pts',(-0.0352355257975899,0.142292641904202,
1.04836619220696));
#15544=CARTESIAN_POINT('Ctrl Pts',(-0.0822799023578202,0.130643175552769,
1.05101358158122));
#15545=CARTESIAN_POINT('Ctrl Pts',(-0.122974944967313,0.0933530104539243,
1.05366097095548));
#15546=CARTESIAN_POINT('Ctrl Pts',(-0.138680233730631,0.0475029577050484,
1.05630836032974));
#15547=CARTESIAN_POINT('Ctrl Pts',(-0.143873300563147,0.0323423075707214,
1.05718373869173));
#15548=CARTESIAN_POINT('Ctrl Pts',(-0.146334133026589,0.0162457690968458,
1.05805911705372));
#15549=CARTESIAN_POINT('Ctrl Pts',(-0.146216477546812,0.000114345603752017,
1.05893449541571));
#15550=CARTESIAN_POINT('Origin',(0.,0.,0.));
#15551=CARTESIAN_POINT('',(-0.146204073634541,-0.000109175101205505,1.11606550458429));
#15552=CARTESIAN_POINT('',(-0.146170555016798,-9.22629125885076E-5,1.10893449541571));
#15553=CARTESIAN_POINT('',(-0.14635,-1.79227059055215E-17,0.));
#15554=CARTESIAN_POINT('Ctrl Pts',(-0.146204073634541,-0.000109175101205505,
1.11606550458429));
#15555=CARTESIAN_POINT('Ctrl Pts',(-0.145981599624502,0.032003853555373,
1.1143232512413));
#15556=CARTESIAN_POINT('Ctrl Pts',(-0.135565881201595,0.0642480963468658,
1.11258099789831));
#15557=CARTESIAN_POINT('Ctrl Pts',(-0.11609067353381,0.0895073597405865,
1.11083874455532));
#15558=CARTESIAN_POINT('Ctrl Pts',(-0.0865095427755784,0.127873963375947,
1.10819241467622));
#15559=CARTESIAN_POINT('Ctrl Pts',(-0.0360273159486943,0.150125560802435,
1.10554608479712));
#15560=CARTESIAN_POINT('Ctrl Pts',(0.0122494975033169,0.14607724579886,
1.10289975491801));
#15561=CARTESIAN_POINT('Ctrl Pts',(0.0605263109553308,0.142028930795284,
1.10025342503891));
#15562=CARTESIAN_POINT('Ctrl Pts',(0.10659771103247,0.111680703361642,1.09760709515981));
#15563=CARTESIAN_POINT('Ctrl Pts',(0.129376093089052,0.0689234246557527,
1.09496076528071));
#15564=CARTESIAN_POINT('Ctrl Pts',(0.152154475145634,0.0261661459498645,
1.09231443540161));
#15565=CARTESIAN_POINT('Ctrl Pts',(0.151639839181659,-0.0290001840282729,
1.0896681055225));
#15566=CARTESIAN_POINT('Ctrl Pts',(0.128067742174483,-0.0713250681289163,
1.0870217756434));
#15567=CARTESIAN_POINT('Ctrl Pts',(0.104495645167307,-0.11364995222956,
1.0843754457643));
#15568=CARTESIAN_POINT('Ctrl Pts',(0.0578660871169326,-0.143133390452712,
1.0817291158852));
#15569=CARTESIAN_POINT('Ctrl Pts',(0.00952215035475689,-0.146280349267719,
1.0790827860061));
#15570=CARTESIAN_POINT('Ctrl Pts',(-0.0388217864074202,-0.149427308082725,
1.07643645612699));
#15571=CARTESIAN_POINT('Ctrl Pts',(-0.0888801018813974,-0.126237787489585,
1.07379012624789));
#15572=CARTESIAN_POINT('Ctrl Pts',(-0.117740317519168,-0.0873259958989869,
1.07114379636879));
#15573=CARTESIAN_POINT('Ctrl Pts',(-0.136201180005177,-0.0624354946409797,
1.06945103244062));
#15574=CARTESIAN_POINT('Ctrl Pts',(-0.145988395071105,-0.0311118962502767,
1.06775826851246));
#15575=CARTESIAN_POINT('Ctrl Pts',(-0.146184049129756,9.96948043307314E-5,
1.06606550458429));
#15576=CARTESIAN_POINT('Ctrl Pts',(-0.146216477546812,0.000114345603752017,
1.05893449541571));
#15577=CARTESIAN_POINT('Ctrl Pts',(-0.145978309898544,-0.0325401742182177,
1.06070650642798));
#15578=CARTESIAN_POINT('Ctrl Pts',(-0.135174246449945,-0.06533764273189,
1.06247851744025));
#15579=CARTESIAN_POINT('Ctrl Pts',(-0.115079600404687,-0.0908043159161929,
1.06425052845252));
#15580=CARTESIAN_POINT('Ctrl Pts',(-0.0850581433982766,-0.128851596389654,
1.06689791782678));
#15581=CARTESIAN_POINT('Ctrl Pts',(-0.0342996944683099,-0.150536216937668,
1.06954530720104));
#15582=CARTESIAN_POINT('Ctrl Pts',(0.0139457694684962,-0.145925507476389,
1.0721926965753));
#15583=CARTESIAN_POINT('Ctrl Pts',(0.0621912334052997,-0.14131479801511,
1.07484008594956));
#15584=CARTESIAN_POINT('Ctrl Pts',(0.107923712348941,-0.110408758544542,
1.07748747532382));
#15585=CARTESIAN_POINT('Ctrl Pts',(0.1301953818052,-0.0673639426912374,
1.08013486469808));
#15586=CARTESIAN_POINT('Ctrl Pts',(0.15246705126146,-0.024319126837932,
1.08278225407234));
#15587=CARTESIAN_POINT('Ctrl Pts',(0.151277911230334,0.0308644653981125,
1.0854296434466));
#15588=CARTESIAN_POINT('Ctrl Pts',(0.127172648928576,0.0729099141598672,
1.08807703282086));
#15589=CARTESIAN_POINT('Ctrl Pts',(0.103067386626818,0.114955362921624,
1.09072442219512));
#15590=CARTESIAN_POINT('Ctrl Pts',(0.0560460020544268,0.143862668209093,
1.09337181156938));
#15591=CARTESIAN_POINT('Ctrl Pts',(0.00764670469074742,0.146390799320458,
1.09601920094364));
#15592=CARTESIAN_POINT('Ctrl Pts',(-0.0407525926729279,0.148918930431823,
1.0986665903179));
#15593=CARTESIAN_POINT('Ctrl Pts',(-0.0905298028278899,0.125067887367091,
1.10131397969216));
#15594=CARTESIAN_POINT('Ctrl Pts',(-0.11888440661962,0.0857626730052823,
1.10396136906642));
#15595=CARTESIAN_POINT('Ctrl Pts',(-0.136639133674055,0.0611510311732957,
1.10561907784952));
#15596=CARTESIAN_POINT('Ctrl Pts',(-0.145994366384503,0.0304800321277272,
1.10727678663261));
#15597=CARTESIAN_POINT('Ctrl Pts',(-0.146170555016798,-9.22629125885076E-5,
1.10893449541571));
#15598=CARTESIAN_POINT('Origin',(0.,0.,0.));
#15599=CARTESIAN_POINT('',(-0.146577386142569,-3.88073511912723E-5,1.16606550458429));
#15600=CARTESIAN_POINT('',(-0.146552328192774,-6.73160170860698E-5,1.15893449541571));
#15601=CARTESIAN_POINT('',(-0.14635,-1.79227059055215E-17,0.));
#15602=CARTESIAN_POINT('Ctrl Pts',(-0.146577386142569,-3.88073511912723E-5,
1.16606550458429));
#15603=CARTESIAN_POINT('Ctrl Pts',(-0.146413350709018,0.0463056768050285,
1.16353456384924));
#15604=CARTESIAN_POINT('Ctrl Pts',(-0.122574225104448,0.0927954474992645,
1.1610036231142));
#15605=CARTESIAN_POINT('Ctrl Pts',(-0.0847742546295189,0.119590709008994,
1.15847268237915));
#15606=CARTESIAN_POINT('Ctrl Pts',(-0.0452509303920754,0.147607604138013,
1.15582635250005));
#15607=CARTESIAN_POINT('Ctrl Pts',(0.00953524646069181,0.154093252855687,
1.15318002262095));
#15608=CARTESIAN_POINT('Ctrl Pts',(0.0545077808453859,0.136079071706768,
1.15053369274185));
#15609=CARTESIAN_POINT('Ctrl Pts',(0.0994803152300801,0.118064890557849,
1.14788736286275));
#15610=CARTESIAN_POINT('Ctrl Pts',(0.134639207146701,0.0755508795423365,
1.14524103298364));
#15611=CARTESIAN_POINT('Ctrl Pts',(0.14389167861853,0.027996370364851,1.14259470310454));
#15612=CARTESIAN_POINT('Ctrl Pts',(0.15314415009036,-0.0195581388126345,
1.13994837322544));
#15613=CARTESIAN_POINT('Ctrl Pts',(0.136490201117397,-0.0721531461520931,
1.13730204334634));
#15614=CARTESIAN_POINT('Ctrl Pts',(0.101552606157185,-0.105715089329518,
1.13465571346724));
#15615=CARTESIAN_POINT('Ctrl Pts',(0.0666150111969725,-0.139277032506943,
1.13200938358813));
#15616=CARTESIAN_POINT('Ctrl Pts',(0.0133937702495101,-0.153805911522335,
1.12936305370903));
#15617=CARTESIAN_POINT('Ctrl Pts',(-0.033750917386428,-0.142651629870951,
1.12671672382993));
#15618=CARTESIAN_POINT('Ctrl Pts',(-0.0808956050223675,-0.131497348219567,
1.12407039395083));
#15619=CARTESIAN_POINT('Ctrl Pts',(-0.121963739346782,-0.094659905901407,
1.12142406407173));
#15620=CARTESIAN_POINT('Ctrl Pts',(-0.1381577891642,-0.0490003798202082,
1.11877773419262));
#15621=CARTESIAN_POINT('Ctrl Pts',(-0.143690228857438,-0.0334015285560649,
1.11787365765651));
#15622=CARTESIAN_POINT('Ctrl Pts',(-0.146319518115206,-0.0167730178360648,
1.1169695811204));
#15623=CARTESIAN_POINT('Ctrl Pts',(-0.146204073634541,-0.000109175101205505,
1.11606550458429));
#15624=CARTESIAN_POINT('Ctrl Pts',(-0.146170555016798,-9.22629125885076E-5,
1.10893449541571));
#15625=CARTESIAN_POINT('Ctrl Pts',(-0.146275742653821,-0.0183444476975235,
1.10992417600687));
#15626=CARTESIAN_POINT('Ctrl Pts',(-0.143109248288425,-0.0365614514641733,
1.11091385659804));
#15627=CARTESIAN_POINT('Ctrl Pts',(-0.136505188007283,-0.0534328725168923,
1.1119035371892));
#15628=CARTESIAN_POINT('Ctrl Pts',(-0.118839368174718,-0.0985638180183679,
1.11455092656346));
#15629=CARTESIAN_POINT('Ctrl Pts',(-0.0765757310810901,-0.134066323362434,
1.11719831593772));
#15630=CARTESIAN_POINT('Ctrl Pts',(-0.0290731934694857,-0.143678417446031,
1.11984570531198));
#15631=CARTESIAN_POINT('Ctrl Pts',(0.01842934414212,-0.153290511529629,
1.12249309468624));
#15632=CARTESIAN_POINT('Ctrl Pts',(0.071170782271703,-0.137012194352758,
1.1251404840605));
#15633=CARTESIAN_POINT('Ctrl Pts',(0.10499283308901,-0.102299771349957,
1.12778787343476));
#15634=CARTESIAN_POINT('Ctrl Pts',(0.138814883906317,-0.0675873483471558,
1.13043526280902));
#15635=CARTESIAN_POINT('Ctrl Pts',(0.153717547411349,-0.0144408195184256,
1.13308265218328));
#15636=CARTESIAN_POINT('Ctrl Pts',(0.142874638214406,0.0327959749574983,
1.13573004155754));
#15637=CARTESIAN_POINT('Ctrl Pts',(0.132031729017462,0.0800327694334235,
1.1383774309318));
#15638=CARTESIAN_POINT('Ctrl Pts',(0.0954432471185425,0.121359829556542,
1.14102482030606));
#15639=CARTESIAN_POINT('Ctrl Pts',(0.0498685966661331,0.137847238945365,
1.14367220968032));
#15640=CARTESIAN_POINT('Ctrl Pts',(0.00429394621372511,0.154334648334189,
1.14631959905458));
#15641=CARTESIAN_POINT('Ctrl Pts',(-0.0502668727921719,0.145982406988718,
1.14896698842884));
#15642=CARTESIAN_POINT('Ctrl Pts',(-0.0888222026239048,0.116616270474356,
1.1516143778031));
#15643=CARTESIAN_POINT('Ctrl Pts',(-0.124357782404925,0.0895501633622979,
1.1540544170073));
#15644=CARTESIAN_POINT('Ctrl Pts',(-0.146296868742479,0.0446329749882746,
1.15649445621151));
#15645=CARTESIAN_POINT('Ctrl Pts',(-0.146552328192774,-6.73160170860698E-5,
1.15893449541571));
#15646=CARTESIAN_POINT('Origin',(0.,0.,0.));
#15647=CARTESIAN_POINT('',(-0.146318311025392,0.000133437649768732,1.21606550458429));
#15648=CARTESIAN_POINT('',(-0.146373054956946,0.000132657382717961,1.20893449541571));
#15649=CARTESIAN_POINT('',(-0.14635,-1.79227059055215E-17,0.));
#15650=CARTESIAN_POINT('Ctrl Pts',(-0.146318311025392,0.000133437649768732,
1.21606550458429));
#15651=CARTESIAN_POINT('Ctrl Pts',(-0.146429658069886,0.0125190846592594,
1.21539220633629));
#15652=CARTESIAN_POINT('Ctrl Pts',(-0.144988168643405,0.0248791929292086,
1.21471890808829));
#15653=CARTESIAN_POINT('Ctrl Pts',(-0.141892968227885,0.0368102906365087,
1.21404560984029));
#15654=CARTESIAN_POINT('Ctrl Pts',(-0.129727599662405,0.083704249513052,
1.21139927996119));
#15655=CARTESIAN_POINT('Ctrl Pts',(-0.0920156607298113,0.123970842060419,
1.20875295008209));
#15656=CARTESIAN_POINT('Ctrl Pts',(-0.0460184991925076,0.139179415364965,
1.20610662020299));
#15657=CARTESIAN_POINT('Ctrl Pts',(-2.13376552038805E-5,0.15438798866951,
1.20346029032389));
#15658=CARTESIAN_POINT('Ctrl Pts',(0.0542610464868107,0.144538542731236,
1.20081396044478));
#15659=CARTESIAN_POINT('Ctrl Pts',(0.091982751999895,0.114139323915075,
1.19816763056568));
#15660=CARTESIAN_POINT('Ctrl Pts',(0.129704457512977,0.0837401050989159,
1.19552130068658));
#15661=CARTESIAN_POINT('Ctrl Pts',(0.150865484397133,0.0327911134048729,
1.19287497080748));
#15662=CARTESIAN_POINT('Ctrl Pts',(0.145780097726084,-0.0153874961003253,
1.19022864092838));
#15663=CARTESIAN_POINT('Ctrl Pts',(0.140694711055036,-0.063566105605525,
1.18758231104927));
#15664=CARTESIAN_POINT('Ctrl Pts',(0.109362910828785,-0.108974332921877,
1.18493598117017));
#15665=CARTESIAN_POINT('Ctrl Pts',(0.0661257549466402,-0.130828118009858,
1.18228965129107));
#15666=CARTESIAN_POINT('Ctrl Pts',(0.0228885990644955,-0.152681903097838,
1.17964332141197));
#15667=CARTESIAN_POINT('Ctrl Pts',(-0.0322539124735426,-0.150981245957443,
1.17699699153287));
#15668=CARTESIAN_POINT('Ctrl Pts',(-0.0740621845924981,-0.126504564117865,
1.17435066165376));
#15669=CARTESIAN_POINT('Ctrl Pts',(-0.115870456711455,-0.102027882278287,
1.17170433177466));
#15670=CARTESIAN_POINT('Ctrl Pts',(-0.144344489411329,-0.0547751757395235,
1.16905800189556));
#15671=CARTESIAN_POINT('Ctrl Pts',(-0.146451269950206,-0.00637475169995868,
1.16641167201646));
#15672=CARTESIAN_POINT('Ctrl Pts',(-0.146543132875163,-0.00426432565444621,
1.1662962828724));
#15673=CARTESIAN_POINT('Ctrl Pts',(-0.146584864748453,-0.00215171749738942,
1.16618089372835));
#15674=CARTESIAN_POINT('Ctrl Pts',(-0.146577386142569,-3.88073511912723E-5,
1.16606550458429));
#15675=CARTESIAN_POINT('Ctrl Pts',(-0.146552328192774,-6.73160170860698E-5,
1.15893449541571));
#15676=CARTESIAN_POINT('Ctrl Pts',(-0.146574036680232,-0.00386586684592084,
1.15914184558577));
#15677=CARTESIAN_POINT('Ctrl Pts',(-0.1464391612665,-0.00766285139452399,
1.15934919575582));
#15678=CARTESIAN_POINT('Ctrl Pts',(-0.146142739258869,-0.0114471821958193,
1.15955654592588));
#15679=CARTESIAN_POINT('Ctrl Pts',(-0.142358105404532,-0.0597644666683822,
1.16220393530014));
#15680=CARTESIAN_POINT('Ctrl Pts',(-0.112238997038288,-0.106019003930254,
1.1648513246744));
#15681=CARTESIAN_POINT('Ctrl Pts',(-0.0695815129186611,-0.129023839960917,
1.16749871404866));
#15682=CARTESIAN_POINT('Ctrl Pts',(-0.026924028799035,-0.15202867599158,
1.17014610342292));
#15683=CARTESIAN_POINT('Ctrl Pts',(0.0282718310739737,-0.151783810791035,
1.17279349279718));
#15684=CARTESIAN_POINT('Ctrl Pts',(0.0707235276354612,-0.128401405199111,
1.17544088217144));
#15685=CARTESIAN_POINT('Ctrl Pts',(0.11317522419695,-0.105018999607187,
1.1780882715457));
#15686=CARTESIAN_POINT('Ctrl Pts',(0.142882757446916,-0.0584990536238821,
1.18073566091996));
#15687=CARTESIAN_POINT('Ctrl Pts',(0.146238551171451,-0.0101500920973681,
1.18338305029422));
#15688=CARTESIAN_POINT('Ctrl Pts',(0.149594344895986,0.0381988694291446,
1.18603043966848));
#15689=CARTESIAN_POINT('Ctrl Pts',(0.12659839909509,0.0883768464988665,
1.18867782904274));
#15690=CARTESIAN_POINT('Ctrl Pts',(0.0877840381772113,0.117399748124142,
1.191325218417));
#15691=CARTESIAN_POINT('Ctrl Pts',(0.0489696772593311,0.146422649749419,
1.19397260779126));
#15692=CARTESIAN_POINT('Ctrl Pts',(-0.00566309877553352,0.154290475930249,
1.19661999716552));
#15693=CARTESIAN_POINT('Ctrl Pts',(-0.0510896721842483,0.137399358129564,
1.19926738653978));
#15694=CARTESIAN_POINT('Ctrl Pts',(-0.0965162455929618,0.12050824032888,
1.20191477591404));
#15695=CARTESIAN_POINT('Ctrl Pts',(-0.132736616375526,0.0788581785466829,
1.2045621652883));
#15696=CARTESIAN_POINT('Ctrl Pts',(-0.143159994183491,0.0315270405159292,
1.20720955466256));
#15697=CARTESIAN_POINT('Ctrl Pts',(-0.145423823013163,0.021247302336111,
1.20778453491361));
#15698=CARTESIAN_POINT('Ctrl Pts',(-0.146470795531708,0.0106995851133921,
1.20835951516466));
#15699=CARTESIAN_POINT('Ctrl Pts',(-0.146373054956946,0.000132657382717961,
1.20893449541571));
#15700=CARTESIAN_POINT('Origin',(0.,0.,0.));
#15701=CARTESIAN_POINT('',(-0.146120596765396,-4.14129048147555E-5,1.26606550458429));
#15702=CARTESIAN_POINT('',(-0.146109918970638,-1.0198006988139E-5,1.25893449541571));
#15703=CARTESIAN_POINT('',(-0.14635,-1.79227059055215E-17,0.));
#15704=CARTESIAN_POINT('Ctrl Pts',(-0.146120596765396,-4.14129048147555E-5,
1.26606550458429));
#15705=CARTESIAN_POINT('Ctrl Pts',(-0.14605219935785,0.0269443530192317,
1.26460351894424));
#15706=CARTESIAN_POINT('Ctrl Pts',(-0.138898723445843,0.053963836666407,
1.26314153330418));
#15707=CARTESIAN_POINT('Ctrl Pts',(-0.124882896249422,0.0767650581554474,
1.26167954766413));
#15708=CARTESIAN_POINT('Ctrl Pts',(-0.0995129464537159,0.118037388097231,
1.25903321778503));
#15709=CARTESIAN_POINT('Ctrl Pts',(-0.051658938874944,0.145488850208621,
1.25638688790592));
#15710=CARTESIAN_POINT('Ctrl Pts',(-0.00322440565727106,0.146554478394238,
1.25374055802682));
#15711=CARTESIAN_POINT('Ctrl Pts',(0.0452101275604033,0.147620106579856,
1.25109422814772));
#15712=CARTESIAN_POINT('Ctrl Pts',(0.0942251864169787,0.122299900839699,
1.24844789826862));
#15713=CARTESIAN_POINT('Ctrl Pts',(0.121385807331354,0.0821833176976391,
1.24580156838952));
#15714=CARTESIAN_POINT('Ctrl Pts',(0.148546428245729,0.0420667345555804,
1.24315523851041));
#15715=CARTESIAN_POINT('Ctrl Pts',(0.153852611217905,-0.0128462259883804,
1.24050890863131));
#15716=CARTESIAN_POINT('Ctrl Pts',(0.134875632820701,-0.0574210379606392,
1.23786257875221));
#15717=CARTESIAN_POINT('Ctrl Pts',(0.115898654423498,-0.101995849932898,
1.23521624887311));
#15718=CARTESIAN_POINT('Ctrl Pts',(0.0726385146569148,-0.136232513333455,
1.23256991899401));
#15719=CARTESIAN_POINT('Ctrl Pts',(0.0248960600935515,-0.144460368686643,
1.2299235891149));
#15720=CARTESIAN_POINT('Ctrl Pts',(-0.0228463944698117,-0.152688224039831,
1.2272772592358));
#15721=CARTESIAN_POINT('Ctrl Pts',(-0.0750711638299551,-0.134907271345651,
1.2246309293567));
#15722=CARTESIAN_POINT('Ctrl Pts',(-0.107874149410843,-0.0992561323957017,
1.2219845994776));
#15723=CARTESIAN_POINT('Ctrl Pts',(-0.132331163880887,-0.072675612185966,
1.2200115678465));
#15724=CARTESIAN_POINT('Ctrl Pts',(-0.145992019903337,-0.0361614337449312,
1.21803853621539));
#15725=CARTESIAN_POINT('Ctrl Pts',(-0.146318311025392,0.000133437649768732,
1.21606550458429));
#15726=CARTESIAN_POINT('Ctrl Pts',(-0.146373054956946,0.000132657382717961,
1.20893449541571));
#15727=CARTESIAN_POINT('Ctrl Pts',(-0.146020767276673,-0.0379538636644633,
1.21100690453892));
#15728=CARTESIAN_POINT('Ctrl Pts',(-0.130797424420382,-0.0762899498869128,
1.21307931366213));
#15729=CARTESIAN_POINT('Ctrl Pts',(-0.104081054125652,-0.103227285106232,
1.21515172278534));
#15730=CARTESIAN_POINT('Ctrl Pts',(-0.0699523514264828,-0.137638258418326,
1.2177991121596));
#15731=CARTESIAN_POINT('Ctrl Pts',(-0.0170685611947798,-0.153447990763203,
1.22044650153386));
#15732=CARTESIAN_POINT('Ctrl Pts',(0.0303468241642401,-0.143414812629152,
1.22309389090812));
#15733=CARTESIAN_POINT('Ctrl Pts',(0.0777622095232573,-0.133381634495101,
1.22574128028238));
#15734=CARTESIAN_POINT('Ctrl Pts',(0.119709190009594,-0.0975055458821257,
1.22838866965664));
#15735=CARTESIAN_POINT('Ctrl Pts',(0.136973893871985,-0.052219638220276,
1.2310360590309));
#15736=CARTESIAN_POINT('Ctrl Pts',(0.154238597734379,-0.00693373055842239,
1.23368344840516));
#15737=CARTESIAN_POINT('Ctrl Pts',(0.146821024972825,0.0477619961523044,
1.23633083777942));
#15738=CARTESIAN_POINT('Ctrl Pts',(0.118118804930222,0.0868140895256425,
1.23897822715368));
#15739=CARTESIAN_POINT('Ctrl Pts',(0.0894165848876198,0.125866182898978,
1.24162561652794));
#15740=CARTESIAN_POINT('Ctrl Pts',(0.0394297175639698,0.149274642934924,
1.2442730059022));
#15741=CARTESIAN_POINT('Ctrl Pts',(-0.00894524413350711,0.146317192515786,
1.24692039527646));
#15742=CARTESIAN_POINT('Ctrl Pts',(-0.0573202058309854,0.143359742096648,
1.24956778465072));
#15743=CARTESIAN_POINT('Ctrl Pts',(-0.104083261902292,0.114036381222425,
1.25221517402498));
#15744=CARTESIAN_POINT('Ctrl Pts',(-0.127814530591109,0.0717787154251623,
1.25486256339924));
#15745=CARTESIAN_POINT('Ctrl Pts',(-0.139981499518435,0.0501133037087236,
1.2562198740714));
#15746=CARTESIAN_POINT('Ctrl Pts',(-0.146094355379323,0.0250479932723348,
1.25757718474355));
#15747=CARTESIAN_POINT('Ctrl Pts',(-0.146109918970638,-1.0198006988139E-5,
1.25893449541571));
#15748=CARTESIAN_POINT('Origin',(0.,0.,0.));
#15749=CARTESIAN_POINT('',(-0.146470135615938,-0.000111966546850736,1.31606550458429));
#15750=CARTESIAN_POINT('',(-0.146410535958061,-0.000127756381200432,1.30893449541571));
#15751=CARTESIAN_POINT('',(-0.14635,-1.79227059055215E-17,0.));
#15752=CARTESIAN_POINT('Ctrl Pts',(-0.146470135615938,-0.000111966546850736,
1.31606550458429));
#15753=CARTESIAN_POINT('Ctrl Pts',(-0.146120207411574,0.0411799307449602,
1.31381483155218));
#15754=CARTESIAN_POINT('Ctrl Pts',(-0.127827491572984,0.0827431563937987,
1.31156415852007));
#15755=CARTESIAN_POINT('Ctrl Pts',(-0.0969137672218927,0.10998333351997,
1.30931348548796));
#15756=CARTESIAN_POINT('Ctrl Pts',(-0.0605655677022408,0.142012194937238,
1.30666715560886));
#15757=CARTESIAN_POINT('Ctrl Pts',(-0.00676890401288169,0.154239532672684,
1.30402082572976));
#15758=CARTESIAN_POINT('Ctrl Pts',(0.0398526445220406,0.14106870189023,
1.30137449585066));
#15759=CARTESIAN_POINT('Ctrl Pts',(0.0864741930569617,0.127897871107775,
1.29872816597155));
#15760=CARTESIAN_POINT('Ctrl Pts',(0.125920626437448,0.0893288718074177,
1.29608183609245));
#15761=CARTESIAN_POINT('Ctrl Pts',(0.14013669149516,0.0430153417578024,
1.29343550621335));
#15762=CARTESIAN_POINT('Ctrl Pts',(0.154352756552873,-0.00329818829181684,
1.29078917633425));
#15763=CARTESIAN_POINT('Ctrl Pts',(0.143338453287813,-0.0573562490906975,
1.28814284645515));
#15764=CARTESIAN_POINT('Ctrl Pts',(0.112135201594409,-0.0944156157243562,
1.28549651657604));
#15765=CARTESIAN_POINT('Ctrl Pts',(0.0809319499010078,-0.131474982358013,
1.28285018669694));
#15766=CARTESIAN_POINT('Ctrl Pts',(0.0295397497792676,-0.151535654826449,
1.28020385681784));
#15767=CARTESIAN_POINT('Ctrl Pts',(-0.0185183802362589,-0.1454155477333,
1.27755752693874));
#15768=CARTESIAN_POINT('Ctrl Pts',(-0.066576510251784,-0.139295440640151,
1.27491119705964));
#15769=CARTESIAN_POINT('Ctrl Pts',(-0.111300570161094,-0.106994553985419,
1.27226486718053));
#15770=CARTESIAN_POINT('Ctrl Pts',(-0.13221965410943,-0.0632975117719662,
1.26961853730143));
#15771=CARTESIAN_POINT('Ctrl Pts',(-0.141581826511298,-0.0437412423069929,
1.26843419306239));
#15772=CARTESIAN_POINT('Ctrl Pts',(-0.146176005022067,-0.0219023912433209,
1.26724984882334));
#15773=CARTESIAN_POINT('Ctrl Pts',(-0.146120596765396,-4.14129048147555E-5,
1.26606550458429));
#15774=CARTESIAN_POINT('Ctrl Pts',(-0.146109918970638,-1.0198006988139E-5,
1.25893449541571));
#15775=CARTESIAN_POINT('Ctrl Pts',(-0.146124711647138,-0.0238271763493914,
1.26022457411781));
#15776=CARTESIAN_POINT('Ctrl Pts',(-0.140631289159497,-0.0476377233371588,
1.26151465281992));
#15777=CARTESIAN_POINT('Ctrl Pts',(-0.129592576141605,-0.0685164391025303,
1.26280473152202));
#15778=CARTESIAN_POINT('Ctrl Pts',(-0.106939871696956,-0.111361957112663,
1.26545212089628));
#15779=CARTESIAN_POINT('Ctrl Pts',(-0.0609349815013302,-0.141861022412626,
1.26809951027054));
#15780=CARTESIAN_POINT('Ctrl Pts',(-0.0126505083952331,-0.146043496451057,
1.2707468996448));
#15781=CARTESIAN_POINT('Ctrl Pts',(0.0356339647108625,-0.150225970489488,
1.27339428901906));
#15782=CARTESIAN_POINT('Ctrl Pts',(0.0861980207274291,-0.128091853266388,
1.27604167839332));
#15783=CARTESIAN_POINT('Ctrl Pts',(0.11588072467734,-0.0897797074320025,
1.27868906776758));
#15784=CARTESIAN_POINT('Ctrl Pts',(0.145563428627253,-0.0514675615976161,
1.28133645714184));
#15785=CARTESIAN_POINT('Ctrl Pts',(0.154364780510509,0.00302261284805656,
1.2839838465161));
#15786=CARTESIAN_POINT('Ctrl Pts',(0.138253309066183,0.0487315170146188,
1.28663123589036));
#15787=CARTESIAN_POINT('Ctrl Pts',(0.122141837621857,0.0944404211811797,
1.28927862526462));
#15788=CARTESIAN_POINT('Ctrl Pts',(0.0811175428499519,0.131368055068631,
1.29192601463888));
#15789=CARTESIAN_POINT('Ctrl Pts',(0.0339716590485425,0.142599665496764,
1.29457340401314));
#15790=CARTESIAN_POINT('Ctrl Pts',(-0.013174224752867,0.153831275924897,
1.2972207933874));
#15791=CARTESIAN_POINT('Ctrl Pts',(-0.0664416975837803,0.139366862893713,
1.29986818276166));
#15792=CARTESIAN_POINT('Ctrl Pts',(-0.101431520699135,0.105831870563862,
1.30251557213592));
#15793=CARTESIAN_POINT('Ctrl Pts',(-0.129710573305276,0.0787286237393239,
1.30465521322918));
#15794=CARTESIAN_POINT('Ctrl Pts',(-0.146050663974784,0.0391684733249047,
1.30679485432245));
#15795=CARTESIAN_POINT('Ctrl Pts',(-0.146410535958061,-0.000127756381200432,
1.30893449541571));
#15796=CARTESIAN_POINT('Origin',(0.,0.,0.));
#15797=CARTESIAN_POINT('',(-0.146471469669193,0.000111495080380188,1.36606550458429));
#15798=CARTESIAN_POINT('',(-0.146526884620975,8.5711493927648E-5,1.35893449541571));
#15799=CARTESIAN_POINT('',(-0.14635,-1.79227059055215E-17,0.));
#15800=CARTESIAN_POINT('Ctrl Pts',(-0.146471469669193,0.000111495080380188,
1.36606550458429));
#15801=CARTESIAN_POINT('Ctrl Pts',(-0.146532402405025,0.0073220458586883,
1.36567247403923));
#15802=CARTESIAN_POINT('Ctrl Pts',(-0.146045973070864,0.0145243451116175,
1.36527944349416));
#15803=CARTESIAN_POINT('Ctrl Pts',(-0.144983764805735,0.0216407019395156,
1.3648864129491));
#15804=CARTESIAN_POINT('Ctrl Pts',(-0.137831767320671,0.0695561322809842,
1.36224008307));
#15805=CARTESIAN_POINT('Ctrl Pts',(-0.104576727819841,0.113575347233418,
1.3595937531909));
#15806=CARTESIAN_POINT('Ctrl Pts',(-0.060440002550743,0.133550058215342,
1.3569474233118));
#15807=CARTESIAN_POINT('Ctrl Pts',(-0.0163032772816473,0.153524769197265,
1.35430109343269));
#15808=CARTESIAN_POINT('Ctrl Pts',(0.0387151337557165,0.149454976208681,
1.35165476355359));
#15809=CARTESIAN_POINT('Ctrl Pts',(0.0794324390145508,0.123203488242689,
1.34900843367449));
#15810=CARTESIAN_POINT('Ctrl Pts',(0.120149744273387,0.0969520002766962,
1.34636210379539));
#15811=CARTESIAN_POINT('Ctrl Pts',(0.146565943753694,0.048518817333291,
1.34371577391629));
#15812=CARTESIAN_POINT('Ctrl Pts',(0.14658992694451,7.25688577880009E-5,
1.34106944403718));
#15813=CARTESIAN_POINT('Ctrl Pts',(0.146613910135327,-0.0483736796177136,
1.33842311415808));
#15814=CARTESIAN_POINT('Ctrl Pts',(0.120245677036657,-0.0968329936253116,
1.33577678427898));
#15815=CARTESIAN_POINT('Ctrl Pts',(0.0795543829983497,-0.123124782547022,
1.33313045439988));
#15816=CARTESIAN_POINT('Ctrl Pts',(0.0388630889600415,-0.149416571468734,
1.33048412452078));
#15817=CARTESIAN_POINT('Ctrl Pts',(-0.0161512660179049,-0.153540835304554,
1.32783779464168));
#15818=CARTESIAN_POINT('Ctrl Pts',(-0.0603077462478081,-0.133609833714981,
1.32519146476257));
#15819=CARTESIAN_POINT('Ctrl Pts',(-0.10446422647771,-0.113678832125408,
1.32254513488347));
#15820=CARTESIAN_POINT('Ctrl Pts',(-0.137762831959571,-0.0696925651104417,
1.31989880500437));
#15821=CARTESIAN_POINT('Ctrl Pts',(-0.144962267025529,-0.0217842390534145,
1.31725247512527));
#15822=CARTESIAN_POINT('Ctrl Pts',(-0.146038665626028,-0.0146213916011371,
1.31685681827827));
#15823=CARTESIAN_POINT('Ctrl Pts',(-0.146531651210624,-0.00737087161912708,
1.31646116143128));
#15824=CARTESIAN_POINT('Ctrl Pts',(-0.146470135615938,-0.000111966546850736,
1.31606550458429));
#15825=CARTESIAN_POINT('Ctrl Pts',(-0.146410535958061,-0.000127756381200432,
1.30893449541571));
#15826=CARTESIAN_POINT('Ctrl Pts',(-0.146495935505426,-0.00945296197092968,
1.30944224369671));
#15827=CARTESIAN_POINT('Ctrl Pts',(-0.145681427739287,-0.018763305174839,
1.3099499919777));
#15828=CARTESIAN_POINT('Ctrl Pts',(-0.143913007029536,-0.0278887903271487,
1.3104577402587));
#15829=CARTESIAN_POINT('Ctrl Pts',(-0.134692496844786,-0.0754688872597875,
1.31310512963296));
#15830=CARTESIAN_POINT('Ctrl Pts',(-0.0995393030754929,-0.118023509496548,
1.31575251900722));
#15831=CARTESIAN_POINT('Ctrl Pts',(-0.0545553941775042,-0.136060454153345,
1.31839990838148));
#15832=CARTESIAN_POINT('Ctrl Pts',(-0.00957148527951295,-0.154097398810142,
1.32104729775574));
#15833=CARTESIAN_POINT('Ctrl Pts',(0.0452431387471776,-0.14761666588697,
1.32369468713));
#15834=CARTESIAN_POINT('Ctrl Pts',(0.0847805644327026,-0.119586763955155,
1.32634207650426));
#15835=CARTESIAN_POINT('Ctrl Pts',(0.124317990118227,-0.09155686202334,
1.32898946587852));
#15836=CARTESIAN_POINT('Ctrl Pts',(0.148578217462589,-0.041977791082884,
1.33163685525278));
#15837=CARTESIAN_POINT('Ctrl Pts',(0.146448816178573,0.00644068764408242,
1.33428424462704));
#15838=CARTESIAN_POINT('Ctrl Pts',(0.144319414894557,0.0548591663710502,
1.3369316340013));
#15839=CARTESIAN_POINT('Ctrl Pts',(0.115800384982161,0.102117052884526,
1.33957902337556));
#15840=CARTESIAN_POINT('Ctrl Pts',(0.0739549070570988,0.126567807678519,
1.34222641274982));
#15841=CARTESIAN_POINT('Ctrl Pts',(0.0321094291320376,0.151018562472512,
1.34487380212408));
#15842=CARTESIAN_POINT('Ctrl Pts',(-0.0230624968056921,0.152662185547021,
1.34752119149834));
#15843=CARTESIAN_POINT('Ctrl Pts',(-0.0662892946253695,0.1307458130856,
1.3501685808726));
#15844=CARTESIAN_POINT('Ctrl Pts',(-0.109516092445046,0.10882944062418,
1.35281597024686));
#15845=CARTESIAN_POINT('Ctrl Pts',(-0.140797762146673,0.0633530726268328,
1.35546335962112));
#15846=CARTESIAN_POINT('Ctrl Pts',(-0.145805692234247,0.0151472216574969,
1.35811074899538));
#15847=CARTESIAN_POINT('Ctrl Pts',(-0.146325105122407,0.0101474034011793,
1.35838533113549));
#15848=CARTESIAN_POINT('Ctrl Pts',(-0.146561879835735,0.00511822289583405,
1.3586599132756));
#15849=CARTESIAN_POINT('Ctrl Pts',(-0.146526884620975,8.5711493927648E-5,
1.35893449541571));
#15850=CARTESIAN_POINT('Origin',(0.,0.,0.));
#15851=CARTESIAN_POINT('',(-0.146120987371435,4.2191387702159E-5,1.41606550458429));
#15852=CARTESIAN_POINT('',(-0.146148882937928,7.6306569664006E-5,1.40893449541571));
#15853=CARTESIAN_POINT('',(-0.14635,-1.79227059055215E-17,0.));
#15854=CARTESIAN_POINT('Ctrl Pts',(-0.146120987371435,4.2191387702159E-5,
1.41606550458429));
#15855=CARTESIAN_POINT('Ctrl Pts',(-0.146177309023295,0.021854523983563,
1.41488378664717));
#15856=CARTESIAN_POINT('Ctrl Pts',(-0.141604359564088,0.0436444172696427,
1.41370206871005));
#15857=CARTESIAN_POINT('Ctrl Pts',(-0.132282279973341,0.0631665524487371,
1.41252035077294));
#15858=CARTESIAN_POINT('Ctrl Pts',(-0.1114064880593,0.106884268839086,1.40987402089383));
#15859=CARTESIAN_POINT('Ctrl Pts',(-0.0667143915920224,0.139229456738304,
1.40722769101473));
#15860=CARTESIAN_POINT('Ctrl Pts',(-0.0186623352932378,0.145397151366753,
1.40458136113563));
#15861=CARTESIAN_POINT('Ctrl Pts',(0.0293897210055454,0.151564845995202,
1.40193503125653));
#15862=CARTESIAN_POINT('Ctrl Pts',(0.0808017371358351,0.131555047352884,
1.39928870137743));
#15863=CARTESIAN_POINT('Ctrl Pts',(0.112041660826149,0.0945265884816804,
1.39664237149832));
#15864=CARTESIAN_POINT('Ctrl Pts',(0.143281584516463,0.0574981296104763,
1.39399604161922));
#15865=CARTESIAN_POINT('Ctrl Pts',(0.154349415766802,0.00345101051038574,
1.39134971174012));
#15866=CARTESIAN_POINT('Ctrl Pts',(0.140179214932283,-0.0428765696854336,
1.38870338186102));
#15867=CARTESIAN_POINT('Ctrl Pts',(0.126009014097764,-0.089204149881253,
1.38605705198192));
#15868=CARTESIAN_POINT('Ctrl Pts',(0.0866007811783877,-0.127812191172801,
1.38341072210282));
#15869=CARTESIAN_POINT('Ctrl Pts',(0.0399922944706322,-0.14102917638501,
1.38076439222371));
#15870=CARTESIAN_POINT('Ctrl Pts',(-0.00661619223712474,-0.15424616159722,
1.37811806234461));
#15871=CARTESIAN_POINT('Ctrl Pts',(-0.060424932733261,-0.142072090730089,
1.37547173246551));
#15872=CARTESIAN_POINT('Ctrl Pts',(-0.0968048252466797,-0.110079232431271,
1.37282540258641));
#15873=CARTESIAN_POINT('Ctrl Pts',(-0.127781608685608,-0.08283792481198,
1.37057210325237));
#15874=CARTESIAN_POINT('Ctrl Pts',(-0.146122133733866,-0.0412276055847571,
1.36831880391833));
#15875=CARTESIAN_POINT('Ctrl Pts',(-0.146471469669193,0.000111495080380188,
1.36606550458429));
#15876=CARTESIAN_POINT('Ctrl Pts',(-0.146526884620975,8.5711493927648E-5,
1.35893449541571));
#15877=CARTESIAN_POINT('Ctrl Pts',(-0.146224472749943,-0.0434028397118431,
1.36130730264986));
#15878=CARTESIAN_POINT('Ctrl Pts',(-0.125627402569456,-0.0871401285467012,
1.36368010988401));
#15879=CARTESIAN_POINT('Ctrl Pts',(-0.0917490966422633,-0.114327780902106,
1.36605291711816));
#15880=CARTESIAN_POINT('Ctrl Pts',(-0.0539503804891888,-0.144661598551044,
1.36870030649242));
#15881=CARTESIAN_POINT('Ctrl Pts',(0.00038124229047478,-0.154393899907594,
1.37134769586668));
#15882=CARTESIAN_POINT('Ctrl Pts',(0.0463590973565905,-0.139066790892088,
1.37399508524094));
#15883=CARTESIAN_POINT('Ctrl Pts',(0.0923369524227062,-0.123739681876581,
1.3766424746152));
#15884=CARTESIAN_POINT('Ctrl Pts',(0.129961039775272,-0.083353162489017,
1.37928986398946));
#15885=CARTESIAN_POINT('Ctrl Pts',(0.141997595260484,-0.0364063334065561,
1.38193725336372));
#15886=CARTESIAN_POINT('Ctrl Pts',(0.154034150745695,0.0105404956759021,
1.38458464273798));
#15887=CARTESIAN_POINT('Ctrl Pts',(0.140483174363557,0.0640476344532581,
1.38723203211224));
#15888=CARTESIAN_POINT('Ctrl Pts',(0.10755170844225,0.0996060653705087,
1.3898794214865));
#15889=CARTESIAN_POINT('Ctrl Pts',(0.0746202425209409,0.135164496287762,
1.39252681086076));
#15890=CARTESIAN_POINT('Ctrl Pts',(0.0223082870604623,0.152774219344908,
1.39517420023502));
#15891=CARTESIAN_POINT('Ctrl Pts',(-0.025422593472234,0.144369075867769,
1.39782158960928));
#15892=CARTESIAN_POINT('Ctrl Pts',(-0.073153474004929,0.135963932390631,
1.40046897898354));
#15893=CARTESIAN_POINT('Ctrl Pts',(-0.11630327960984,0.101543922379208,
1.4031163683578));
#15894=CARTESIAN_POINT('Ctrl Pts',(-0.135107186188192,0.0568751802851974,
1.40576375773206));
#15895=CARTESIAN_POINT('Ctrl Pts',(-0.142614236437708,0.0390421576584788,
1.40682067029328));
#15896=CARTESIAN_POINT('Ctrl Pts',(-0.14624095998336,0.0195756595648056,
1.40787758285449));
#15897=CARTESIAN_POINT('Ctrl Pts',(-0.146148882937928,7.6306569664006E-5,
1.40893449541571));
#15898=CARTESIAN_POINT('Origin',(0.,0.,0.));
#15899=CARTESIAN_POINT('',(-0.14631473222987,-0.000131398079681141,1.46606550458429));
#15900=CARTESIAN_POINT('',(-0.146248097568756,-0.000123763188177425,1.45893449541571));
#15901=CARTESIAN_POINT('',(-0.14635,-1.79227059055215E-17,0.));
#15902=CARTESIAN_POINT('Ctrl Pts',(-0.14631473222987,-0.000131398079681141,
1.46606550458429));
#15903=CARTESIAN_POINT('Ctrl Pts',(-0.145989697979493,0.0361157155227289,
1.46409509925512));
#15904=CARTESIAN_POINT('Ctrl Pts',(-0.132370868650209,0.0725796635271419,
1.46212469392594));
#15905=CARTESIAN_POINT('Ctrl Pts',(-0.107973319296019,0.0991484059484618,
1.46015428859677));
#15906=CARTESIAN_POINT('Ctrl Pts',(-0.0752064754000165,0.134831245351468,
1.45750795871767));
#15907=CARTESIAN_POINT('Ctrl Pts',(-0.0229974942306327,0.152665588379184,
1.45486162883857));
#15908=CARTESIAN_POINT('Ctrl Pts',(0.0247535192036911,0.144485406820094,
1.45221529895946));
#15909=CARTESIAN_POINT('Ctrl Pts',(0.0725045326380122,0.136305225261004,
1.44956896908036));
#15910=CARTESIAN_POINT('Ctrl Pts',(0.115797578337275,0.102110519115111,
1.44692263920126));
#15911=CARTESIAN_POINT('Ctrl Pts',(0.134818450998255,0.0575543070937695,
1.44427630932216));
#15912=CARTESIAN_POINT('Ctrl Pts',(0.153839323659235,0.0129980950724284,
1.44162997944306));
#15913=CARTESIAN_POINT('Ctrl Pts',(0.148588023281934,-0.0419196228243577,
1.43898364956396));
#15914=CARTESIAN_POINT('Ctrl Pts',(0.121467255745355,-0.082062966762292,
1.43633731968485));
#15915=CARTESIAN_POINT('Ctrl Pts',(0.0943464882087764,-0.122206310700226,
1.43369098980575));
#15916=CARTESIAN_POINT('Ctrl Pts',(0.0453562535129183,-0.147575280679306,
1.43104465992665));
#15917=CARTESIAN_POINT('Ctrl Pts',(-0.00307937473935208,-0.146557666176543,
1.42839833004755));
#15918=CARTESIAN_POINT('Ctrl Pts',(-0.0515150029916225,-0.14554005167378,
1.42575200016845));
#15919=CARTESIAN_POINT('Ctrl Pts',(-0.0993960248003067,-0.118135852689175,
1.42310567028934));
#15920=CARTESIAN_POINT('Ctrl Pts',(-0.124806792024246,-0.0768886307561326,
1.42045934041024));
#15921=CARTESIAN_POINT('Ctrl Pts',(-0.138870387581649,-0.0540603453281256,
1.41899472846826));
#15922=CARTESIAN_POINT('Ctrl Pts',(-0.146051182757901,-0.0269918425378075,
1.41753011652627));
#15923=CARTESIAN_POINT('Ctrl Pts',(-0.146120987371435,4.2191387702159E-5,
1.41606550458429));
#15924=CARTESIAN_POINT('Ctrl Pts',(-0.146148882937928,7.6306569664006E-5,
1.40893449541571));
#15925=CARTESIAN_POINT('Ctrl Pts',(-0.146010322369016,-0.0292669616874671,
1.41052497222875));
#15926=CARTESIAN_POINT('Ctrl Pts',(-0.137450455640384,-0.0586846305953837,
1.4121154490418));
#15927=CARTESIAN_POINT('Ctrl Pts',(-0.121019719714466,-0.0827222215753489,
1.41370592585484));
#15928=CARTESIAN_POINT('Ctrl Pts',(-0.0936703391105966,-0.122733407165291,
1.4163533152291));
#15929=CARTESIAN_POINT('Ctrl Pts',(-0.0445135703510636,-0.147838304168576,
1.41900070460336));
#15930=CARTESIAN_POINT('Ctrl Pts',(0.00393424939099551,-0.146537573651384,
1.42164809397762));
#15931=CARTESIAN_POINT('Ctrl Pts',(0.0523820691330518,-0.145236843134192,
1.42429548335188));
#15932=CARTESIAN_POINT('Ctrl Pts',(0.100120939857634,-0.117530485096527,
1.42694287272614));
#15933=CARTESIAN_POINT('Ctrl Pts',(0.125284029446909,-0.0761094471358441,
1.4295902621004));
#15934=CARTESIAN_POINT('Ctrl Pts',(0.150447119036187,-0.0346884091751576,
1.43223765147466));
#15935=CARTESIAN_POINT('Ctrl Pts',(0.153034427490153,0.020447308708549,
1.43488504084892));
#15936=CARTESIAN_POINT('Ctrl Pts',(0.13186079120536,0.0640427391611241,
1.43753243022318));
#15937=CARTESIAN_POINT('Ctrl Pts',(0.110687154920568,0.107638169613697,
1.44017981959744));
#15938=CARTESIAN_POINT('Ctrl Pts',(0.0657525738970213,0.139693312635139,
1.4428272089717));
#15939=CARTESIAN_POINT('Ctrl Pts',(0.0176394768514684,0.145525221357757,
1.44547459834596));
#15940=CARTESIAN_POINT('Ctrl Pts',(-0.0304736201940859,0.151357130080375,
1.44812198772022));
#15941=CARTESIAN_POINT('Ctrl Pts',(-0.0817652332616461,0.130965804504167,
1.45076937709448));
#15942=CARTESIAN_POINT('Ctrl Pts',(-0.112741325423428,0.0936916042199666,
1.45341676646874));
#15943=CARTESIAN_POINT('Ctrl Pts',(-0.134261605244105,0.0677957870194472,
1.45525600945106));
#15944=CARTESIAN_POINT('Ctrl Pts',(-0.145976367207401,0.0337512577971725,
1.45709525243339));
#15945=CARTESIAN_POINT('Ctrl Pts',(-0.146248097568756,-0.000123763188177425,
1.45893449541571));
#15946=CARTESIAN_POINT('Origin',(0.,0.,-0.0924367114736175));
#15947=CARTESIAN_POINT('',(-0.117746618301147,-0.000105742458702955,1.48256328852638));
#15948=CARTESIAN_POINT('',(-0.117971241274414,-5.28325160115065E-6,1.49243671147361));
#15949=CARTESIAN_POINT('',(-0.117775,2.85464118895969E-14,-0.0924367114736175));
#15950=CARTESIAN_POINT('',(-0.117668597464313,0.00500517689812599,1.532225));
#15951=CARTESIAN_POINT('Ctrl Pts',(-0.117746618301147,-0.000105742458702949,
1.48256328852638));
#15952=CARTESIAN_POINT('Ctrl Pts',(-0.117836347163251,-0.0101121102621826,
1.48323921307631));
#15953=CARTESIAN_POINT('Ctrl Pts',(-0.112089674709738,-0.0591937430214443,
1.48656146750534));
#15954=CARTESIAN_POINT('Ctrl Pts',(-0.0435804807853106,-0.132222740314769,
1.49253005181348));
#15955=CARTESIAN_POINT('Ctrl Pts',(0.0874774386997331,-0.108286040948335,
1.50046904145078));
#15956=CARTESIAN_POINT('Ctrl Pts',(0.138385550162814,0.0147146982980264,
1.50840803108809));
#15957=CARTESIAN_POINT('Ctrl Pts',(0.0627460642121078,0.124368470664037,
1.51634702072539));
#15958=CARTESIAN_POINT('Ctrl Pts',(-0.0706026869052757,0.119928391791904,
1.5242860103627));
#15959=CARTESIAN_POINT('Ctrl Pts',(-0.116004137797729,0.0441355889673283,
1.5295786701209));
#15960=CARTESIAN_POINT('Ctrl Pts',(-0.117668597464313,0.00500517689812487,
1.532225));
#15961=CARTESIAN_POINT('',(-0.0334019664627544,0.1129391839063,1.53222500000001));
#15962=CARTESIAN_POINT('Origin',(0.,0.,1.532225));
#15963=CARTESIAN_POINT('Ctrl Pts',(-0.117971276761593,-5.28420699491729E-6,
1.49243671147361));
#15964=CARTESIAN_POINT('Ctrl Pts',(-0.117971582784674,-0.000385634193345565,
1.49246252744444));
#15965=CARTESIAN_POINT('Ctrl Pts',(-0.117794795258817,-0.0397700451254522,
1.49513573278954));
#15966=CARTESIAN_POINT('Ctrl Pts',(-0.0742871760264013,-0.117748889605885,
1.50045632750888));
#15967=CARTESIAN_POINT('Ctrl Pts',(0.0586284551779338,-0.126233948370975,
1.50839849563167));
#15968=CARTESIAN_POINT('Ctrl Pts',(0.137995068118234,-0.019163470063063,
1.51634066375444));
#15969=CARTESIAN_POINT('Ctrl Pts',(0.0906261803825392,0.105639137646141,
1.52428283187723));
#15970=CARTESIAN_POINT('Ctrl Pts',(0.00417072711528833,0.124051375507138,
1.52957761062575));
#15971=CARTESIAN_POINT('Ctrl Pts',(-0.0334019664627544,0.1129391839063,
1.53222500000001));
#15972=CARTESIAN_POINT('Origin',(0.,0.,-0.0924367114736175));
#15973=CARTESIAN_POINT('',(-0.117590702341447,3.3953472435133E-5,1.43256328852638));
#15974=CARTESIAN_POINT('',(-0.117692994131604,-9.95982882293356E-5,1.44243671147361));
#15975=CARTESIAN_POINT('',(-0.117775,2.85464118895969E-14,-0.0924367114736175));
#15976=CARTESIAN_POINT('Ctrl Pts',(-0.117590702341447,3.39534724351446E-5,
1.43256328852638));
#15977=CARTESIAN_POINT('Ctrl Pts',(-0.117534527156218,-0.0217216553118358,
1.43402790046837));
#15978=CARTESIAN_POINT('Ctrl Pts',(-0.101314495966545,-0.0828641818343832,
1.43813884228945));
#15979=CARTESIAN_POINT('Ctrl Pts',(-0.00292444232197888,-0.139176693688359,
1.44489611398964));
#15980=CARTESIAN_POINT('Ctrl Pts',(0.115350068603298,-0.0779297424218237,
1.45283510362695));
#15981=CARTESIAN_POINT('Ctrl Pts',(0.128028003046829,0.0546551750765237,
1.46077409326425));
#15982=CARTESIAN_POINT('Ctrl Pts',(0.0235079116789307,0.137209630484779,
1.46871308290156));
#15983=CARTESIAN_POINT('Ctrl Pts',(-0.0918059616614023,0.0978189523496558,
1.47597614798894));
#15984=CARTESIAN_POINT('Ctrl Pts',(-0.117485047349053,0.0290640819657798,
1.48059288319721));
#15985=CARTESIAN_POINT('Ctrl Pts',(-0.117746618301147,-0.000105742458702949,
1.48256328852638));
#15986=CARTESIAN_POINT('Ctrl Pts',(-0.117692994131604,-9.9598288229346E-5,
1.44243671147361));
#15987=CARTESIAN_POINT('Ctrl Pts',(-0.117789077779518,-0.0120777797952868,
1.44324485786555));
#15988=CARTESIAN_POINT('Ctrl Pts',(-0.110597905189529,-0.0631824179582176,
1.44670039363175));
#15989=CARTESIAN_POINT('Ctrl Pts',(-0.0368790902657646,-0.134252921254984,
1.45280331877221));
#15990=CARTESIAN_POINT('Ctrl Pts',(0.0928396680879532,-0.103751556080299,
1.46074548689499));
#15991=CARTESIAN_POINT('Ctrl Pts',(0.137511141307062,0.0217950526079239,
1.46868765501776));
#15992=CARTESIAN_POINT('Ctrl Pts',(0.0562018483347667,0.127378648737854,
1.47662982314055));
#15993=CARTESIAN_POINT('Ctrl Pts',(-0.0761502833827582,0.1162998103107,
1.48454617529249));
#15994=CARTESIAN_POINT('Ctrl Pts',(-0.117940200573233,0.0386186906477724,
1.48981513807018));
#15995=CARTESIAN_POINT('Ctrl Pts',(-0.117971276761593,-5.28420699491729E-6,
1.49243671147361));
#15996=CARTESIAN_POINT('Origin',(0.,0.,-0.0924367114736175));
#15997=CARTESIAN_POINT('',(-0.117872752581409,8.97255421561373E-5,1.38256328852638));
#15998=CARTESIAN_POINT('',(-0.117613151267609,6.14076272390171E-5,1.39243671147361));
#15999=CARTESIAN_POINT('',(-0.117775,2.85464118895969E-14,-0.0924367114736175));
#16000=CARTESIAN_POINT('Ctrl Pts',(-0.117872752581409,8.97255421561322E-5,
1.38256328852638));
#16001=CARTESIAN_POINT('Ctrl Pts',(-0.117591624875346,-0.0331778698171688,
1.38481658786042));
#16002=CARTESIAN_POINT('Ctrl Pts',(-0.0854981695600773,-0.105990339321694,
1.38971621707357));
#16003=CARTESIAN_POINT('Ctrl Pts',(0.0379781508110965,-0.133926497290667,
1.39726217616581));
#16004=CARTESIAN_POINT('Ctrl Pts',(0.133119345865688,-0.0407171622080862,
1.40520116580311));
#16005=CARTESIAN_POINT('Ctrl Pts',(0.106398871137127,0.0897659150453452,
1.41314015544042));
#16006=CARTESIAN_POINT('Ctrl Pts',(-0.0177224175491345,0.138074504763813,
1.42107914507772));
#16007=CARTESIAN_POINT('Ctrl Pts',(-0.105714817800915,0.0743914165933911,
1.42755352277305));
#16008=CARTESIAN_POINT('Ctrl Pts',(-0.11763602712824,0.0175874039095825,
1.43138157058926));
#16009=CARTESIAN_POINT('Ctrl Pts',(-0.117590702341447,3.39534724351446E-5,
1.43256328852638));
#16010=CARTESIAN_POINT('Ctrl Pts',(-0.117613151267609,6.1407627239024E-5,
1.39243671147361));
#16011=CARTESIAN_POINT('Ctrl Pts',(-0.117501644803633,-0.0235525549213426,
1.39402718828666));
#16012=CARTESIAN_POINT('Ctrl Pts',(-0.0991469449676741,-0.0866320980727062,
1.39826505447396));
#16013=CARTESIAN_POINT('Ctrl Pts',(0.00373660876362508,-0.139175849115243,
1.40515031003553));
#16014=CARTESIAN_POINT('Ctrl Pts',(0.118990018389619,-0.0722858665142316,
1.41309247815831));
#16015=CARTESIAN_POINT('Ctrl Pts',(0.125236419206141,0.0608253567263532,
1.42103464628109));
#16016=CARTESIAN_POINT('Ctrl Pts',(0.0167532566496359,0.13821437898841,
1.42897681440387));
#16017=CARTESIAN_POINT('Ctrl Pts',(-0.0944771051913143,0.0939940009069027,
1.43611083613471));
#16018=CARTESIAN_POINT('Ctrl Pts',(-0.117474319425011,0.0271612872365273,
1.44059746849129));
#16019=CARTESIAN_POINT('Ctrl Pts',(-0.117692994131604,-9.9598288229346E-5,
1.44243671147361));
#16020=CARTESIAN_POINT('Origin',(0.,0.,-0.0924367114736175));
#16021=CARTESIAN_POINT('',(-0.117871679003533,-9.01049542302267E-5,1.33256328852638));
#16022=CARTESIAN_POINT('',(-0.117917347702326,6.89762296073142E-5,1.34243671147361));
#16023=CARTESIAN_POINT('',(-0.117775,2.85464118895969E-14,-0.0924367114736175));
#16024=CARTESIAN_POINT('Ctrl Pts',(-0.117871679003533,-9.01049542302501E-5,
1.33256328852638));
#16025=CARTESIAN_POINT('Ctrl Pts',(-0.117921183610054,-0.00593170075121234,
1.33295894537338));
#16026=CARTESIAN_POINT('Ctrl Pts',(-0.114870949065289,-0.0507926200311143,
1.33600093209947));
#16027=CARTESIAN_POINT('Ctrl Pts',(-0.0572704544775333,-0.126880813469472,
1.34168924870467));
#16028=CARTESIAN_POINT('Ctrl Pts',(0.0755477687720905,-0.116923823242002,
1.34962823834197));
#16029=CARTESIAN_POINT('Ctrl Pts',(0.13920718769651,6.89141801743488E-5,
1.35756722797928));
#16030=CARTESIAN_POINT('Ctrl Pts',(0.0754319660950179,0.116998564767658,
1.36550621761658));
#16031=CARTESIAN_POINT('Ctrl Pts',(-0.0573960494825499,0.126824048933643,
1.37344520725389));
#16032=CARTESIAN_POINT('Ctrl Pts',(-0.11489462347839,0.0507140179075799,
1.37913089755716));
#16033=CARTESIAN_POINT('Ctrl Pts',(-0.117921788132912,0.00589240827474643,
1.38217025798132));
#16034=CARTESIAN_POINT('Ctrl Pts',(-0.117872752581409,8.97255421561322E-5,
1.38256328852638));
#16035=CARTESIAN_POINT('Ctrl Pts',(-0.117917347702326,6.89762296073276E-5,
1.34243671147361));
#16036=CARTESIAN_POINT('Ctrl Pts',(-0.117673982084908,-0.0349283870656527,
1.34480951870776));
#16037=CARTESIAN_POINT('Ctrl Pts',(-0.0826049238592893,-0.109396528181867,
1.34982971531618));
#16038=CARTESIAN_POINT('Ctrl Pts',(0.0440301174146577,-0.132080378229483,
1.35749730129884));
#16039=CARTESIAN_POINT('Ctrl Pts',(0.13486394497766,-0.0345773583278084,
1.36543946942163));
#16040=CARTESIAN_POINT('Ctrl Pts',(0.102148545386143,0.0946020732301706,
1.3733816375444));
#16041=CARTESIAN_POINT('Ctrl Pts',(-0.0241454188302812,0.137116288461919,
1.38132380566719));
#16042=CARTESIAN_POINT('Ctrl Pts',(-0.107458038693719,0.07065895059964,
1.38767549697692));
#16043=CARTESIAN_POINT('Ctrl Pts',(-0.117687250167678,0.015753490298928,
1.3913797989124));
#16044=CARTESIAN_POINT('Ctrl Pts',(-0.117613151267609,6.1407627239024E-5,
1.39243671147361));
#16045=CARTESIAN_POINT('Origin',(0.,0.,-0.0924367114736175));
#16046=CARTESIAN_POINT('',(-0.117590388001671,-3.33269891443968E-5,1.28256328852638));
#16047=CARTESIAN_POINT('',(-0.117823716245033,-0.000102811805890834,1.29243671147362));
#16048=CARTESIAN_POINT('',(-0.117775,2.85464118895969E-14,-0.0924367114736175));
#16049=CARTESIAN_POINT('Ctrl Pts',(-0.117590388001671,-3.33269891444124E-5,
1.28256328852638));
#16050=CARTESIAN_POINT('Ctrl Pts',(-0.117634977734708,-0.017625925033684,
1.28374763276543));
#16051=CARTESIAN_POINT('Ctrl Pts',(-0.105676786131388,-0.0744702911817869,
1.28757830688358));
#16052=CARTESIAN_POINT('Ctrl Pts',(-0.0175857351491984,-0.138091953858251,
1.29405531088083));
#16053=CARTESIAN_POINT('Ctrl Pts',(0.106487712804436,-0.089660542174548,
1.30199430051814));
#16054=CARTESIAN_POINT('Ctrl Pts',(0.133078957772855,0.0408489510387311,
1.30993329015544));
#16055=CARTESIAN_POINT('Ctrl Pts',(0.0378455373822902,0.133964029124136,
1.31787227979275));
#16056=CARTESIAN_POINT('Ctrl Pts',(-0.0855601048685178,0.105915403748908,
1.32541561258306));
#16057=CARTESIAN_POINT('Ctrl Pts',(-0.117590074669608,0.0331395035428114,
1.33031261549427));
#16058=CARTESIAN_POINT('Ctrl Pts',(-0.117871679003533,-9.01049542302501E-5,
1.33256328852638));
#16059=CARTESIAN_POINT('Ctrl Pts',(-0.117823716245033,-0.000102811805890825,
1.29243671147362));
#16060=CARTESIAN_POINT('Ctrl Pts',(-0.117892441435953,-0.00760726064997237,
1.29294445975461));
#16061=CARTESIAN_POINT('Ctrl Pts',(-0.113819337750002,-0.0541654333254181,
1.29609959740987));
#16062=CARTESIAN_POINT('Ctrl Pts',(-0.0518146499729274,-0.129225073214149,
1.30190212443939));
#16063=CARTESIAN_POINT('Ctrl Pts',(0.0805213734929343,-0.11357898534207,
1.30984429256217));
#16064=CARTESIAN_POINT('Ctrl Pts',(0.1390915465469,0.0061171215252809,1.31778646068495));
#16065=CARTESIAN_POINT('Ctrl Pts',(0.0702395735793815,0.120209316621791,
1.32572862880773));
#16066=CARTESIAN_POINT('Ctrl Pts',(-0.0629590648350173,0.124177428154433,
1.33367079693051));
#16067=CARTESIAN_POINT('Ctrl Pts',(-0.115917830154768,0.0471875384414626,
1.33924015781913));
#16068=CARTESIAN_POINT('Ctrl Pts',(-0.117945510062545,0.00411888419242175,
1.3421621293335));
#16069=CARTESIAN_POINT('Ctrl Pts',(-0.117917347702326,6.89762296073276E-5,
1.34243671147361));
#16070=CARTESIAN_POINT('Origin',(0.,0.,-0.0924367114736175));
#16071=CARTESIAN_POINT('',(-0.11774949833287,0.000107383800510985,1.23256328852638));
#16072=CARTESIAN_POINT('',(-0.117581795058195,-8.20683476789735E-6,1.24243671147361));
#16073=CARTESIAN_POINT('',(-0.117775,2.85464118895969E-14,-0.0924367114736175));
#16074=CARTESIAN_POINT('Ctrl Pts',(-0.11774949833287,0.000107383800510997,
1.23256328852638));
#16075=CARTESIAN_POINT('Ctrl Pts',(-0.1174869159147,-0.0291008736543001,
1.23453632015749));
#16076=CARTESIAN_POINT('Ctrl Pts',(-0.0917482398636095,-0.0978979247776974,
1.23915568166769));
#16077=CARTESIAN_POINT('Ctrl Pts',(0.0236422145726536,-0.137184880695923,
1.246421373057));
#16078=CARTESIAN_POINT('Ctrl Pts',(0.128082862902196,-0.0545291301253663,
1.2543603626943));
#16079=CARTESIAN_POINT('Ctrl Pts',(0.115272428336817,0.0780443019497631,
1.26229935233161));
#16080=CARTESIAN_POINT('Ctrl Pts',(-0.00306201423577413,0.139173524314926,
1.27023834196891));
#16081=CARTESIAN_POINT('Ctrl Pts',(-0.101358337705897,0.08278581645186,
1.27699298736717));
#16082=CARTESIAN_POINT('Ctrl Pts',(-0.117535345263889,0.02168343817453,
1.28110130288633));
#16083=CARTESIAN_POINT('Ctrl Pts',(-0.117590388001671,-3.33269891444124E-5,
1.28256328852638));
#16084=CARTESIAN_POINT('Ctrl Pts',(-0.117581795058195,-8.20683476789562E-6,
1.24243671147361));
#16085=CARTESIAN_POINT('Ctrl Pts',(-0.117593699448189,-0.0191748937105988,
1.24372679017572));
#16086=CARTESIAN_POINT('Ctrl Pts',(-0.104100832827715,-0.0776580224685839,
1.24766425825208));
#16087=CARTESIAN_POINT('Ctrl Pts',(-0.0120149744006178,-0.138706589206355,
1.25424911570271));
#16088=CARTESIAN_POINT('Ctrl Pts',(0.110059129405696,-0.0852693704304675,
1.26219128382548));
#16089=CARTESIAN_POINT('Ctrl Pts',(0.13130776387206,0.0462833517151888,
1.27013345194827));
#16090=CARTESIAN_POINT('Ctrl Pts',(0.0322649968732001,0.135435768819968,
1.27807562007105));
#16091=CARTESIAN_POINT('Ctrl Pts',(-0.0881142830049797,0.102747609761224,
1.28551003991283));
#16092=CARTESIAN_POINT('Ctrl Pts',(-0.117534109666069,0.0315207854174475,
1.29029707038035));
#16093=CARTESIAN_POINT('Ctrl Pts',(-0.117823716245033,-0.000102811805890825,
1.29243671147362));
#16094=CARTESIAN_POINT('Origin',(0.,0.,-0.0924367114736175));
#16095=CARTESIAN_POINT('',(-0.117957988745754,-3.12301727557783E-5,1.18256328852638));
#16096=CARTESIAN_POINT('',(-0.117793553451004,0.000106755881474893,1.19243671147362));
#16097=CARTESIAN_POINT('',(-0.117775,2.85464118895969E-14,-0.0924367114736175));
#16098=CARTESIAN_POINT('Ctrl Pts',(-0.117957988745754,-3.12301727557569E-5,
1.18256328852638));
#16099=CARTESIAN_POINT('Ctrl Pts',(-0.117964007145535,-0.00173159226684161,
1.18267867767044));
#16100=CARTESIAN_POINT('Ctrl Pts',(-0.117160216762375,-0.0424221720604921,
1.1854403966936));
#16101=CARTESIAN_POINT('Ctrl Pts',(-0.0703321751825429,-0.12013338809653,
1.19084844559586));
#16102=CARTESIAN_POINT('Ctrl Pts',(0.0627954496153871,-0.124239193932754,
1.19878743523316));
#16103=CARTESIAN_POINT('Ctrl Pts',(0.138438143943654,-0.0146125323915816,
1.20672642487047));
#16104=CARTESIAN_POINT('Ctrl Pts',(0.0873502052771435,0.108390901091839,
1.21466541450777));
#16105=CARTESIAN_POINT('Ctrl Pts',(-0.043700859820065,0.132169893139269,
1.22260440414508));
#16106=CARTESIAN_POINT('Ctrl Pts',(-0.112119660921406,0.0591163174148552,
1.22857036215128));
#16107=CARTESIAN_POINT('Ctrl Pts',(-0.117839104743291,0.0100747194789664,
1.23188999027838));
#16108=CARTESIAN_POINT('Ctrl Pts',(-0.11774949833287,0.000107383800510997,
1.23256328852638));
#16109=CARTESIAN_POINT('Ctrl Pts',(-0.117793553451004,0.000106755881474891,
1.19243671147362));
#16110=CARTESIAN_POINT('Ctrl Pts',(-0.117510050331475,-0.0305433296418112,
1.19450912059683));
#16111=CARTESIAN_POINT('Ctrl Pts',(-0.0896091397727994,-0.100804620014092,
1.19922891909429));
#16112=CARTESIAN_POINT('Ctrl Pts',(0.0288222657999454,-0.136209964735594,
1.20659610696603));
#16113=CARTESIAN_POINT('Ctrl Pts',(0.130092623711363,-0.0495962373069701,
1.21453827508881));
#16114=CARTESIAN_POINT('Ctrl Pts',(0.112184773380136,0.082452738709893,
1.22248044321158));
#16115=CARTESIAN_POINT('Ctrl Pts',(-0.00849585454694533,0.138966535376798,
1.23042261133437));
#16116=CARTESIAN_POINT('Ctrl Pts',(-0.103054997843392,0.079672038485689,
1.23707470075504));
#16117=CARTESIAN_POINT('Ctrl Pts',(-0.11756927027536,0.0201573447738481,
1.24107940080146));
#16118=CARTESIAN_POINT('Ctrl Pts',(-0.117581795058195,-8.20683476789562E-6,
1.24243671147361));
#16119=CARTESIAN_POINT('Origin',(0.,0.,-0.0924367114736175));
#16120=CARTESIAN_POINT('',(-0.117657565919426,-8.78585414499747E-5,1.13256328852638));
#16121=CARTESIAN_POINT('',(-0.117937823388479,-5.4172489969917E-5,1.14243671147362));
#16122=CARTESIAN_POINT('',(-0.117775,2.85464118895969E-14,-0.0924367114736175));
#16123=CARTESIAN_POINT('Ctrl Pts',(-0.117657565919426,-8.78585414499974E-5,
1.13256328852638));
#16124=CARTESIAN_POINT('Ctrl Pts',(-0.11775046973706,-0.0134980674796043,
1.13346736506249));
#16125=CARTESIAN_POINT('Ctrl Pts',(-0.109441032251172,-0.0660497484721492,
1.13701777147771));
#16126=CARTESIAN_POINT('Ctrl Pts',(-0.0320511128216771,-0.13546723577438,
1.14321450777202));
#16127=CARTESIAN_POINT('Ctrl Pts',(0.0964380908528195,-0.100390938007982,
1.15115349740933));
#16128=CARTESIAN_POINT('Ctrl Pts',(0.136644831685568,0.0265863832644056,
1.15909248704664));
#16129=CARTESIAN_POINT('Ctrl Pts',(0.0517625939920979,0.129225692742072,
1.16703147668394));
#16130=CARTESIAN_POINT('Ctrl Pts',(-0.0785823129332351,0.113795317289389,
1.17485507717719));
#16131=CARTESIAN_POINT('Ctrl Pts',(-0.117825981412732,0.0372644419932696,
1.18003234779134));
#16132=CARTESIAN_POINT('Ctrl Pts',(-0.117957988745754,-3.12301727557569E-5,
1.18256328852638));
#16133=CARTESIAN_POINT('Ctrl Pts',(-0.117937823388479,-5.41724899699178E-5,
1.14243671147362));
#16134=CARTESIAN_POINT('Ctrl Pts',(-0.117955293269658,-0.0031110520517566,
1.14264406164367));
#16135=CARTESIAN_POINT('Ctrl Pts',(-0.116460933142332,-0.0451799670343263,
1.14549880118799));
#16136=CARTESIAN_POINT('Ctrl Pts',(-0.0660858892268601,-0.122541963197144,
1.15100093010657));
#16137=CARTESIAN_POINT('Ctrl Pts',(0.0671705316110708,-0.121950798202395,
1.15894309822935));
#16138=CARTESIAN_POINT('Ctrl Pts',(0.138891844802359,-0.00964017357273747,
1.16688526635212));
#16139=CARTESIAN_POINT('Ctrl Pts',(0.0833739592533277,0.111501840422208,
1.17482743447491));
#16140=CARTESIAN_POINT('Ctrl Pts',(-0.0485230383040216,0.130496713571114,
1.18276960259768));
#16141=CARTESIAN_POINT('Ctrl Pts',(-0.113150295826959,0.0561813708375219,
1.18863936159726));
#16142=CARTESIAN_POINT('Ctrl Pts',(-0.117872210070015,0.00861047923971886,
1.19186173122257));
#16143=CARTESIAN_POINT('Ctrl Pts',(-0.117793553451004,0.000106755881474891,
1.19243671147362));
#16144=CARTESIAN_POINT('Origin',(0.,0.,-0.0924367114736175));
#16145=CARTESIAN_POINT('',(-0.117641451221435,8.0229283111194E-5,1.08256328852638));
#16146=CARTESIAN_POINT('',(-0.117630591849015,-7.42484764288953E-5,1.09243671147362));
#16147=CARTESIAN_POINT('',(-0.117775,2.85464118895969E-14,-0.0924367114736175));
#16148=CARTESIAN_POINT('Ctrl Pts',(-0.117641451221435,8.02292831111745E-5,
1.08256328852638));
#16149=CARTESIAN_POINT('Ctrl Pts',(-0.117483998834985,-0.0250372639622414,
1.08425605245455));
#16150=CARTESIAN_POINT('Ctrl Pts',(-0.0972946570053161,-0.0896524615425008,
1.08859514626182));
#16151=CARTESIAN_POINT('Ctrl Pts',(0.00904258428980543,-0.13891320121148,
1.09558056994819));
#16152=CARTESIAN_POINT('Ctrl Pts',(0.121617839487272,-0.067732908692211,
1.1035195595855));
#16153=CARTESIAN_POINT('Ctrl Pts',(0.122860297649024,0.0654522196953821,
1.1114585492228));
#16154=CARTESIAN_POINT('Ctrl Pts',(0.0116325734791967,0.138720326685422,
1.11939753886011));
#16155=CARTESIAN_POINT('Ctrl Pts',(-0.096364912740844,0.0911171059582243,
1.1264324519613));
#16156=CARTESIAN_POINT('Ctrl Pts',(-0.117478530206868,0.0257550656131636,
1.13082103518339));
#16157=CARTESIAN_POINT('Ctrl Pts',(-0.117657565919426,-8.78585414499974E-5,
1.13256328852638));
#16158=CARTESIAN_POINT('Ctrl Pts',(-0.117630591849015,-7.42484764288814E-5,
1.09243671147362));
#16159=CARTESIAN_POINT('Ctrl Pts',(-0.117715241483118,-0.0147626739157663,
1.09342639206478));
#16160=CARTESIAN_POINT('Ctrl Pts',(-0.108350501834675,-0.0686384992808382,
1.0970634620302));
#16161=CARTESIAN_POINT('Ctrl Pts',(-0.0276126195379174,-0.136460326620484,
1.10334792136989));
#16162=CARTESIAN_POINT('Ctrl Pts',(0.0997182217817603,-0.0971604536002107,
1.11129008949267));
#16163=CARTESIAN_POINT('Ctrl Pts',(0.135696927507188,0.0311483765905046,
1.11923225761545));
#16164=CARTESIAN_POINT('Ctrl Pts',(0.0473633069609982,0.130922093830007,
1.12717442573822));
#16165=CARTESIAN_POINT('Ctrl Pts',(-0.0809210029008042,0.111284164335459,
1.13490924369095));
#16166=CARTESIAN_POINT('Ctrl Pts',(-0.117732242679493,0.0359183370635313,
1.13999667226941));
#16167=CARTESIAN_POINT('Ctrl Pts',(-0.117937823388479,-5.41724899699178E-5,
1.14243671147362));
#16168=CARTESIAN_POINT('Origin',(0.,0.,-0.0924367114736175));
#16169=CARTESIAN_POINT('',(-0.117948158721073,4.38502512853227E-5,1.03256328852638));
#16170=CARTESIAN_POINT('',(-0.117667547954054,9.20194976846214E-5,1.04243671147362));
#16171=CARTESIAN_POINT('',(-0.117775,2.85464118895969E-14,-0.0924367114736175));
#16172=CARTESIAN_POINT('Ctrl Pts',(-0.117948158721073,4.38502512853157E-5,
1.03256328852638));
#16173=CARTESIAN_POINT('Ctrl Pts',(-0.117773439871091,-0.0365306738650768,
1.03504473984661));
#16174=CARTESIAN_POINT('Ctrl Pts',(-0.0798690478914953,-0.112422454385097,
1.04017252104593));
#16175=CARTESIAN_POINT('Ctrl Pts',(0.0493427524230464,-0.130168884856471,
1.04794663212436));
#16176=CARTESIAN_POINT('Ctrl Pts',(0.136125055048066,-0.0291310004912345,
1.05588562176166));
#16177=CARTESIAN_POINT('Ctrl Pts',(0.0982941990358779,0.0985743183458784,
1.06382461139897));
#16178=CARTESIAN_POINT('Ctrl Pts',(-0.0295182596522469,0.136041604476578,
1.07176360103627));
#16179=CARTESIAN_POINT('Ctrl Pts',(-0.108818061611988,0.067537217334308,
1.07800982674541));
#16180=CARTESIAN_POINT('Ctrl Pts',(-0.11773014713001,0.0142293884972668,
1.08160972257545));
#16181=CARTESIAN_POINT('Ctrl Pts',(-0.117641451221435,8.02292831111745E-5,
1.08256328852638));
#16182=CARTESIAN_POINT('Ctrl Pts',(-0.117667547954054,9.20194976846197E-5,
1.04243671147362));
#16183=CARTESIAN_POINT('Ctrl Pts',(-0.117475882803567,-0.0261866690710452,
1.04420872248589));
#16184=CARTESIAN_POINT('Ctrl Pts',(-0.0957916308421219,-0.0920126959480487,
1.04862812287242));
#16185=CARTESIAN_POINT('Ctrl Pts',(0.0132451643780021,-0.13859452774087,
1.05569491263321));
#16186=CARTESIAN_POINT('Ctrl Pts',(0.123654649330263,-0.0639797248987874,
1.06363708075599));
#16187=CARTESIAN_POINT('Ctrl Pts',(0.120783771971213,0.0692470788374567,
1.07157924887876));
#16188=CARTESIAN_POINT('Ctrl Pts',(0.00726255089817806,0.139036444335888,
1.07952141700155));
#16189=CARTESIAN_POINT('Ctrl Pts',(-0.0979368667310299,0.0886295245336828,
1.08647390453316));
#16190=CARTESIAN_POINT('Ctrl Pts',(-0.117488804242801,0.0245287720112504,
1.09077900269052));
#16191=CARTESIAN_POINT('Ctrl Pts',(-0.117630591849015,-7.42484764288814E-5,
1.09243671147362));
#16192=CARTESIAN_POINT('Origin',(0.,0.,-0.0924367114736175));
#16193=CARTESIAN_POINT('',(-0.117771476475648,-0.000107683352847938,0.982563288526384));
#16194=CARTESIAN_POINT('',(-0.11796176292438,2.53781033017321E-5,0.992436711473616));
#16195=CARTESIAN_POINT('',(-0.117775,2.85464118895969E-14,-0.0924367114736175));
#16196=CARTESIAN_POINT('Ctrl Pts',(-0.117771476475648,-0.000107683352847945,
0.982563288526384));
#16197=CARTESIAN_POINT('Ctrl Pts',(-0.117856103358663,-0.00933799346614349,
0.983187097359559));
#16198=CARTESIAN_POINT('Ctrl Pts',(-0.112646870919438,-0.057630810124202,
0.986457236071836));
#16199=CARTESIAN_POINT('Ctrl Pts',(-0.0461590140787468,-0.131331607851033,
0.992373704663214));
#16200=CARTESIAN_POINT('Ctrl Pts',(0.0853128637208732,-0.110001641284132,
1.00031269430052));
#16201=CARTESIAN_POINT('Ctrl Pts',(0.138686661656432,0.0120272889735618,
1.00825168393783));
#16202=CARTESIAN_POINT('Ctrl Pts',(0.0651023256631918,0.123046060459907,
1.01619067357513));
#16203=CARTESIAN_POINT('Ctrl Pts',(-0.0680787277209358,0.121424596492465,
1.02412966321244));
#16204=CARTESIAN_POINT('Ctrl Pts',(-0.116790117880403,0.0438975063746073,
1.02958720152952));
#16205=CARTESIAN_POINT('Ctrl Pts',(-0.11795976781127,0.00247402277930658,
1.0323984099675));
#16206=CARTESIAN_POINT('Ctrl Pts',(-0.117948158721073,4.38502512853157E-5,
1.03256328852638));
#16207=CARTESIAN_POINT('Ctrl Pts',(-0.11796176292438,2.53781033017319E-5,
0.992436711473616));
#16208=CARTESIAN_POINT('Ctrl Pts',(-0.117851518882229,-0.0376119105440478,
0.994991052906992));
#16209=CARTESIAN_POINT('Ctrl Pts',(-0.077958511321084,-0.114458475672252,
1.00019278371463));
#16210=CARTESIAN_POINT('Ctrl Pts',(0.0529591494285269,-0.128760265574912,
1.00804190389653));
#16211=CARTESIAN_POINT('Ctrl Pts',(0.136912761112491,-0.0252739657289669,
1.0159840720193));
#16212=CARTESIAN_POINT('Ctrl Pts',(0.0954402180350474,0.101365883217864,
1.02392624014209));
#16213=CARTESIAN_POINT('Ctrl Pts',(-0.0334653697086341,0.135144169424284,
1.03186840826486));
#16214=CARTESIAN_POINT('Ctrl Pts',(-0.109792739119276,0.0652029671457737,
1.03803856537538));
#16215=CARTESIAN_POINT('Ctrl Pts',(-0.117762231070763,0.0130737646421874,
1.04156133311163));
#16216=CARTESIAN_POINT('Ctrl Pts',(-0.117667547954054,9.20194976846197E-5,
1.04243671147362));
#16217=CARTESIAN_POINT('Origin',(0.,0.,-0.0924367114736175));
#16218=CARTESIAN_POINT('',(-0.117585265278523,2.16484251076657E-5,0.932563288526384));
#16219=CARTESIAN_POINT('',(-0.117742563953077,-0.000107211314308964,0.942436711473616));
#16220=CARTESIAN_POINT('',(-0.117775,2.85464118895969E-14,-0.0924367114736175));
#16221=CARTESIAN_POINT('Ctrl Pts',(-0.117585265278523,2.16484251076635E-5,
0.932563288526384));
#16222=CARTESIAN_POINT('Ctrl Pts',(-0.117550805757046,-0.0209622679161363,
0.933975784751614));
#16223=CARTESIAN_POINT('Ctrl Pts',(-0.102172791552808,-0.0813069697478888,
0.938034610855947));
#16224=CARTESIAN_POINT('Ctrl Pts',(-0.00565790085648466,-0.139092177922979,
0.944739766839381));
#16225=CARTESIAN_POINT('Ctrl Pts',(0.113796373024222,-0.0801812402497705,
0.952678756476687));
#16226=CARTESIAN_POINT('Ctrl Pts',(0.129077866376032,0.0521301276928276,
0.960617746113992));
#16227=CARTESIAN_POINT('Ctrl Pts',(0.026197419344502,0.13671993644362,0.968556735751298));
#16228=CARTESIAN_POINT('Ctrl Pts',(-0.0906967139502387,0.0993396518733501,
0.975871916555428));
#16229=CARTESIAN_POINT('Ctrl Pts',(-0.117497098103867,0.02981894716558,
0.980540767480457));
#16230=CARTESIAN_POINT('Ctrl Pts',(-0.117771476475648,-0.000107683352847945,
0.982563288526384));
#16231=CARTESIAN_POINT('Ctrl Pts',(-0.117742563953077,-0.000107211314308957,
0.942436711473616));
#16232=CARTESIAN_POINT('Ctrl Pts',(-0.117833632602859,-0.0103126986533654,
0.943125993953839));
#16233=CARTESIAN_POINT('Ctrl Pts',(-0.111944766202914,-0.0596118697348184,
0.946462665808322));
#16234=CARTESIAN_POINT('Ctrl Pts',(-0.0428565117498991,-0.132465832952297,
0.952446727037066));
#16235=CARTESIAN_POINT('Ctrl Pts',(0.0880997963686447,-0.107806787258123,
0.960388895159846));
#16236=CARTESIAN_POINT('Ctrl Pts',(0.138347640177547,0.0156143509765511,
0.968331063282625));
#16237=CARTESIAN_POINT('Ctrl Pts',(0.061854832590724,0.124731139593481,
0.976273231405407));
#16238=CARTESIAN_POINT('Ctrl Pts',(-0.0713033562375951,0.119581390225944,
0.984215399528185));
#16239=CARTESIAN_POINT('Ctrl Pts',(-0.117322772537986,0.0417718924351975,
0.989603226217589));
#16240=CARTESIAN_POINT('Ctrl Pts',(-0.11796577882491,0.00139640554830399,
0.992343663532733));
#16241=CARTESIAN_POINT('Ctrl Pts',(-0.11796176292438,2.53781033017319E-5,
0.992436711473616));
#16242=CARTESIAN_POINT('Origin',(0.,0.,-0.0924367114736175));
#16243=CARTESIAN_POINT('',(-0.117850913371472,9.6525574830472E-5,0.882563288526384));
#16244=CARTESIAN_POINT('',(-0.117591231449503,3.54948526558943E-5,0.892436711473616));
#16245=CARTESIAN_POINT('',(-0.117775,2.85464118895969E-14,-0.0924367114736175));
#16246=CARTESIAN_POINT('Ctrl Pts',(-0.117850913371472,9.65255748304767E-5,
0.882563288526384));
#16247=CARTESIAN_POINT('Ctrl Pts',(-0.117563006813672,-0.0324172738354332,
0.884764472143669));
#16248=CARTESIAN_POINT('Ctrl Pts',(-0.0867151192651892,-0.104499852648429,
0.889611985640057));
#16249=CARTESIAN_POINT('Ctrl Pts',(0.0353397195745277,-0.134646760160997,
0.897105829015547));
#16250=CARTESIAN_POINT('Ctrl Pts',(0.132293719443212,-0.0433245611326863,
0.905044818652852));
#16251=CARTESIAN_POINT('Ctrl Pts',(0.108141885842356,0.0876583043865096,
0.912983808290157));
#16252=CARTESIAN_POINT('Ctrl Pts',(-0.0150064327997127,0.138395999855801,
0.920922797927463));
#16253=CARTESIAN_POINT('Ctrl Pts',(-0.104951114476159,0.0759553573435841,
0.927449291339539));
#16254=CARTESIAN_POINT('Ctrl Pts',(-0.117615366114572,0.01835136974357,
0.931329454872513));
#16255=CARTESIAN_POINT('Ctrl Pts',(-0.117585265278523,2.16484251076635E-5,
0.932563288526384));
#16256=CARTESIAN_POINT('Ctrl Pts',(-0.117591231449503,3.54948526559117E-5,
0.892436711473616));
#16257=CARTESIAN_POINT('Ctrl Pts',(-0.117532234588281,-0.0218238662162972,
0.893908324374946));
#16258=CARTESIAN_POINT('Ctrl Pts',(-0.101194437785642,-0.0830895288483654,
0.898027326650536));
#16259=CARTESIAN_POINT('Ctrl Pts',(-0.00250162451743248,-0.139203517821528,
0.904793718300386));
#16260=CARTESIAN_POINT('Ctrl Pts',(0.115632500949424,-0.0775435504945224,
0.912735886423165));
#16261=CARTESIAN_POINT('Ctrl Pts',(0.127835376168433,0.0551542754370876,
0.920678054545947));
#16262=CARTESIAN_POINT('Ctrl Pts',(0.0229279137899797,0.137325118854324,
0.928620222668725));
#16263=CARTESIAN_POINT('Ctrl Pts',(-0.0920562790907298,0.0974788594069619,
0.935873108311283));
#16264=CARTESIAN_POINT('Ctrl Pts',(-0.117483857027998,0.0288844367965532,
0.94047860457958));
#16265=CARTESIAN_POINT('Ctrl Pts',(-0.117742563953077,-0.000107211314308957,
0.942436711473616));
#16266=CARTESIAN_POINT('Origin',(0.,0.,-0.0924367114736175));
#16267=CARTESIAN_POINT('',(-0.11789232318732,-8.18790992476613E-5,0.832563288526384));
#16268=CARTESIAN_POINT('',(-0.117872825429845,8.99519344067963E-5,0.842436711473616));
#16269=CARTESIAN_POINT('',(-0.117775,2.85464118895969E-14,-0.0924367114736175));
#16270=CARTESIAN_POINT('Ctrl Pts',(-0.11789232318732,-8.18790992476734E-5,
0.832563288526384));
#16271=CARTESIAN_POINT('Ctrl Pts',(-0.117932494517479,-0.00515170743829337,
0.832906829656623));
#16272=CARTESIAN_POINT('Ctrl Pts',(-0.115332713682068,-0.0492334187378749,
0.835896700665964));
#16273=CARTESIAN_POINT('Ctrl Pts',(-0.059752088941783,-0.125731196083361,
0.841532901554406));
#16274=CARTESIAN_POINT('Ctrl Pts',(0.0732361146625898,-0.118385460722959,
0.849471891191712));
#16275=CARTESIAN_POINT('Ctrl Pts',(0.139181674492094,-0.00266594955618734,
0.857410880829018));
#16276=CARTESIAN_POINT('Ctrl Pts',(0.077715950067195,0.115494055719818,
0.865349870466323));
#16277=CARTESIAN_POINT('Ctrl Pts',(-0.0548934004223171,0.127927168308903,
0.87328886010363));
#16278=CARTESIAN_POINT('Ctrl Pts',(-0.114416768398411,0.0522742940766184,
0.879026666123649));
#16279=CARTESIAN_POINT('Ctrl Pts',(-0.117909136832228,0.0066718045071592,
0.882118142264567));
#16280=CARTESIAN_POINT('Ctrl Pts',(-0.117850913371472,9.65255748304767E-5,
0.882563288526384));
#16281=CARTESIAN_POINT('Ctrl Pts',(-0.117872825429845,8.99519344067998E-5,
0.842436711473616));
#16282=CARTESIAN_POINT('Ctrl Pts',(-0.117591169542271,-0.0331870933343037,
0.844690654796053));
#16283=CARTESIAN_POINT('Ctrl Pts',(-0.0854771005934613,-0.106025606004136,
0.84959198749275));
#16284=CARTESIAN_POINT('Ctrl Pts',(0.0380692928980519,-0.133920149482284,
0.857140709563706));
#16285=CARTESIAN_POINT('Ctrl Pts',(0.133179650076608,-0.0405839661022353,
0.865082877686486));
#16286=CARTESIAN_POINT('Ctrl Pts',(0.106283765719693,0.0899312995767124,
0.873025045809266));
#16287=CARTESIAN_POINT('Ctrl Pts',(-0.0179789669825735,0.138060255849953,
0.880967213932046));
#16288=CARTESIAN_POINT('Ctrl Pts',(-0.105798194743126,0.0742290978659706,
0.887437769153496));
#16289=CARTESIAN_POINT('Ctrl Pts',(-0.117638368248411,0.0175004969839459,
0.891260935000686));
#16290=CARTESIAN_POINT('Ctrl Pts',(-0.117591231449503,3.54948526559117E-5,
0.892436711473616));
#16291=CARTESIAN_POINT('Origin',(0.,0.,-0.0924367114736175));
#16292=CARTESIAN_POINT('',(-0.117598114366551,-4.51832715892789E-5,0.782563288526384));
#16293=CARTESIAN_POINT('',(-0.117874685330111,-8.92836445515327E-5,0.792436711473617));
#16294=CARTESIAN_POINT('',(-0.117775,2.85464118895969E-14,-0.0924367114736175));
#16295=CARTESIAN_POINT('Ctrl Pts',(-0.117598114366551,-4.518327158929E-5,
0.782563288526384));
#16296=CARTESIAN_POINT('Ctrl Pts',(-0.117656123976761,-0.0168608793038394,
0.783695517048678));
#16297=CARTESIAN_POINT('Ctrl Pts',(-0.106420815930739,-0.0729055463807818,
0.787474075450074));
#16298=CARTESIAN_POINT('Ctrl Pts',(-0.0202952816069424,-0.137719814645367,
0.793898963730571));
#16299=CARTESIAN_POINT('Ctrl Pts',(0.104705698854998,-0.0917352845351548,
0.801837953367879));
#16300=CARTESIAN_POINT('Ctrl Pts',(0.133855787965376,0.0382266115373486,
0.809776943005182));
#16301=CARTESIAN_POINT('Ctrl Pts',(0.0404700769297216,0.133194664588195,
0.81771593264249));
#16302=CARTESIAN_POINT('Ctrl Pts',(-0.0843190215395119,0.107398870964955,
0.825311381149555));
#16303=CARTESIAN_POINT('Ctrl Pts',(-0.117623050954756,0.0339016606582783,
0.830260499777521));
#16304=CARTESIAN_POINT('Ctrl Pts',(-0.11789232318732,-8.18790992476734E-5,
0.832563288526384));
#16305=CARTESIAN_POINT('Ctrl Pts',(-0.117874685330111,-8.9283644551537E-5,
0.792436711473617));
#16306=CARTESIAN_POINT('Ctrl Pts',(-0.11792303416021,-0.00583050672374999,
0.7928255958429));
#16307=CARTESIAN_POINT('Ctrl Pts',(-0.114931453360353,-0.0506053896743902,
0.795861869586443));
#16308=CARTESIAN_POINT('Ctrl Pts',(-0.0575513573065257,-0.126774282767806,
0.801545532704245));
#16309=CARTESIAN_POINT('Ctrl Pts',(0.0753527000357912,-0.117071978271622,
0.809487700827026));
#16310=CARTESIAN_POINT('Ctrl Pts',(0.139225942868322,-0.000119714417332432,
0.817429868949805));
#16311=CARTESIAN_POINT('Ctrl Pts',(0.0755539188089132,0.116942220141962,
0.825372037072586));
#16312=CARTESIAN_POINT('Ctrl Pts',(-0.0573332568284509,0.12687306712048,
0.833314205195366));
#16313=CARTESIAN_POINT('Ctrl Pts',(-0.114890414736801,0.0507419104293215,
0.839002429995709));
#16314=CARTESIAN_POINT('Ctrl Pts',(-0.117921990994851,0.00589875908008548,
0.842043265421793));
#16315=CARTESIAN_POINT('Ctrl Pts',(-0.117872825429845,8.99519344067998E-5,
0.842436711473616));
#16316=CARTESIAN_POINT('Origin',(0.,0.,-0.0924367114736175));
#16317=CARTESIAN_POINT('',(-0.11772691567491,0.000105512987197037,0.732563288526384));
#16318=CARTESIAN_POINT('',(-0.117591850253004,-3.65476421498312E-5,0.742436711473616));
#16319=CARTESIAN_POINT('',(-0.117775,2.85464118895969E-14,-0.0924367114736175));
#16320=CARTESIAN_POINT('Ctrl Pts',(-0.11772691567491,0.000105512987197042,
0.732563288526384));
#16321=CARTESIAN_POINT('Ctrl Pts',(-0.117479624464894,-0.0283451130369189,
0.734484204440733));
#16322=CARTESIAN_POINT('Ctrl Pts',(-0.0928318426870313,-0.096374559506161,
0.739051450234184));
#16323=CARTESIAN_POINT('Ctrl Pts',(0.0209425314183671,-0.137622876656644,
0.746265025906738));
#16324=CARTESIAN_POINT('Ctrl Pts',(0.126986869252672,-0.0570349089493802,
0.754204015544043));
#16325=CARTESIAN_POINT('Ctrl Pts',(0.11678343126468,0.0757646090434518,
0.762143005181349));
#16326=CARTESIAN_POINT('Ctrl Pts',(-0.000327234354877375,0.139206819944772,
0.770081994818654));
#16327=CARTESIAN_POINT('Ctrl Pts',(-0.100479183608201,0.0843410365921374,
0.776888755933667));
#16328=CARTESIAN_POINT('Ctrl Pts',(-0.117520539541507,0.0224420334666934,
0.781049187169576));
#16329=CARTESIAN_POINT('Ctrl Pts',(-0.117598114366551,-4.518327158929E-5,
0.782563288526384));
#16330=CARTESIAN_POINT('Ctrl Pts',(-0.117591850253004,-3.65476421498364E-5,
0.742436711473616));
#16331=CARTESIAN_POINT('Ctrl Pts',(-0.117640211257931,-0.0174335619022046,
0.743607926264006));
#16332=CARTESIAN_POINT('Ctrl Pts',(-0.105863856762799,-0.0740921523660566,
0.747426530428656));
#16333=CARTESIAN_POINT('Ctrl Pts',(-0.0182163644075178,-0.138029133036789,
0.753892523967566));
#16334=CARTESIAN_POINT('Ctrl Pts',(0.106128952536144,-0.0901139441634624,
0.761834692090347));
#16335=CARTESIAN_POINT('Ctrl Pts',(0.133249245915149,0.0403548753208232,
0.769776860213125));
#16336=CARTESIAN_POINT('Ctrl Pts',(0.0382995408207276,0.133854483197375,
0.777719028335907));
#16337=CARTESIAN_POINT('Ctrl Pts',(-0.0853693283863186,0.106155717082476,
0.785272312089402));
#16338=CARTESIAN_POINT('Ctrl Pts',(-0.117593892160246,0.0332537408718532,
0.79017820646864));
#16339=CARTESIAN_POINT('Ctrl Pts',(-0.117874685330111,-8.9283644551537E-5,
0.792436711473617));
#16340=CARTESIAN_POINT('Origin',(0.,0.,-0.0924367114736175));
#16341=CARTESIAN_POINT('',(-0.117964947617991,-1.73329198795185E-5,0.682563288526384));
#16342=CARTESIAN_POINT('',(-0.117740574064672,0.000107068518266168,0.692436711473616));
#16343=CARTESIAN_POINT('',(-0.117775,2.85464118895969E-14,-0.0924367114736175));
#16344=CARTESIAN_POINT('Ctrl Pts',(-0.117964947617991,-1.73329198795367E-5,
0.682563288526384));
#16345=CARTESIAN_POINT('Ctrl Pts',(-0.117966864156947,-0.000949576032666658,
0.682626561953687));
#16346=CARTESIAN_POINT('Ctrl Pts',(-0.117534558560489,-0.0408698671952461,
0.685336165260092));
#16347=CARTESIAN_POINT('Ctrl Pts',(-0.0726787294560835,-0.118728463672822,
0.690692098445597));
#16348=CARTESIAN_POINT('Ctrl Pts',(0.0603425395611779,-0.125448888878168,
0.698631088082904));
#16349=CARTESIAN_POINT('Ctrl Pts',(0.138124349154501,-0.0173294538893964,
0.706570077720209));
#16350=CARTESIAN_POINT('Ctrl Pts',(0.0894627833767505,0.106653908470079,
0.714509067357515));
#16351=CARTESIAN_POINT('Ctrl Pts',(-0.0410958292974484,0.133002927094911,
0.72244805699482));
#16352=CARTESIAN_POINT('Ctrl Pts',(-0.111546724107196,0.0606813038481789,
0.728466130717777));
#16353=CARTESIAN_POINT('Ctrl Pts',(-0.117820302634623,0.0108495967181263,
0.731837874561632));
#16354=CARTESIAN_POINT('Ctrl Pts',(-0.11772691567491,0.000105512987197042,
0.732563288526384));
#16355=CARTESIAN_POINT('Ctrl Pts',(-0.117740574064672,0.000107068518266165,
0.692436711473616));
#16356=CARTESIAN_POINT('Ctrl Pts',(-0.117483171888848,-0.0288182833237499,
0.694390256685113));
#16357=CARTESIAN_POINT('Ctrl Pts',(-0.0921515028359353,-0.0973455904149804,
0.698991191270869));
#16358=CARTESIAN_POINT('Ctrl Pts',(0.022691720100341,-0.137364345221032,
0.706239515230886));
#16359=CARTESIAN_POINT('Ctrl Pts',(0.127740337615313,-0.0553740340325759,
0.714181683353665));
#16360=CARTESIAN_POINT('Ctrl Pts',(0.115765682611161,0.077344581120379,
0.722123851476446));
#16361=CARTESIAN_POINT('Ctrl Pts',(-0.00226223072526165,0.139207614056346,
0.730066019599226));
#16362=CARTESIAN_POINT('Ctrl Pts',(-0.101117998472899,0.083225715609228,
0.736836972931616));
#16363=CARTESIAN_POINT('Ctrl Pts',(-0.117530897055598,0.0218902846491045,
0.740960536889746));
#16364=CARTESIAN_POINT('Ctrl Pts',(-0.117591850253004,-3.65476421498364E-5,
0.742436711473616));
#16365=CARTESIAN_POINT('Origin',(0.,0.,-0.0924367114736175));
#16366=CARTESIAN_POINT('',(-0.117676160015555,-9.46906955630148E-5,0.632563288526383));
#16367=CARTESIAN_POINT('',(-0.117962383120995,-2.41598447144192E-5,0.642436711473616));
#16368=CARTESIAN_POINT('',(-0.117775,2.85464118895969E-14,-0.0924367114736175));
#16369=CARTESIAN_POINT('Ctrl Pts',(-0.117676160015555,-9.46906955630045E-5,
0.632563288526383));
#16370=CARTESIAN_POINT('Ctrl Pts',(-0.117771520970562,-0.0127268345011372,
0.633415249345741));
#16371=CARTESIAN_POINT('Ctrl Pts',(-0.110078248258936,-0.064483421762156,
0.636913540044201));
#16372=CARTESIAN_POINT('Ctrl Pts',(-0.0347063025259737,-0.134811417789573,
0.643058160621763));
#16373=CARTESIAN_POINT('Ctrl Pts',(0.0944472082050275,-0.102266175560326,
0.65099715025907));
#16374=CARTESIAN_POINT('Ctrl Pts',(0.137140772714236,0.0238967416356601,
0.658936139896373));
#16375=CARTESIAN_POINT('Ctrl Pts',(0.054291358674537,0.128183829614862,
0.666875129533682));
#16376=CARTESIAN_POINT('Ctrl Pts',(-0.0772016597727435,0.11523146575827,
0.674750845743682));
#16377=CARTESIAN_POINT('Ctrl Pts',(-0.117886707375211,0.0380402955314478,
0.679980232074585));
#16378=CARTESIAN_POINT('Ctrl Pts',(-0.117964947617991,-1.73329198795367E-5,
0.682563288526384));
#16379=CARTESIAN_POINT('Ctrl Pts',(-0.117962383120995,-2.41598447144253E-5,
0.642436711473616));
#16380=CARTESIAN_POINT('Ctrl Pts',(-0.117966033213387,-0.0013279541977536,
0.642525197731959));
#16381=CARTESIAN_POINT('Ctrl Pts',(-0.117355585052125,-0.0416360146359673,
0.645261073364563));
#16382=CARTESIAN_POINT('Ctrl Pts',(-0.0715088964667609,-0.119458592094588,
0.650644338371427));
#16383=CARTESIAN_POINT('Ctrl Pts',(0.0616402393688536,-0.124837327709565,
0.658586506494205));
#16384=CARTESIAN_POINT('Ctrl Pts',(0.138320583400205,-0.0158522461166236,
0.666528674616987));
#16385=CARTESIAN_POINT('Ctrl Pts',(0.0882850628235238,0.107655121482266,
0.674470842739765));
#16386=CARTESIAN_POINT('Ctrl Pts',(-0.0426286451686149,0.132539337972556,
0.682413010862546));
#16387=CARTESIAN_POINT('Ctrl Pts',(-0.111894847147975,0.059748848130285,
0.68840163377383));
#16388=CARTESIAN_POINT('Ctrl Pts',(-0.117831996057943,0.0103805377030848,
0.691742867310853));
#16389=CARTESIAN_POINT('Ctrl Pts',(-0.117740574064672,0.000107068518266165,
0.692436711473616));
#16390=CARTESIAN_POINT('Origin',(0.,0.,-0.0924367114736175));
#16391=CARTESIAN_POINT('',(-0.117626285855324,7.11112359239178E-5,0.582563288526384));
#16392=CARTESIAN_POINT('',(-0.11766919235599,-9.26074537421634E-5,0.592436711473616));
#16393=CARTESIAN_POINT('',(-0.117775,2.85464118895969E-14,-0.0924367114736175));
#16394=CARTESIAN_POINT('Ctrl Pts',(-0.117626285855324,7.11112359239024E-5,
0.582563288526383));
#16395=CARTESIAN_POINT('Ctrl Pts',(-0.117492102008102,-0.0242809575267813,
0.584203936737797));
#16396=CARTESIAN_POINT('Ctrl Pts',(-0.0982512120079041,-0.0881067492982899,
0.588490914828312));
#16397=CARTESIAN_POINT('Ctrl Pts',(0.00631176444456456,-0.139064040754811,
0.595424222797929));
#16398=CARTESIAN_POINT('Ctrl Pts',(0.120263693490807,-0.0701091280034811,
0.603363212435234));
#16399=CARTESIAN_POINT('Ctrl Pts',(0.124122453355413,0.0630258865426945,
0.611302202072541));
#16400=CARTESIAN_POINT('Ctrl Pts',(0.0143556138404206,0.138465021405133,
0.619241191709845));
#16401=CARTESIAN_POINT('Ctrl Pts',(-0.0953630726970595,0.0926558297308384,
0.626328220527794));
#16402=CARTESIAN_POINT('Ctrl Pts',(-0.117475314221613,0.0265106736450616,
0.630768919466639));
#16403=CARTESIAN_POINT('Ctrl Pts',(-0.117676160015555,-9.46906955630045E-5,
0.632563288526383));
#16404=CARTESIAN_POINT('Ctrl Pts',(-0.11766919235599,-9.26074537421669E-5,
0.592436711473616));
#16405=CARTESIAN_POINT('Ctrl Pts',(-0.117764072896019,-0.0130062487266101,
0.593307528153066));
#16406=CARTESIAN_POINT('Ctrl Pts',(-0.109848366281979,-0.0650658641993071,
0.596825734206776));
#16407=CARTESIAN_POINT('Ctrl Pts',(-0.0336977294021144,-0.135086418755761,
0.602991329634746));
#16408=CARTESIAN_POINT('Ctrl Pts',(0.0952657566843092,-0.101529863106778,
0.610933497757526));
#16409=CARTESIAN_POINT('Ctrl Pts',(0.136956022624868,0.025038477707157,
0.618875665880307));
#16410=CARTESIAN_POINT('Ctrl Pts',(0.0531805018142573,0.128669000640787,
0.626817834003085));
#16411=CARTESIAN_POINT('Ctrl Pts',(-0.0778376600742765,0.114584191752874,
0.634671515867523));
#16412=CARTESIAN_POINT('Ctrl Pts',(-0.117856827377429,0.0376798124439797,
0.639877808357699));
#16413=CARTESIAN_POINT('Ctrl Pts',(-0.117962383120995,-2.41598447144253E-5,
0.642436711473616));
#16414=CARTESIAN_POINT('Origin',(0.,0.,-0.0924367114736175));
#16415=CARTESIAN_POINT('',(-0.117934829819181,5.63106208242181E-5,0.532563288526383));
#16416=CARTESIAN_POINT('',(-0.117629301205424,7.34277634442948E-5,0.542436711473615));
#16417=CARTESIAN_POINT('',(-0.117775,2.85464118895969E-14,-0.0924367114736175));
#16418=CARTESIAN_POINT('Ctrl Pts',(-0.117934829819181,5.63106208242166E-5,
0.532563288526383));
#16419=CARTESIAN_POINT('Ctrl Pts',(-0.117723349859012,-0.0357608023914865,
0.534992624129852));
#16420=CARTESIAN_POINT('Ctrl Pts',(-0.0811985738067347,-0.110967619805887,
0.540068289612422));
#16421=CARTESIAN_POINT('Ctrl Pts',(0.0467759446245483,-0.131113145053959,
0.547790284974095));
#16422=CARTESIAN_POINT('Ctrl Pts',(0.135526478334676,-0.031799677225719,
0.555729274611401));
#16423=CARTESIAN_POINT('Ctrl Pts',(0.100211809365564,0.0966242157284558,
0.563668264248707));
#16424=CARTESIAN_POINT('Ctrl Pts',(-0.0268399031138932,0.136595261273209,
0.571607253886012));
#16425=CARTESIAN_POINT('Ctrl Pts',(-0.108142973925314,0.0691035501437442,
0.577905595311905));
#16426=CARTESIAN_POINT('Ctrl Pts',(-0.117708537635025,0.0149983997031143,
0.581557606858695));
#16427=CARTESIAN_POINT('Ctrl Pts',(-0.117626285855324,7.11112359239024E-5,
0.582563288526383));
#16428=CARTESIAN_POINT('Ctrl Pts',(-0.117629301205424,7.34277634442983E-5,
0.542436711473615));
#16429=CARTESIAN_POINT('Ctrl Pts',(-0.11748956090956,-0.0244625652698295,
0.544089858574172));
#16430=CARTESIAN_POINT('Ctrl Pts',(-0.0980201725405651,-0.0884941619373469,
0.548390395048989));
#16431=CARTESIAN_POINT('Ctrl Pts',(0.00702343738442799,-0.139048728244533,
0.555338320898066));
#16432=CARTESIAN_POINT('Ctrl Pts',(0.12066450826877,-0.0694546898587181,
0.563280489020846));
#16433=CARTESIAN_POINT('Ctrl Pts',(0.123764493242992,0.063766979789076,
0.571222657143626));
#16434=CARTESIAN_POINT('Ctrl Pts',(0.0134834875971477,0.13857154491934,
0.579164825266405));
#16435=CARTESIAN_POINT('Ctrl Pts',(-0.0957036897026042,0.092147346049863,
0.586236176709736));
#16436=CARTESIAN_POINT('Ctrl Pts',(-0.117475624432153,0.0262528025703711,
0.590660138778806));
#16437=CARTESIAN_POINT('Ctrl Pts',(-0.11766919235599,-9.26074537421669E-5,
0.592436711473616));
#16438=CARTESIAN_POINT('Origin',(0.,0.,-0.0924367114736175));
#16439=CARTESIAN_POINT('',(-0.117794891956694,-0.000106411733115368,0.482563288526384));
#16440=CARTESIAN_POINT('',(-0.117936566864074,5.52347650140707E-5,0.492436711473616));
#16441=CARTESIAN_POINT('',(-0.117775,2.85464118895969E-14,-0.0924367114736175));
#16442=CARTESIAN_POINT('Ctrl Pts',(-0.117794891956694,-0.000106411733115381,
0.482563288526384));
#16443=CARTESIAN_POINT('Ctrl Pts',(-0.117872998614688,-0.00856127641466401,
0.483134981642805));
#16444=CARTESIAN_POINT('Ctrl Pts',(-0.113184542395844,-0.0560672187853419,
0.486353004638329));
#16445=CARTESIAN_POINT('Ctrl Pts',(-0.0487302328423073,-0.130399425645183,
0.492217357512954));
#16446=CARTESIAN_POINT('Ctrl Pts',(0.0831353173341669,-0.111656458896056,
0.50015634715026));
#16447=CARTESIAN_POINT('Ctrl Pts',(0.13889618212661,0.00930034365552528,
0.508095336787567));
#16448=CARTESIAN_POINT('Ctrl Pts',(0.0675071113591811,0.12174331898465,
0.516034326424871));
#16449=CARTESIAN_POINT('Ctrl Pts',(-0.0656800932930844,0.122738629397884,
0.523973316062178));
#16450=CARTESIAN_POINT('Ctrl Pts',(-0.116384786286051,0.04545243224792,
0.529482970096015));
#16451=CARTESIAN_POINT('Ctrl Pts',(-0.117953719733239,0.00325558390455253,
0.53234629425075));
#16452=CARTESIAN_POINT('Ctrl Pts',(-0.117934829819181,5.63106208242166E-5,
0.532563288526383));
#16453=CARTESIAN_POINT('Ctrl Pts',(-0.117936566864074,5.52347650140663E-5,
0.492436711473616));
#16454=CARTESIAN_POINT('Ctrl Pts',(-0.117728017843002,-0.0358510361847084,
0.494872188995279));
#16455=CARTESIAN_POINT('Ctrl Pts',(-0.0810366231971402,-0.111156550628637,
0.499955055891203));
#16456=CARTESIAN_POINT('Ctrl Pts',(0.0471380885036503,-0.131003351527116,
0.507685312161385));
#16457=CARTESIAN_POINT('Ctrl Pts',(0.135643160584381,-0.031381690295376,
0.515627480284167));
#16458=CARTESIAN_POINT('Ctrl Pts',(0.0998851624184703,0.0969888232104648,
0.523569648406945));
#16459=CARTESIAN_POINT('Ctrl Pts',(-0.0273779061153799,0.136507610615132,
0.531511816529727));
#16460=CARTESIAN_POINT('Ctrl Pts',(-0.108290992649607,0.0687756007668377,
0.537800837551949));
#16461=CARTESIAN_POINT('Ctrl Pts',(-0.117713344367368,0.0148299618267192,
0.541442469199912));
#16462=CARTESIAN_POINT('Ctrl Pts',(-0.117629301205424,7.34277634442983E-5,
0.542436711473615));
#16463=CARTESIAN_POINT('Origin',(0.,0.,-0.0924367114736175));
#16464=CARTESIAN_POINT('',(-0.117582256074849,9.06819982020624E-6,0.432563288526383));
#16465=CARTESIAN_POINT('',(-0.11779560903417,-0.000106574656651148,0.442436711473616));
#16466=CARTESIAN_POINT('',(-0.117775,2.85464118895969E-14,-0.0924367114736175));
#16467=CARTESIAN_POINT('Ctrl Pts',(-0.117582256074849,9.06819982019261E-6,
0.432563288526383));
#16468=CARTESIAN_POINT('Ctrl Pts',(-0.117568373935691,-0.020201912089319,
0.43392366903486));
#16469=CARTESIAN_POINT('Ctrl Pts',(-0.10300922874285,-0.0797477867736473,
0.437930379422439));
#16470=CARTESIAN_POINT('Ctrl Pts',(-0.00838939967687663,-0.138954178686792,
0.44458341968912));
#16471=CARTESIAN_POINT('Ctrl Pts',(0.11219917790857,-0.0824013973067221,
0.452522409326426));
#16472=CARTESIAN_POINT('Ctrl Pts',(0.13007709763057,0.0495842159710775,
0.460461398963732));
#16473=CARTESIAN_POINT('Ctrl Pts',(0.0288783492374893,0.136178877755608,
0.468400388601037));
#16474=CARTESIAN_POINT('Ctrl Pts',(-0.0895654556576369,0.100852400902523,
0.475767685121922));
#16475=CARTESIAN_POINT('Ctrl Pts',(-0.117511448025972,0.0305757367622385,
0.480488651763704));
#16476=CARTESIAN_POINT('Ctrl Pts',(-0.117794891956694,-0.000106411733115381,
0.482563288526384));
#16477=CARTESIAN_POINT('Ctrl Pts',(-0.11779560903417,-0.000106574656651151,
0.442436711473616));
#16478=CARTESIAN_POINT('Ctrl Pts',(-0.117873644338608,-0.00854245500997505,
0.443007130042126));
#16479=CARTESIAN_POINT('Ctrl Pts',(-0.113196618671047,-0.056044542179559,
0.446224937984896));
#16480=CARTESIAN_POINT('Ctrl Pts',(-0.0487473834415776,-0.130413074907061,
0.452090135301926));
#16481=CARTESIAN_POINT('Ctrl Pts',(0.0831820848081396,-0.111645054821459,
0.460032303424706));
#16482=CARTESIAN_POINT('Ctrl Pts',(0.138908217753341,0.00940130521287039,
0.467974471547486));
#16483=CARTESIAN_POINT('Ctrl Pts',(0.0673801526530663,0.121835103839429,
0.475916639670265));
#16484=CARTESIAN_POINT('Ctrl Pts',(-0.0658750545035054,0.12265543075329,
0.483858807793047));
#16485=CARTESIAN_POINT('Ctrl Pts',(-0.116424939330292,0.0453161125527027,
0.489365498394162));
#16486=CARTESIAN_POINT('Ctrl Pts',(-0.11795471279604,0.00317945345687678,
0.492224799621019));
#16487=CARTESIAN_POINT('Ctrl Pts',(-0.117936566864074,5.52347650140663E-5,
0.492436711473616));
#16488=CARTESIAN_POINT('Origin',(0.,0.,-0.0924367114736175));
#16489=CARTESIAN_POINT('',(-0.117828183671793,0.000101754196006455,0.382563288526383));
#16490=CARTESIAN_POINT('',(-0.117581664177921,7.09484545444172E-6,0.392436711473616));
#16491=CARTESIAN_POINT('',(-0.117775,2.85464118895969E-14,-0.0924367114736175));
#16492=CARTESIAN_POINT('Ctrl Pts',(-0.117828183671793,0.000101754196006446,
0.382563288526384));
#16493=CARTESIAN_POINT('Ctrl Pts',(-0.117538790254565,-0.0316580736410773,
0.384712356426916));
#16494=CARTESIAN_POINT('Ctrl Pts',(-0.0879068326507716,-0.103002379129266,
0.38950775420655));
#16495=CARTESIAN_POINT('Ctrl Pts',(0.0326876424682324,-0.135315053971568,
0.396949481865287));
#16496=CARTESIAN_POINT('Ctrl Pts',(0.13141703692502,-0.0459152284901983,
0.404888471502591));
#16497=CARTESIAN_POINT('Ctrl Pts',(0.109843140674695,0.0855168418978295,
0.412827461139898));
#16498=CARTESIAN_POINT('Ctrl Pts',(-0.0122846228212416,0.13866410438033,
0.420766450777203));
#16499=CARTESIAN_POINT('Ctrl Pts',(-0.104166535924894,0.0775181589932739,
0.427345059906032));
#16500=CARTESIAN_POINT('Ctrl Pts',(-0.117595378674006,0.0191142356295008,
0.431277339155758));
#16501=CARTESIAN_POINT('Ctrl Pts',(-0.117582256074849,9.06819982019261E-6,
0.432563288526383));
#16502=CARTESIAN_POINT('Ctrl Pts',(-0.117581664177921,7.09484545444172E-6,
0.392436711473616));
#16503=CARTESIAN_POINT('Ctrl Pts',(-0.117570873504463,-0.0200907396801347,
0.393789460463232));
#16504=CARTESIAN_POINT('Ctrl Pts',(-0.10312708440739,-0.079535468422451,
0.397789598827109));
#16505=CARTESIAN_POINT('Ctrl Pts',(-0.00873482453528946,-0.138951719454826,
0.404437126565246));
#16506=CARTESIAN_POINT('Ctrl Pts',(0.112042812448737,-0.0826455423945668,
0.412379294688026));
#16507=CARTESIAN_POINT('Ctrl Pts',(0.130177722634257,0.049372441998279,
0.420321462810806));
#16508=CARTESIAN_POINT('Ctrl Pts',(0.0290564652212241,0.136160197297018,
0.428263630933586));
#16509=CARTESIAN_POINT('Ctrl Pts',(-0.0895090212855029,0.100936776489487,
0.435635380487856));
#16510=CARTESIAN_POINT('Ctrl Pts',(-0.117511471984497,0.0306096014671689,
0.440359740667866));
#16511=CARTESIAN_POINT('Ctrl Pts',(-0.11779560903417,-0.000106574656651151,
0.442436711473616));
#16512=CARTESIAN_POINT('Origin',(0.,0.,-0.0924367114736175));
#16513=CARTESIAN_POINT('',(-0.117911328466355,-7.22474488887591E-5,0.332563288526384));
#16514=CARTESIAN_POINT('',(-0.117821685414254,0.000103165543095151,0.342436711473616));
#16515=CARTESIAN_POINT('',(-0.117775,2.85464118895969E-14,-0.0924367114736175));
#16516=CARTESIAN_POINT('Ctrl Pts',(-0.117911328466355,-7.22474488887752E-5,
0.332563288526384));
#16517=CARTESIAN_POINT('Ctrl Pts',(-0.117942332027964,-0.00437115939612809,
0.332854713939869));
#16518=CARTESIAN_POINT('Ctrl Pts',(-0.115777752883067,-0.0476754067323583,
0.335792469232457));
#16519=CARTESIAN_POINT('Ctrl Pts',(-0.0622106591311991,-0.12453304658572,
0.341376554404146));
#16520=CARTESIAN_POINT('Ctrl Pts',(0.0708961914151981,-0.119801401679107,
0.349315544041452));
#16521=CARTESIAN_POINT('Ctrl Pts',(0.1391024375543,-0.00539978406154301,
0.357254533678757));
#16522=CARTESIAN_POINT('Ctrl Pts',(0.0799699354250877,0.113944965792994,
0.365193523316063));
#16523=CARTESIAN_POINT('Ctrl Pts',(-0.0523695618881846,0.128980908622551,
0.373132512953369));
#16524=CARTESIAN_POINT('Ctrl Pts',(-0.113921748517257,0.0538356345748906,
0.378922434690143));
#16525=CARTESIAN_POINT('Ctrl Pts',(-0.117895144954496,0.00745050051778832,
0.382066026547814));
#16526=CARTESIAN_POINT('Ctrl Pts',(-0.117828183671793,0.000101754196006446,
0.382563288526384));
#16527=CARTESIAN_POINT('Ctrl Pts',(-0.117821685414254,0.000103165543095145,
0.342436711473616));
#16528=CARTESIAN_POINT('Ctrl Pts',(-0.117532262555972,-0.0314544122979593,
0.344571790884339));
#16529=CARTESIAN_POINT('Ctrl Pts',(-0.0882170202347594,-0.102616110661261,
0.349354259669323));
#16530=CARTESIAN_POINT('Ctrl Pts',(0.0320320385160992,-0.135491055083419,
0.356784117828566));
#16531=CARTESIAN_POINT('Ctrl Pts',(0.131227975626944,-0.0465090949381858,
0.364726285951346));
#16532=CARTESIAN_POINT('Ctrl Pts',(0.110205605501345,0.0850799742312894,
0.372668454074126));
#16533=CARTESIAN_POINT('Ctrl Pts',(-0.0117764211155082,0.138727046407055,
0.380610622196906));
#16534=CARTESIAN_POINT('Ctrl Pts',(-0.10403099481448,0.0777947493501838,
0.387200041330069));
#16535=CARTESIAN_POINT('Ctrl Pts',(-0.117591991327853,0.019241607989002,
0.391142071088973));
#16536=CARTESIAN_POINT('Ctrl Pts',(-0.117581664177921,7.09484545444172E-6,
0.392436711473616));
#16537=CARTESIAN_POINT('Origin',(0.,0.,-0.0924367114736175));
#16538=CARTESIAN_POINT('',(-0.117608153246896,-5.64262068778628E-5,0.282563288526383));
#16539=CARTESIAN_POINT('',(-0.117918861549493,-6.80329776671096E-5,0.292436711473615));
#16540=CARTESIAN_POINT('',(-0.117775,2.85464118895969E-14,-0.0924367114736175));
#16541=CARTESIAN_POINT('Ctrl Pts',(-0.117608153246896,-5.64262068778604E-5,
0.282563288526383));
#16542=CARTESIAN_POINT('Ctrl Pts',(-0.117677606263852,-0.0160946837114709,
0.283643401331924));
#16543=CARTESIAN_POINT('Ctrl Pts',(-0.107144424846824,-0.0713401098021974,
0.287369844016567));
#16544=CARTESIAN_POINT('Ctrl Pts',(-0.0229969941138309,-0.137294515779738,
0.293742616580312));
#16545=CARTESIAN_POINT('Ctrl Pts',(0.102883268653204,-0.0937746172089793,
0.301681606217617));
#16546=CARTESIAN_POINT('Ctrl Pts',(0.134580950019115,0.0355895166223291,
0.309620595854923));
#16547=CARTESIAN_POINT('Ctrl Pts',(0.0430789950773988,0.13237388709478,
0.317559585492229));
#16548=CARTESIAN_POINT('Ctrl Pts',(-0.0830523456774332,0.10887452531409,
0.325207149716049));
#16549=CARTESIAN_POINT('Ctrl Pts',(-0.11766079978112,0.0346657214219864,
0.330208384060767));
#16550=CARTESIAN_POINT('Ctrl Pts',(-0.117911328466355,-7.22474488887752E-5,
0.332563288526384));
#16551=CARTESIAN_POINT('Ctrl Pts',(-0.117918861549493,-6.80329776671157E-5,
0.292436711473616));
#16552=CARTESIAN_POINT('Ctrl Pts',(-0.117946256357307,-0.00405052459867665,
0.292706731931186));
#16553=CARTESIAN_POINT('Ctrl Pts',(-0.11595553950755,-0.0470512577090033,
0.295624141763016));
#16554=CARTESIAN_POINT('Ctrl Pts',(-0.0631725212350128,-0.124068972994571,
0.301188940969106));
#16555=CARTESIAN_POINT('Ctrl Pts',(0.0700327441786229,-0.12032993078169,
0.309131109091886));
#16556=CARTESIAN_POINT('Ctrl Pts',(0.139080821187468,-0.00635631000930847,
0.317073277214666));
#16557=CARTESIAN_POINT('Ctrl Pts',(0.0807165776729536,0.11344034374014,
0.325015445337446));
#16558=CARTESIAN_POINT('Ctrl Pts',(-0.0515923433190751,0.129313988454311,
0.332957613460226));
#16559=CARTESIAN_POINT('Ctrl Pts',(-0.113774867115171,0.0543021652640841,
0.338764702172283));
#16560=CARTESIAN_POINT('Ctrl Pts',(-0.117891132111753,0.00767537174388221,
0.341924401510079));
#16561=CARTESIAN_POINT('Ctrl Pts',(-0.117821685414254,0.000103165543095145,
0.342436711473616));
#16562=CARTESIAN_POINT('Origin',(0.,0.,-0.0924367114736175));
#16563=CARTESIAN_POINT('',(-0.117705188630573,0.000102098618198066,0.232563288526383));
#16564=CARTESIAN_POINT('',(-0.1176142238744,-6.23262858038681E-5,0.242436711473616));
#16565=CARTESIAN_POINT('',(-0.117775,2.85464118895969E-14,-0.0924367114736175));
#16566=CARTESIAN_POINT('Ctrl Pts',(-0.117705188630573,0.000102098618198071,
0.232563288526383));
#16567=CARTESIAN_POINT('Ctrl Pts',(-0.117475649963863,-0.0275896003179174,
0.234432088723979));
#16568=CARTESIAN_POINT('Ctrl Pts',(-0.0938913217252411,-0.0948462909608301,
0.238947218800678));
#16569=CARTESIAN_POINT('Ctrl Pts',(0.0182347644767634,-0.138007750384372,
0.246108678756477));
#16570=CARTESIAN_POINT('Ctrl Pts',(0.125841858853055,-0.0595186723796334,
0.254047668393783));
#16571=CARTESIAN_POINT('Ctrl Pts',(0.118249355954961,0.073455671106145,
0.261986658031089));
#16572=CARTESIAN_POINT('Ctrl Pts',(0.00240767183786234,0.139186381940956,
0.269925647668394));
#16573=CARTESIAN_POINT('Ctrl Pts',(-0.0995777503027144,0.0858938305448248,
0.27678452450016));
#16574=CARTESIAN_POINT('Ctrl Pts',(-0.117507442931816,0.0231998416616275,
0.280997071452822));
#16575=CARTESIAN_POINT('Ctrl Pts',(-0.117608153246896,-5.64262068778604E-5,
0.282563288526383));
#16576=CARTESIAN_POINT('Ctrl Pts',(-0.1176142238744,-6.2326285803882E-5,
0.242436711473616));
#16577=CARTESIAN_POINT('Ctrl Pts',(-0.117689148257971,-0.0156863246439697,
0.243489062352292));
#16578=CARTESIAN_POINT('Ctrl Pts',(-0.107519643382358,-0.0705218816827611,
0.247188802605229));
#16579=CARTESIAN_POINT('Ctrl Pts',(-0.024381182195918,-0.137074561658528,
0.253535932232426));
#16580=CARTESIAN_POINT('Ctrl Pts',(0.101985705091022,-0.094777599970642,
0.261478100355206));
#16581=CARTESIAN_POINT('Ctrl Pts',(0.134923209124943,0.0343453801629359,
0.269420268477986));
#16582=CARTESIAN_POINT('Ctrl Pts',(0.0442571924125319,0.132004463632409,
0.277362436600766));
#16583=CARTESIAN_POINT('Ctrl Pts',(-0.0824920331482911,0.109525057495754,
0.285034584265976));
#16584=CARTESIAN_POINT('Ctrl Pts',(-0.117677666622401,0.0349954280503056,
0.290059342556926));
#16585=CARTESIAN_POINT('Ctrl Pts',(-0.117918861549493,-6.80329776671157E-5,
0.292436711473616));
#16586=CARTESIAN_POINT('Origin',(0.,0.,-0.0924367114736175));
#16587=CARTESIAN_POINT('',(-0.117967994073432,-3.0724305424694E-6,0.182563288526383));
#16588=CARTESIAN_POINT('',(-0.117691121003631,9.91971943564221E-5,0.192436711473615));
#16589=CARTESIAN_POINT('',(-0.117775,2.85464118895969E-14,-0.0924367114736175));
#16590=CARTESIAN_POINT('Ctrl Pts',(-0.117967994073432,-3.07243054247449E-6,
0.182563288526383));
#16591=CARTESIAN_POINT('Ctrl Pts',(-0.117968057042159,-0.000167453844217198,
0.182574446236933));
#16592=CARTESIAN_POINT('Ctrl Pts',(-0.117893299674953,-0.0393189363008842,
0.185231933826584));
#16593=CARTESIAN_POINT('Ctrl Pts',(-0.0749972298318695,-0.11727771015962,
0.190535751295337));
#16594=CARTESIAN_POINT('Ctrl Pts',(0.0578663373665801,-0.126610160769685,
0.198474740932643));
#16595=CARTESIAN_POINT('Ctrl Pts',(0.13775723856723,-0.0200396862227523,
0.206413730569949));
#16596=CARTESIAN_POINT('Ctrl Pts',(0.091540828968026,0.104875747581476,
0.214352720207254));
#16597=CARTESIAN_POINT('Ctrl Pts',(-0.0384749358425138,0.133784622116252,
0.22229170984456));
#16598=CARTESIAN_POINT('Ctrl Pts',(-0.110955338697302,0.0622468391270206,
0.22836189928427));
#16599=CARTESIAN_POINT('Ctrl Pts',(-0.11780069007939,0.0116234575531164,
0.231785758844877));
#16600=CARTESIAN_POINT('Ctrl Pts',(-0.117705188630573,0.000102098618198071,
0.232563288526383));
#16601=CARTESIAN_POINT('Ctrl Pts',(-0.117691121003631,9.91971943564221E-5,
0.192436711473615));
#16602=CARTESIAN_POINT('Ctrl Pts',(-0.117474218986382,-0.0270951350261672,
0.194271392773399));
#16603=CARTESIAN_POINT('Ctrl Pts',(-0.0945676524372527,-0.0938598508209937,
0.198753463447442));
#16604=CARTESIAN_POINT('Ctrl Pts',(0.0165156171993534,-0.138242945169174,
0.205882923495746));
#16605=CARTESIAN_POINT('Ctrl Pts',(0.125131592687617,-0.061040658666823,
0.213825091618526));
#16606=CARTESIAN_POINT('Ctrl Pts',(0.119114174013628,0.0720811421096423,
0.221767259741306));
#16607=CARTESIAN_POINT('Ctrl Pts',(0.0039759348809324,0.139169211541763,
0.229709427864086));
#16608=CARTESIAN_POINT('Ctrl Pts',(-0.0990660356104632,0.0867677816679632,
0.236599245108189));
#16609=CARTESIAN_POINT('Ctrl Pts',(-0.117500661679058,0.0236188235484957,
0.240841672978032));
#16610=CARTESIAN_POINT('Ctrl Pts',(-0.1176142238744,-6.2326285803882E-5,
0.242436711473616));
#16611=CARTESIAN_POINT('Origin',(0.,0.,-0.0924367114736175));
#16612=CARTESIAN_POINT('',(-0.117696212882312,-0.000100181105204699,0.132563288526383));
#16613=CARTESIAN_POINT('',(-0.117967699956222,8.3697257429456E-6,0.142436711473616));
#16614=CARTESIAN_POINT('',(-0.117775,2.85464118895969E-14,-0.0924367114736175));
#16615=CARTESIAN_POINT('Ctrl Pts',(-0.117696212882312,-0.000100181105204706,
0.132563288526383));
#16616=CARTESIAN_POINT('Ctrl Pts',(-0.117792074781153,-0.0119544960022407,
0.133363133628988));
#16617=CARTESIAN_POINT('Ctrl Pts',(-0.110696412003459,-0.0629173266909915,
0.136809308610694));
#16618=CARTESIAN_POINT('Ctrl Pts',(-0.0373480950846616,-0.134103559412242,
0.142901813471503));
#16619=CARTESIAN_POINT('Ctrl Pts',(0.0924198687735613,-0.104101940294199,
0.150840803108809));
#16620=CARTESIAN_POINT('Ctrl Pts',(0.137583777756591,0.0211978768359354,
0.158779792746114));
#16621=CARTESIAN_POINT('Ctrl Pts',(0.0567991668878991,0.127092487218924,
0.16671878238342));
#16622=CARTESIAN_POINT('Ctrl Pts',(-0.0757945745091616,0.116657324056303,
0.174646614310176));
#16623=CARTESIAN_POINT('Ctrl Pts',(-0.117953122434976,0.0388197061692436,
0.179928116357831));
#16624=CARTESIAN_POINT('Ctrl Pts',(-0.117967994073432,-3.07243054247449E-6,
0.182563288526383));
#16625=CARTESIAN_POINT('Ctrl Pts',(-0.117967699956222,8.3697257429579E-6,
0.142436711473616));
#16626=CARTESIAN_POINT('Ctrl Pts',(-0.117928252023989,-0.038547130539091,
0.145053723194506));
#16627=CARTESIAN_POINT('Ctrl Pts',(-0.0762804946418446,-0.116178754198862,
0.150318124289656));
#16628=CARTESIAN_POINT('Ctrl Pts',(0.0559861945572589,-0.127473226882309,
0.158229914759066));
#16629=CARTESIAN_POINT('Ctrl Pts',(0.137471621702818,-0.0220324926503626,
0.166172082881846));
#16630=CARTESIAN_POINT('Ctrl Pts',(0.0930189202108026,0.103592267873211,
0.174114251004626));
#16631=CARTESIAN_POINT('Ctrl Pts',(-0.0366486683060043,0.134315868829211,
0.182056419127406));
#16632=CARTESIAN_POINT('Ctrl Pts',(-0.110544190454925,0.0633195416932908,
0.188163905950403));
#16633=CARTESIAN_POINT('Ctrl Pts',(-0.11778720200735,0.0121454601492482,
0.191624003399139));
#16634=CARTESIAN_POINT('Ctrl Pts',(-0.117691121003631,9.91971943564221E-5,
0.192436711473615));
#16635=CARTESIAN_POINT('Origin',(0.,0.,-0.0924367114736175));
#16636=CARTESIAN_POINT('',(-0.117613109409711,6.11591708146705E-5,0.0825632885263832));
#16637=CARTESIAN_POINT('',(-0.117715749944134,-0.000104199409386274,0.0924367114736155));
#16638=CARTESIAN_POINT('',(-0.117775,2.85464118895969E-14,-0.0924367114736175));
#16639=CARTESIAN_POINT('Ctrl Pts',(-0.117613109409711,6.11591708146765E-5,
0.0825632885263832));
#16640=CARTESIAN_POINT('Ctrl Pts',(-0.117502393620717,-0.0235240259785673,
0.0841518210210431));
#16641=CARTESIAN_POINT('Ctrl Pts',(-0.0991849320095013,-0.0865581493706475,
0.088386683394805));
#16642=CARTESIAN_POINT('Ctrl Pts',(0.00357853460314598,-0.139161043603659,
0.0952678756476685));
#16643=CARTESIAN_POINT('Ctrl Pts',(0.118863112008681,-0.0724583686054966,
0.103206865284975));
#16644=CARTESIAN_POINT('Ctrl Pts',(0.125336705278751,0.0605752693714656,
0.11114585492228));
#16645=CARTESIAN_POINT('Ctrl Pts',(0.0170731091066207,0.138156245709763,
0.119084844559586));
#16646=CARTESIAN_POINT('Ctrl Pts',(-0.094337657277608,0.0941904991302726,
0.126223989094287));
#16647=CARTESIAN_POINT('Ctrl Pts',(-0.11747491061231,0.0272661325996615,
0.130716803749886));
#16648=CARTESIAN_POINT('Ctrl Pts',(-0.117696212882312,-0.000100181105204706,
0.132563288526383));
#16649=CARTESIAN_POINT('Ctrl Pts',(-0.117715749944134,-0.000104199409386274,
0.0924367114736155));
#16650=CARTESIAN_POINT('Ctrl Pts',(-0.117810584636384,-0.011244028442556,
0.0931886642413524));
#16651=CARTESIAN_POINT('Ctrl Pts',(-0.111246641208053,-0.0614941526881817,
0.0965880063833492));
#16652=CARTESIAN_POINT('Ctrl Pts',(-0.0397151780004399,-0.133441281507892,
0.102634737899606));
#16653=CARTESIAN_POINT('Ctrl Pts',(0.0906220264938673,-0.105695447092796,
0.110576906022386));
#16654=CARTESIAN_POINT('Ctrl Pts',(0.137940159127448,0.0188783162799928,
0.118519074145166));
#16655=CARTESIAN_POINT('Ctrl Pts',(0.0588909273047484,0.126157580947307,
0.126461242267946));
#16656=CARTESIAN_POINT('Ctrl Pts',(-0.074108440039672,0.117863552156501,
0.134403410390726));
#16657=CARTESIAN_POINT('Ctrl Pts',(-0.117763087033452,0.0399060678969832,
0.139728566792616));
#16658=CARTESIAN_POINT('Ctrl Pts',(-0.117968157858494,0.000455912857932787,
0.142406333820246));
#16659=CARTESIAN_POINT('Ctrl Pts',(-0.117967699956222,8.3697257429579E-6,
0.142436711473616));
#16660=CARTESIAN_POINT('Origin',(0.,0.,-0.0924367114736175));
#16661=CARTESIAN_POINT('',(-0.117917485785546,7.60014832213593E-5,0.0325632885263832));
#16662=CARTESIAN_POINT('',(-0.117600989619072,5.04992496179954E-5,0.0424367114736154));
#16663=CARTESIAN_POINT('',(-0.117775,2.85464118895969E-14,-0.0924367114736175));
#16664=CARTESIAN_POINT('Ctrl Pts',(-0.117917485785546,7.60014832213644E-5,
0.0325632885263832));
#16665=CARTESIAN_POINT('Ctrl Pts',(-0.117676727567847,-0.0349830640657269,
0.0349405084130983));
#16666=CARTESIAN_POINT('Ctrl Pts',(-0.0825043195215805,-0.109517225708346,
0.0399640581789154));
#16667=CARTESIAN_POINT('Ctrl Pts',(0.0441923146003338,-0.131999388615902,
0.0476339378238343));
#16668=CARTESIAN_POINT('Ctrl Pts',(0.134874939024977,-0.034459980695041,
0.0555729274611401));
#16669=CARTESIAN_POINT('Ctrl Pts',(0.102091080224759,0.094638871230671,
0.0635119170984456));
#16670=CARTESIAN_POINT('Ctrl Pts',(-0.0241513666277066,0.137095110112719,
0.0714509067357516));
#16671=CARTESIAN_POINT('Ctrl Pts',(-0.107448046275642,0.0706698818446754,
0.0778013638783972));
#16672=CARTESIAN_POINT('Ctrl Pts',(-0.117686834607281,0.0157664388843013,
0.0815054911419412));
#16673=CARTESIAN_POINT('Ctrl Pts',(-0.117613109409711,6.11591708146765E-5,
0.0825632885263832));
#16674=CARTESIAN_POINT('Ctrl Pts',(-0.117600989619072,5.04992496179954E-5,
0.0424367114736154));
#16675=CARTESIAN_POINT('Ctrl Pts',(-0.117514779739531,-0.0227353060542692,
0.043970994662459));
#16676=CARTESIAN_POINT('Ctrl Pts',(-0.100129952091853,-0.0849605109884783,
0.0481526672255625));
#16677=CARTESIAN_POINT('Ctrl Pts',(0.000787973702835166,-0.139222729671589,
0.054981729162926));
#16678=CARTESIAN_POINT('Ctrl Pts',(0.117431922513572,-0.0747907597173192,
0.0629238972857061));
#16679=CARTESIAN_POINT('Ctrl Pts',(0.126496838785129,0.0581591461343325,
0.070866065408486));
#16680=CARTESIAN_POINT('Ctrl Pts',(0.0196773008918215,0.137828289815661,
0.0788082335312661));
#16681=CARTESIAN_POINT('Ctrl Pts',(-0.0933482651079043,0.0956446566614129,
0.085998448886309));
#16682=CARTESIAN_POINT('Ctrl Pts',(-0.11747670148927,0.0279758085988667,
0.0905412748670923));
#16683=CARTESIAN_POINT('Ctrl Pts',(-0.117715749944134,-0.000104199409386274,
0.0924367114736155));
#16684=CARTESIAN_POINT('Origin',(0.,0.,1.55));
#16685=CARTESIAN_POINT('',(-0.143211704627722,-5.70397197726547E-6,1.50700023576178));
#16686=CARTESIAN_POINT('Ctrl Pts',(-0.0334019664626774,0.112939183906323,
1.532225));
#16687=CARTESIAN_POINT('Ctrl Pts',(-0.0250606930336426,0.115799676338094,
1.53184761307169));
#16688=CARTESIAN_POINT('Ctrl Pts',(-0.0164287086124659,0.117635554524944,
1.53147359869818));
#16689=CARTESIAN_POINT('Ctrl Pts',(-0.00767226928320402,0.118510614220874,
1.53110056493424));
#16690=CARTESIAN_POINT('Ctrl Pts',(-0.0042150196872779,0.118856108509867,
1.53095328237096));
#16691=CARTESIAN_POINT('Ctrl Pts',(-0.000736351480830917,0.119051293525916,
1.53080607672538));
#16692=CARTESIAN_POINT('Ctrl Pts',(0.00274830211697625,0.119097943881266,
1.53065904037218));
#16693=CARTESIAN_POINT('Ctrl Pts',(0.00972321854123044,0.119191319684798,
1.53036473098213));
#16694=CARTESIAN_POINT('Ctrl Pts',(0.0166907125456733,0.118690968429664,
1.53007241075126));
#16695=CARTESIAN_POINT('Ctrl Pts',(0.0235721318645625,0.11762150546261,
1.52978094357425));
#16696=CARTESIAN_POINT('Ctrl Pts',(0.0273478463565568,0.117034709826966,
1.52962102062912));
#16697=CARTESIAN_POINT('Ctrl Pts',(0.0310977188904398,0.116276259986281,
1.52946135449799));
#16698=CARTESIAN_POINT('Ctrl Pts',(0.0348087249896146,0.115347945392283,
1.52930175751644));
#16699=CARTESIAN_POINT('Ctrl Pts',(0.0378768737129624,0.114580442682688,
1.52916980751093));
#16700=CARTESIAN_POINT('Ctrl Pts',(0.0409182562642153,0.113696477767379,
1.52903790896105));
#16701=CARTESIAN_POINT('Ctrl Pts',(0.0439120268522727,0.112701821307647,
1.52890655030309));
#16702=CARTESIAN_POINT('Ctrl Pts',(0.0504861734289241,0.110517613410832,
1.52861809430882));
#16703=CARTESIAN_POINT('Ctrl Pts',(0.0568477403450367,0.107796947733889,
1.528331525126));
#16704=CARTESIAN_POINT('Ctrl Pts',(0.0629211062797432,0.10455513280498,
1.52804576869741));
#16705=CARTESIAN_POINT('Ctrl Pts',(0.0667529140263229,0.102509807084265,
1.52786547926507));
#16706=CARTESIAN_POINT('Ctrl Pts',(0.0704699809867569,0.100256700264741,
1.52768551335768));
#16707=CARTESIAN_POINT('Ctrl Pts',(0.0740519796445933,0.0977963961590643,
1.52750560123222));
#16708=CARTESIAN_POINT('Ctrl Pts',(0.0761474027326905,0.0963571499395001,
1.52740035495562));
#16709=CARTESIAN_POINT('Ctrl Pts',(0.0781972522873126,0.0948464165467323,
1.52729509152825));
#16710=CARTESIAN_POINT('Ctrl Pts',(0.0801950758490376,0.0932655888959708,
1.52718986717129));
#16711=CARTESIAN_POINT('Ctrl Pts',(0.0872135629190184,0.0877120362002772,
1.52682020700562));
#16712=CARTESIAN_POINT('Ctrl Pts',(0.0935342345834078,0.0813437113039547,
1.52645409167081));
#16713=CARTESIAN_POINT('Ctrl Pts',(0.0991216768718319,0.0743433873765979,
1.52608928877518));
#16714=CARTESIAN_POINT('Ctrl Pts',(0.101857856375295,0.0709153174549959,
1.52591064420861));
#16715=CARTESIAN_POINT('Ctrl Pts',(0.104417791592617,0.0673349702414553,
1.52573231437502));
#16716=CARTESIAN_POINT('Ctrl Pts',(0.106794530290299,0.0636205708890664,
1.52555403711528));
#16717=CARTESIAN_POINT('Ctrl Pts',(0.108394385735532,0.0611202951812291,
1.52543403324399));
#16718=CARTESIAN_POINT('Ctrl Pts',(0.109912312880749,0.0585571637778213,
1.52531395827658));
#16719=CARTESIAN_POINT('Ctrl Pts',(0.111341951189028,0.0559432008961949,
1.5251940432238));
#16720=CARTESIAN_POINT('Ctrl Pts',(0.115894033640165,0.0476201345006791,
1.52481222412716));
#16721=CARTESIAN_POINT('Ctrl Pts',(0.119530893641226,0.0388304356906876,
1.52443409356659));
#16722=CARTESIAN_POINT('Ctrl Pts',(0.122195159250079,0.0297595052710396,
1.52405718851832));
#16723=CARTESIAN_POINT('Ctrl Pts',(0.123464283518865,0.0254385629829291,
1.52387764960816));
#16724=CARTESIAN_POINT('Ctrl Pts',(0.124512110981915,0.0210533134598664,
1.52369838877875));
#16725=CARTESIAN_POINT('Ctrl Pts',(0.12532867129748,0.0166220814218575,
1.52351913980531));
#16726=CARTESIAN_POINT('Ctrl Pts',(0.126067828800149,0.012610891624201,
1.52335688207487));
#16727=CARTESIAN_POINT('Ctrl Pts',(0.12661735951473,0.00855739899605222,
1.52319445303817));
#16728=CARTESIAN_POINT('Ctrl Pts',(0.126966826155483,0.00450415768051923,
1.52303280899981));
#16729=CARTESIAN_POINT('Ctrl Pts',(0.127602972227412,-0.00287409603749457,
1.52273856283131));
#16730=CARTESIAN_POINT('Ctrl Pts',(0.12758177643555,-0.010267620141741,
1.52244625042084));
#16731=CARTESIAN_POINT('Ctrl Pts',(0.126865581413421,-0.0175939782534482,
1.52215473434257));
#16732=CARTESIAN_POINT('Ctrl Pts',(0.126426462283551,-0.0220859726121444,
1.52197599770985));
#16733=CARTESIAN_POINT('Ctrl Pts',(0.12572570473317,-0.0265528301690258,
1.52179756043894));
#16734=CARTESIAN_POINT('Ctrl Pts',(0.124776542651163,-0.0309793260681717,
1.52161916036391));
#16735=CARTESIAN_POINT('Ctrl Pts',(0.124151644840291,-0.0338935887106027,
1.52150170748789));
#16736=CARTESIAN_POINT('Ctrl Pts',(0.123418330834614,-0.0367926408403149,
1.52138417707714));
#16737=CARTESIAN_POINT('Ctrl Pts',(0.122581975874549,-0.0396644408336013,
1.52126680258073));
#16738=CARTESIAN_POINT('Ctrl Pts',(0.120074191833131,-0.0482754427851461,
1.52091485884509));
#16739=CARTESIAN_POINT('Ctrl Pts',(0.116656903439717,-0.0566007293654626,
1.52056600333313));
#16740=CARTESIAN_POINT('Ctrl Pts',(0.112443760417108,-0.0645262187619275,
1.52021830866717));
#16741=CARTESIAN_POINT('Ctrl Pts',(0.109356904590302,-0.0703330102694749,
1.51996356219884));
#16742=CARTESIAN_POINT('Ctrl Pts',(0.105841781173658,-0.0759253337267248,
1.51970943888381));
#16743=CARTESIAN_POINT('Ctrl Pts',(0.101930367117466,-0.0812537151913617,
1.51945518067311));
#16744=CARTESIAN_POINT('Ctrl Pts',(0.100130771446666,-0.0837052409256295,
1.51933819945644));
#16745=CARTESIAN_POINT('Ctrl Pts',(0.0982476276828181,-0.0860996963839449,
1.51922123442864));
#16746=CARTESIAN_POINT('Ctrl Pts',(0.0962924325256194,-0.0884227179472683,
1.51910469697823));
#16747=CARTESIAN_POINT('Ctrl Pts',(0.0906946176521128,-0.0950736369671782,
1.51877104482549));
#16748=CARTESIAN_POINT('Ctrl Pts',(0.0844921899154374,-0.101162815315101,
1.51843983772287));
#16749=CARTESIAN_POINT('Ctrl Pts',(0.0777644521522082,-0.106582693579069,
1.51810941878));
#16750=CARTESIAN_POINT('Ctrl Pts',(0.0731067700043679,-0.110334931124879,
1.5178806663426));
#16751=CARTESIAN_POINT('Ctrl Pts',(0.0681966627772886,-0.113766151308436,
1.51765229166508));
#16752=CARTESIAN_POINT('Ctrl Pts',(0.0630541948599911,-0.116833686038022,
1.5174237449583));
#16753=CARTESIAN_POINT('Ctrl Pts',(0.0607686815400033,-0.118197018118406,
1.51732216988754));
#16754=CARTESIAN_POINT('Ctrl Pts',(0.0584414404741937,-0.119485783651375,
1.51722075040181));
#16755=CARTESIAN_POINT('Ctrl Pts',(0.0560784264268894,-0.12069488199044,
1.51711960151386));
#16756=CARTESIAN_POINT('Ctrl Pts',(0.0475595529450054,-0.125053787850271,
1.51675495087613));
#16757=CARTESIAN_POINT('Ctrl Pts',(0.038563113830939,-0.128389854466075,
1.51639315730301));
#16758=CARTESIAN_POINT('Ctrl Pts',(0.0292711048986314,-0.130741856378471,
1.51603205677802));
#16759=CARTESIAN_POINT('Ctrl Pts',(0.0254547302664753,-0.13170786066222,
1.51588374709674));
#16760=CARTESIAN_POINT('Ctrl Pts',(0.0215881861914954,-0.132507324978224,
1.51573555432397));
#16761=CARTESIAN_POINT('Ctrl Pts',(0.0176832233642019,-0.13314066674995,
1.51558732853105));
#16762=CARTESIAN_POINT('Ctrl Pts',(0.0144414794405867,-0.133666441752394,
1.51546427740745));
#16763=CARTESIAN_POINT('Ctrl Pts',(0.0111713231872828,-0.134077605234841,
1.5153411329761));
#16764=CARTESIAN_POINT('Ctrl Pts',(0.00789687394913892,-0.134372952697723,
1.51521845803943));
#16765=CARTESIAN_POINT('Ctrl Pts',(-0.00208492598009478,-0.135273287095873,
1.51484449692866));
#16766=CARTESIAN_POINT('Ctrl Pts',(-0.0121386692885745,-0.135107999768821,
1.51447364169918));
#16767=CARTESIAN_POINT('Ctrl Pts',(-0.0220717676774029,-0.133899092645375,
1.51410356562093));
#16768=CARTESIAN_POINT('Ctrl Pts',(-0.0271373055616968,-0.133282591671289,
1.51391483957382));
#16769=CARTESIAN_POINT('Ctrl Pts',(-0.0321716696217597,-0.132393849601707,
1.51372631615657));
#16770=CARTESIAN_POINT('Ctrl Pts',(-0.0371491047637803,-0.131230566976147,
1.51353768678866));
#16771=CARTESIAN_POINT('Ctrl Pts',(-0.0401763453142056,-0.130523066780721,
1.51342296375255));
#16772=CARTESIAN_POINT('Ctrl Pts',(-0.0431793745847511,-0.129714439573166,
1.51330831773957));
#16773=CARTESIAN_POINT('Ctrl Pts',(-0.0461427198170546,-0.128807808452418,
1.51319405707679));
#16774=CARTESIAN_POINT('Ctrl Pts',(-0.0557912886485991,-0.125855842991896,
1.51282202756853));
#16775=CARTESIAN_POINT('Ctrl Pts',(-0.0650506639775802,-0.121862017750276,
1.51245293010828));
#16776=CARTESIAN_POINT('Ctrl Pts',(-0.0737251756215706,-0.116823260910032,
1.51208446868514));
#16777=CARTESIAN_POINT('Ctrl Pts',(-0.0774533877539874,-0.114657657224767,
1.51192610791459));
#16778=CARTESIAN_POINT('Ctrl Pts',(-0.0810733781510443,-0.112298364258586,
1.51176786463208));
#16779=CARTESIAN_POINT('Ctrl Pts',(-0.0845783705992567,-0.109758519633299,
1.51160955655689));
#16780=CARTESIAN_POINT('Ctrl Pts',(-0.0871260289206952,-0.107912394030924,
1.51149448786814));
#16781=CARTESIAN_POINT('Ctrl Pts',(-0.0896122610481647,-0.105970921032248,
1.51137940572563));
#16782=CARTESIAN_POINT('Ctrl Pts',(-0.0920243025666997,-0.10394826075131,
1.51126473391974));
#16783=CARTESIAN_POINT('Ctrl Pts',(-0.0995315444015674,-0.0976529296958118,
1.51090782920982));
#16784=CARTESIAN_POINT('Ctrl Pts',(-0.106349817996106,-0.090554906599088,
1.51055366538392));
#16785=CARTESIAN_POINT('Ctrl Pts',(-0.112409916721278,-0.0828189535999138,
1.51020021897155));
#16786=CARTESIAN_POINT('Ctrl Pts',(-0.11567060314877,-0.0786565598680515,
1.51001004419521));
#16787=CARTESIAN_POINT('Ctrl Pts',(-0.118711357121208,-0.0743087544864998,
1.50982007711492));
#16788=CARTESIAN_POINT('Ctrl Pts',(-0.121517490738653,-0.0697974244982526,
1.50963000253165));
#16789=CARTESIAN_POINT('Ctrl Pts',(-0.123184827969132,-0.0671169005197731,
1.50951706477726));
#16790=CARTESIAN_POINT('Ctrl Pts',(-0.124768226583796,-0.064379797453554,
1.50940414472167));
#16791=CARTESIAN_POINT('Ctrl Pts',(-0.12625918933752,-0.0616017405091787,
1.50929161182319));
#16792=CARTESIAN_POINT('Ctrl Pts',(-0.131254477666307,-0.0522942005345653,
1.50891458411209));
#16793=CARTESIAN_POINT('Ctrl Pts',(-0.135235816373665,-0.0424980109473837,
1.50854057440173));
#16794=CARTESIAN_POINT('Ctrl Pts',(-0.138100316247284,-0.0323932585971084,
1.50816719719795));
#16795=CARTESIAN_POINT('Ctrl Pts',(-0.139428601593765,-0.027707625827389,
1.5079940600046));
#16796=CARTESIAN_POINT('Ctrl Pts',(-0.140516076092011,-0.0229552175461711,
1.50782105881478));
#16797=CARTESIAN_POINT('Ctrl Pts',(-0.14134846970832,-0.01815262603916,
1.50764795577689));
#16798=CARTESIAN_POINT('Ctrl Pts',(-0.141840021659925,-0.0153165600461233,
1.5075457335416));
#16799=CARTESIAN_POINT('Ctrl Pts',(-0.142241997144177,-0.0124651428186592,
1.50744355431084));
#16800=CARTESIAN_POINT('Ctrl Pts',(-0.142550993842162,-0.00961078035088443,
1.50734168592779));
#16801=CARTESIAN_POINT('Ctrl Pts',(-0.142847161918882,-0.00687492249914849,
1.50724404681617));
#16802=CARTESIAN_POINT('Ctrl Pts',(-0.143058332724879,-0.00413406598225375,
1.5071466105924));
#16803=CARTESIAN_POINT('Ctrl Pts',(-0.143182669649515,-0.00139134585336764,
1.50704933585643));
#16804=CARTESIAN_POINT('Ctrl Pts',(-0.143203595382121,-0.00092974984559876,
1.50703296465278));
#16805=CARTESIAN_POINT('Ctrl Pts',(-0.143222061023464,-0.000468100854706259,
1.50701659802318));
#16806=CARTESIAN_POINT('Ctrl Pts',(-0.143238079070951,-6.41379011939899E-6,
1.50700023577028));
#16807=CARTESIAN_POINT('',(-0.00156744678985144,0.146109855568756,1.50365));
#16808=CARTESIAN_POINT('Ctrl Pts',(-0.00156962371672063,0.146072546381438,
1.50365));
#16809=CARTESIAN_POINT('Ctrl Pts',(-0.011711474284147,0.144648739717271,
1.50495065132295));
#16810=CARTESIAN_POINT('Ctrl Pts',(-0.0216501921041044,0.142222471223284,
1.50626105010813));
#16811=CARTESIAN_POINT('Ctrl Pts',(-0.0312062965385204,0.138804788898175,
1.50759029209282));
#16812=CARTESIAN_POINT('Ctrl Pts',(-0.0379863325344082,0.136379950477271,
1.50853338648503));
#16813=CARTESIAN_POINT('Ctrl Pts',(-0.0445735484268955,0.133455002060128,
1.5094859663039));
#16814=CARTESIAN_POINT('Ctrl Pts',(-0.0508923708069948,0.130021662144985,
1.51045128011208));
#16815=CARTESIAN_POINT('Ctrl Pts',(-0.053607485163773,0.128546401418451,
1.51086606268101));
#16816=CARTESIAN_POINT('Ctrl Pts',(-0.0562647183424556,0.126981576978965,
1.51128195276517));
#16817=CARTESIAN_POINT('Ctrl Pts',(-0.0588579379029418,0.125328026221608,
1.51169910067666));
#16818=CARTESIAN_POINT('Ctrl Pts',(-0.0624505046767585,0.123037247762191,
1.51227700458785));
#16819=CARTESIAN_POINT('Ctrl Pts',(-0.0659209207101175,0.120575889029892,
1.51285741907924));
#16820=CARTESIAN_POINT('Ctrl Pts',(-0.0692542752175272,0.117943487410649,
1.51344114883776));
#16821=CARTESIAN_POINT('Ctrl Pts',(-0.0735613784355843,0.114542101371374,
1.51419539934302));
#16822=CARTESIAN_POINT('Ctrl Pts',(-0.0776398170223455,0.110855132244726,
1.51495518495604));
#16823=CARTESIAN_POINT('Ctrl Pts',(-0.0814741368103916,0.106911749311875,
1.51572224163114));
#16824=CARTESIAN_POINT('Ctrl Pts',(-0.0845038784997064,0.103795829845314,
1.51632834224744));
#16825=CARTESIAN_POINT('Ctrl Pts',(-0.087381117690253,0.10051973853988,
1.51693898261853));
#16826=CARTESIAN_POINT('Ctrl Pts',(-0.0900959757046659,0.0970973798321736,
1.51755501917095));
#16827=CARTESIAN_POINT('Ctrl Pts',(-0.0920052356275281,0.0946905606587243,
1.51798825505079));
#16828=CARTESIAN_POINT('Ctrl Pts',(-0.093830595110286,0.092215607777745,
1.51842338946406));
#16829=CARTESIAN_POINT('Ctrl Pts',(-0.0955653742165971,0.0896840982544811,
1.51885969689116));
#16830=CARTESIAN_POINT('Ctrl Pts',(-0.0997851775729162,0.0835262696618028,
1.51992100293214));
#16831=CARTESIAN_POINT('Ctrl Pts',(-0.103479134251024,0.0770231540939269,
1.52099120961793));
#16832=CARTESIAN_POINT('Ctrl Pts',(-0.106606394578922,0.0702509006766953,
1.52207541818308));
#16833=CARTESIAN_POINT('Ctrl Pts',(-0.108879606303698,0.0653281362576702,
1.52286353153598));
#16834=CARTESIAN_POINT('Ctrl Pts',(-0.110852991156964,0.0602629640702717,
1.52365904329275));
#16835=CARTESIAN_POINT('Ctrl Pts',(-0.112503888351057,0.0550849881514033,
1.524463912762));
#16836=CARTESIAN_POINT('Ctrl Pts',(-0.113450017754745,0.0521174894567802,
1.52492518356294));
#16837=CARTESIAN_POINT('Ctrl Pts',(-0.114289979676541,0.0491121240008169,
1.52538965304266));
#16838=CARTESIAN_POINT('Ctrl Pts',(-0.115015874151616,0.0460903162170444,
1.52585530945224));
#16839=CARTESIAN_POINT('Ctrl Pts',(-0.117053612444637,0.0376074669234184,
1.52716250482259));
#16840=CARTESIAN_POINT('Ctrl Pts',(-0.118206139871793,0.0289652499882669,
1.52848357355921));
#16841=CARTESIAN_POINT('Ctrl Pts',(-0.11838625730212,0.0202925750432425,
1.52982832573377));
#16842=CARTESIAN_POINT('Ctrl Pts',(-0.118492077855379,0.015197303257165,
1.53061837930521));
#16843=CARTESIAN_POINT('Ctrl Pts',(-0.118261361656021,0.0100916471271278,
1.53141660760476));
#16844=CARTESIAN_POINT('Ctrl Pts',(-0.11766859746431,0.00500517689818842,
1.532225));
#16845=CARTESIAN_POINT('',(-0.115079981391543,0.0902137050004572,1.50365));
#16846=CARTESIAN_POINT('Origin',(0.,0.,1.50365));
#16847=CARTESIAN_POINT('Ctrl Pts',(-0.143238079070951,-6.41379011939899E-6,
1.50700023577028));
#16848=CARTESIAN_POINT('Ctrl Pts',(-0.143514357617001,0.00795674345750163,
1.50671802038504));
#16849=CARTESIAN_POINT('Ctrl Pts',(-0.14306421847979,0.0159310909218757,
1.50643710681857));
#16850=CARTESIAN_POINT('Ctrl Pts',(-0.141940608246003,0.023841490005315,
1.50615648267927));
#16851=CARTESIAN_POINT('Ctrl Pts',(-0.141317731836386,0.0282266413964,1.50600091791928));
#16852=CARTESIAN_POINT('Ctrl Pts',(-0.14048752132733,0.0325921818867556,
1.50584544210227));
#16853=CARTESIAN_POINT('Ctrl Pts',(-0.139456452513291,0.0369250818702156,
1.5056898827608));
#16854=CARTESIAN_POINT('Ctrl Pts',(-0.138790989895207,0.0397215809279161,
1.50558948313156));
#16855=CARTESIAN_POINT('Ctrl Pts',(-0.138042009924554,0.0425029011667524,
1.50548910366784));
#16856=CARTESIAN_POINT('Ctrl Pts',(-0.137214434473447,0.0452564915355094,
1.50538902890071));
#16857=CARTESIAN_POINT('Ctrl Pts',(-0.134176751889031,0.0553637675507716,
1.50502169637912));
#16858=CARTESIAN_POINT('Ctrl Pts',(-0.130076454936343,0.0651325632434767,
1.50465723703036));
#16859=CARTESIAN_POINT('Ctrl Pts',(-0.125018127980614,0.0743940890034878,
1.50429344851366));
#16860=CARTESIAN_POINT('Ctrl Pts',(-0.122034683484208,0.0798566160996726,
1.50407888293545));
#16861=CARTESIAN_POINT('Ctrl Pts',(-0.118716925567465,0.0851425936725427,
1.50386455072235));
#16862=CARTESIAN_POINT('Ctrl Pts',(-0.115078604842436,0.0902138214954005,
1.50365));
#16863=CARTESIAN_POINT('',(-0.05,-6.12323399573677E-18,1.6));
#16864=CARTESIAN_POINT('',(-0.1,-1.22464679914735E-17,1.55));
#16865=CARTESIAN_POINT('Origin',(0.,0.,1.6));
#16866=CARTESIAN_POINT('Ctrl Pts',(0.0850780204044575,-0.11908002747757,
-0.0164977839420936));
#16867=CARTESIAN_POINT('Ctrl Pts',(0.124677800165771,-0.0907875342533835,
-0.0138514540629917));
#16868=CARTESIAN_POINT('Ctrl Pts',(0.172751483861701,0.00791416360185712,
-0.00855879430478784));
#16869=CARTESIAN_POINT('Ctrl Pts',(0.0868617128612901,0.149726167188418,
-0.000619804667482127));
#16870=CARTESIAN_POINT('Ctrl Pts',(-0.078614020905812,0.154028602276276,
0.00731918496982359));
#16871=CARTESIAN_POINT('Ctrl Pts',(-0.172087192378165,0.0175525219725009,
0.0152581746071293));
#16872=CARTESIAN_POINT('Ctrl Pts',(-0.108045720411827,-0.135108484733225,
0.0231971642444351));
#16873=CARTESIAN_POINT('Ctrl Pts',(0.0549144151285058,-0.164025561655164,
0.0311361538817407));
#16874=CARTESIAN_POINT('Ctrl Pts',(0.167598788591005,-0.0428207868793744,
0.0390751435190465));
#16875=CARTESIAN_POINT('Ctrl Pts',(0.126860790413016,0.117600499296196,
0.0470141331563521));
#16876=CARTESIAN_POINT('Ctrl Pts',(-0.0300110592737492,0.170357625684536,
0.054953122793658));
#16877=CARTESIAN_POINT('Ctrl Pts',(-0.159409054995301,0.0671687418111174,
0.0628921124309635));
#16878=CARTESIAN_POINT('Ctrl Pts',(-0.142879399887002,-0.0975110083167992,
0.0708311020682695));
#16879=CARTESIAN_POINT('Ctrl Pts',(0.00444677171871267,-0.172924803493063,
0.078770091705575));
#16880=CARTESIAN_POINT('Ctrl Pts',(0.147702113712341,-0.0900384822365835,
0.0867090813428809));
#16881=CARTESIAN_POINT('Ctrl Pts',(0.155746353789385,0.0752722621313087,
0.0946480709801864));
#16882=CARTESIAN_POINT('Ctrl Pts',(0.021215449100004,0.17167621786987,0.102587060617492));
#16883=CARTESIAN_POINT('Ctrl Pts',(-0.132736728465598,0.110922462699857,
0.110526050254798));
#16884=CARTESIAN_POINT('Ctrl Pts',(-0.165177537004225,-0.0513732581591355,
0.118465039892104));
#16885=CARTESIAN_POINT('Ctrl Pts',(-0.0464096261145344,-0.166640254043574,
0.126404029529409));
#16886=CARTESIAN_POINT('Ctrl Pts',(0.114843114370719,-0.129359532685675,
0.134343019166715));
#16887=CARTESIAN_POINT('Ctrl Pts',(0.170964855654229,0.0263409830179588,
0.142282008804021));
#16888=CARTESIAN_POINT('Ctrl Pts',(0.0705799878925336,0.157928129946847,
0.150220998441327));
#16889=CARTESIAN_POINT('Ctrl Pts',(-0.0944160212638482,0.144942899583874,
0.158159988078632));
#16890=CARTESIAN_POINT('Ctrl Pts',(-0.172980633894512,-0.000727622896455919,
0.166098977715938));
#16891=CARTESIAN_POINT('Ctrl Pts',(-0.0931933312323777,-0.145732055885043,
0.174037967353244));
#16892=CARTESIAN_POINT('Ctrl Pts',(0.0719060791645076,-0.157328779695546,
0.181976956990549));
#16893=CARTESIAN_POINT('Ctrl Pts',(0.171180402159323,-0.0249017879745179,
0.189915946627855));
#16894=CARTESIAN_POINT('Ctrl Pts',(0.113750798721884,0.13032108391891,0.197854936265161));
#16895=CARTESIAN_POINT('Ctrl Pts',(-0.0478098650864174,0.16624393501773,
0.205793925902467));
#16896=CARTESIAN_POINT('Ctrl Pts',(-0.16560387403618,0.0499818570245514,
0.213732915539772));
#16897=CARTESIAN_POINT('Ctrl Pts',(-0.131798885878402,-0.112035185581475,
0.221671905177078));
#16898=CARTESIAN_POINT('Ctrl Pts',(0.0226589495323734,-0.171491694067101,
0.229610894814384));
#16899=CARTESIAN_POINT('Ctrl Pts',(0.156374069566079,-0.073959309724122,
0.237549884451689));
#16900=CARTESIAN_POINT('Ctrl Pts',(0.146939445926624,0.0912777539068999,
0.245488874088995));
#16901=CARTESIAN_POINT('Ctrl Pts',(0.00299182995941577,0.172956289510158,
0.253427863726301));
#16902=CARTESIAN_POINT('Ctrl Pts',(-0.143694601292225,0.0963051955349955,
0.261366853363607));
#16903=CARTESIAN_POINT('Ctrl Pts',(-0.15883847309497,-0.0685067047260848,
0.269305843000912));
#16904=CARTESIAN_POINT('Ctrl Pts',(-0.0285766086907934,-0.170605411881679,
0.277244832638218));
#16905=CARTESIAN_POINT('Ctrl Pts',(0.12784518248692,-0.116526556812001,
0.285183822275524));
#16906=CARTESIAN_POINT('Ctrl Pts',(0.167233470900423,0.0442243749325307,
0.293122811912829));
#16907=CARTESIAN_POINT('Ctrl Pts',(0.0535309779628647,0.164490922320707,
0.301061801550136));
#16908=CARTESIAN_POINT('Ctrl Pts',(-0.109175456582181,0.134177303623408,
0.309000791187441));
#16909=CARTESIAN_POINT('Ctrl Pts',(-0.171939242908932,-0.0189664407699395,
0.316939780824747));
#16910=CARTESIAN_POINT('Ctrl Pts',(-0.0773044361184472,-0.154747708493488,
0.324878770462053));
#16911=CARTESIAN_POINT('Ctrl Pts',(0.0880972839194656,-0.148868054644337,
0.332817760099358));
#16912=CARTESIAN_POINT('Ctrl Pts',(0.172851978230285,-0.00670989936239309,
0.340756749736664));
#16913=CARTESIAN_POINT('Ctrl Pts',(0.0993725327910066,0.141590708926387,
0.34869573937397));
#16914=CARTESIAN_POINT('Ctrl Pts',(-0.0650756559739905,0.160274727038081,
0.356634729011275));
#16915=CARTESIAN_POINT('Ctrl Pts',(-0.169951541620772,0.0322382168908211,
0.364573718648582));
#16916=CARTESIAN_POINT('Ctrl Pts',(-0.119248438453561,-0.125310171390688,
0.372512708285886));
#16917=CARTESIAN_POINT('Ctrl Pts',(0.0406184374886585,-0.168145685830938,
0.380451697923193));
#16918=CARTESIAN_POINT('Ctrl Pts',(0.163301917673335,-0.0570553486694088,
0.388390687560498));
#16919=CARTESIAN_POINT('Ctrl Pts',(0.136493684039406,0.106265249940549,
0.396329677197804));
#16920=CARTESIAN_POINT('Ctrl Pts',(-0.0152651628095069,0.172307295063139,
0.404268666835109));
#16921=CARTESIAN_POINT('Ctrl Pts',(-0.153049799296248,0.0806138205455782,
0.412207656472416));
#16922=CARTESIAN_POINT('Ctrl Pts',(-0.150727833715048,-0.0848760818555219,
0.420146646109721));
#16923=CARTESIAN_POINT('Ctrl Pts',(-0.0104248664208018,-0.172667748255674,
0.428085635747027));
#16924=CARTESIAN_POINT('Ctrl Pts',(0.139421351618932,-0.10239392482138,
0.436024625384332));
#16925=CARTESIAN_POINT('Ctrl Pts',(0.16163687742079,0.0616145192729195,
0.443963615021638));
#16926=CARTESIAN_POINT('Ctrl Pts',(0.0358849196425865,0.169219093691645,
0.451902604658944));
#16927=CARTESIAN_POINT('Ctrl Pts',(-0.122717222714247,0.121915185177559,
0.45984159429625));
#16928=CARTESIAN_POINT('Ctrl Pts',(-0.168980158036723,-0.0369937199732681,
0.467780583933555));
#16929=CARTESIAN_POINT('Ctrl Pts',(-0.0605533396431397,-0.162037409833775,
0.475719573570861));
#16930=CARTESIAN_POINT('Ctrl Pts',(0.103305911202344,-0.138746956140414,
0.483658563208167));
#16931=CARTESIAN_POINT('Ctrl Pts',(0.172595680358559,0.0115568269495825,
0.491597552845473));
#16932=CARTESIAN_POINT('Ctrl Pts',(0.0838859329010004,0.151281127008313,
0.499536542482778));
#16933=CARTESIAN_POINT('Ctrl Pts',(-0.0816156370489812,0.152517923263679,
0.507475532120084));
#16934=CARTESIAN_POINT('Ctrl Pts',(-0.172403684765527,0.0141350135070757,
0.51541452175739));
#16935=CARTESIAN_POINT('Ctrl Pts',(-0.105367974675403,-0.137187532379513,
0.523353511394695));
#16936=CARTESIAN_POINT('Ctrl Pts',(0.0581248948911363,-0.162924294448283,
0.531292501032001));
#16937=CARTESIAN_POINT('Ctrl Pts',(0.168408406744046,-0.039515030880773,
0.539231490669306));
#16938=CARTESIAN_POINT('Ctrl Pts',(0.124525564004667,0.120067535316156,
0.547170480306613));
#16939=CARTESIAN_POINT('Ctrl Pts',(-0.0333518982867267,0.169736501696743,
0.555109469943918));
#16940=CARTESIAN_POINT('Ctrl Pts',(-0.160697983451488,0.0640233335761385,
0.563048459581225));
#16941=CARTESIAN_POINT('Ctrl Pts',(-0.14093607811848,-0.100298808627811,
0.570987449218529));
#16942=CARTESIAN_POINT('Ctrl Pts',(0.00784314775175556,-0.172804265459278,
0.578926438855836));
#16943=CARTESIAN_POINT('Ctrl Pts',(0.149442509381278,-0.0871192603125336,
0.586865428493141));
#16944=CARTESIAN_POINT('Ctrl Pts',(0.154237495636292,0.0783174569774929,
0.594804418130446));
#16945=CARTESIAN_POINT('Ctrl Pts',(0.0178386252221998,0.172059909850489,
0.602743407767753));
#16946=CARTESIAN_POINT('Ctrl Pts',(-0.134890284021987,0.108293307291099,
0.610682397405058));
#16947=CARTESIAN_POINT('Ctrl Pts',(-0.164136382878957,-0.0546083962682395,
0.618621387042364));
#16948=CARTESIAN_POINT('Ctrl Pts',(-0.0431268722112106,-0.167519855601819,
0.62656037667967));
#16949=CARTESIAN_POINT('Ctrl Pts',(0.117362334288317,-0.127078368017432,
0.634499366316975));
#16950=CARTESIAN_POINT('Ctrl Pts',(0.170414367112955,0.0296946562375699,
0.642438355954282));
#16951=CARTESIAN_POINT('Ctrl Pts',(0.0674637261050104,0.159284257814778,
0.650377345591586));
#16952=CARTESIAN_POINT('Ctrl Pts',(-0.0972453325609638,0.143060037825677,
0.658316335228894));
#16953=CARTESIAN_POINT('Ctrl Pts',(-0.172932953925271,-0.00412584224812367,
0.666255324866198));
#16954=CARTESIAN_POINT('Ctrl Pts',(-0.0903123078403481,-0.147534796506203,
0.674194314503505));
#16955=CARTESIAN_POINT('Ctrl Pts',(0.0749830665657334,-0.155885755782802,
0.68213330414081));
#16956=CARTESIAN_POINT('Ctrl Pts',(0.17163658245605,-0.021533989188811,
0.690072293778116));
#16957=CARTESIAN_POINT('Ctrl Pts',(0.11116857013107,0.132530668686874,0.698011283415421));
#16958=CARTESIAN_POINT('Ctrl Pts',(-0.0510666492692211,0.165272582299639,
0.705950273052727));
#16959=CARTESIAN_POINT('Ctrl Pts',(-0.166553851089581,0.0467187736868841,
0.713889262690032));
#16960=CARTESIAN_POINT('Ctrl Pts',(-0.129572416918314,-0.114602870389546,
0.721828252327339));
#16961=CARTESIAN_POINT('Ctrl Pts',(0.0260236847639906,-0.171013440871999,
0.729767241964644));
#16962=CARTESIAN_POINT('Ctrl Pts',(0.157796886564457,-0.0708729265526718,
0.73770623160195));
#16963=CARTESIAN_POINT('Ctrl Pts',(0.145117853242075,0.0941468947867542,
0.745645221239255));
#16964=CARTESIAN_POINT('Ctrl Pts',(-0.000406629147419015,0.172981686256994,
0.753584210876562));
#16965=CARTESIAN_POINT('Ctrl Pts',(-0.145558870420566,0.0934635991681543,
0.761523200513868));
#16966=CARTESIAN_POINT('Ctrl Pts',(-0.157461941624574,-0.0716140074803496,
0.769462190151172));
#16967=CARTESIAN_POINT('Ctrl Pts',(-0.0252193968429213,-0.17113389830906,
0.777401179788479));
#16968=CARTESIAN_POINT('Ctrl Pts',(0.130109777350283,-0.113992433807847,
0.785340169425784));
#16969=CARTESIAN_POINT('Ctrl Pts',(0.166332367384696,0.0475012914327479,
0.793279159063091));
#16970=CARTESIAN_POINT('Ctrl Pts',(0.0502890745800368,0.165510839842773,
0.801218148700395));
#16971=CARTESIAN_POINT('Ctrl Pts',(-0.111790419467279,0.132006557575396,
0.809157138337702));
#16972=CARTESIAN_POINT('Ctrl Pts',(-0.171533445990104,-0.0223406811520247,
0.817096127975007));
#16973=CARTESIAN_POINT('Ctrl Pts',(-0.0742493586638003,-0.156236557391639,
0.825035117612313));
#16974=CARTESIAN_POINT('Ctrl Pts',(0.0910049278783345,-0.147108572929777,
0.832974107249618));
#16975=CARTESIAN_POINT('Ctrl Pts',(0.172950439922886,-0.00331277195964383,
0.840913096886925));
#16976=CARTESIAN_POINT('Ctrl Pts',(0.0965716772857839,0.143515644700454,
0.848852086524229));
#16977=CARTESIAN_POINT('Ctrl Pts',(-0.0682118374171683,0.158965324406771,
0.856791076161536));
#16978=CARTESIAN_POINT('Ctrl Pts',(-0.170552089827228,0.0288931442238776,
0.864730065798841));
#16979=CARTESIAN_POINT('Ctrl Pts',(-0.116763592698541,-0.127628729319482,
0.872669055436147));
#16980=CARTESIAN_POINT('Ctrl Pts',(0.0439139712140358,-0.167315248138923,
0.880608045073453));
#16981=CARTESIAN_POINT('Ctrl Pts',(0.164391304101163,-0.0538361241500125,
0.888547034710759));
#16982=CARTESIAN_POINT('Ctrl Pts',(0.134379664555536,0.108926281867684,
0.896486024348063));
#16983=CARTESIAN_POINT('Ctrl Pts',(-0.018647348250808,0.17197414204115,
0.904425013985371));
#16984=CARTESIAN_POINT('Ctrl Pts',(-0.154603991719776,0.0775914613336281,
0.912364003622676));
#16985=CARTESIAN_POINT('Ctrl Pts',(-0.149031276472826,-0.0878208845346985,
0.920302993259982));
#16986=CARTESIAN_POINT('Ctrl Pts',(-0.00703064139541984,-0.172839229369798,
0.928241982897287));
#16987=CARTESIAN_POINT('Ctrl Pts',(0.141406064038169,-0.099635105162837,
0.936180972534593));
#16988=CARTESIAN_POINT('Ctrl Pts',(0.160395209035295,0.064778129380991,
0.944119962171899));
#16989=CARTESIAN_POINT('Ctrl Pts',(0.03255353276219,0.169891426011666,0.952058951809204));
#16990=CARTESIAN_POINT('Ctrl Pts',(-0.125088671715395,0.119480765548496,
0.959997941446511));
#16991=CARTESIAN_POINT('Ctrl Pts',(-0.168220770124088,-0.040306347222682,
0.967936931083815));
#16992=CARTESIAN_POINT('Ctrl Pts',(-0.0573582824064844,-0.163195761485875,
0.975875920721122));
#16993=CARTESIAN_POINT('Ctrl Pts',(0.106011781834435,-0.136690640644722,
0.983814910358427));
#16994=CARTESIAN_POINT('Ctrl Pts',(0.17233532526783,0.014945393685262,0.991753899995733));
#16995=CARTESIAN_POINT('Ctrl Pts',(0.0808976893297158,0.152899944371113,
0.999692889633039));
#16996=CARTESIAN_POINT('Ctrl Pts',(-0.0845962369090198,0.150885074902754,
1.00763187927034));
#16997=CARTESIAN_POINT('Ctrl Pts',(-0.172648106016301,0.0107452601904448,
1.01557086890765));
#16998=CARTESIAN_POINT('Ctrl Pts',(-0.102652466413112,-0.13923110380544,
1.02350985854496));
#16999=CARTESIAN_POINT('Ctrl Pts',(0.0613144709582997,-0.161750934398167,
1.03144884818226));
#17000=CARTESIAN_POINT('Ctrl Pts',(0.169152212322519,-0.0361988700648799,
1.03938783781957));
#17001=CARTESIAN_POINT('Ctrl Pts',(0.122142696063681,0.12249077894222,1.04732682745687));
#17002=CARTESIAN_POINT('Ctrl Pts',(-0.0366800874558037,0.169048514669047,
1.05526581709418));
#17003=CARTESIAN_POINT('Ctrl Pts',(-0.161924764760067,0.0608539208677085,
1.06320480673148));
#17004=CARTESIAN_POINT('Ctrl Pts',(-0.138938417355371,-0.103048266896446,
1.07114379636879));
#17005=CARTESIAN_POINT('Ctrl Pts',(0.011236529066559,-0.172616828675865,
1.0790827860061));
#17006=CARTESIAN_POINT('Ctrl Pts',(0.151125203217684,-0.0841665140064042,
1.0870217756434));
#17007=CARTESIAN_POINT('Ctrl Pts',(0.152669111109608,0.0813324759279986,
1.09496076528071));
#17008=CARTESIAN_POINT('Ctrl Pts',(0.0144549108781955,0.172377158228925,
1.10289975491801));
#17009=CARTESIAN_POINT('Ctrl Pts',(-0.136991769602464,0.10562236594946,
1.11083874455532));
#17010=CARTESIAN_POINT('Ctrl Pts',(-0.163031873671196,-0.0578224635832477,
1.11877773419263));
#17011=CARTESIAN_POINT('Ctrl Pts',(-0.0398274706979539,-0.168334790537727,
1.12671672382993));
#17012=CARTESIAN_POINT('Ctrl Pts',(0.119836252144435,-0.124748153491552,
1.13465571346724));
#17013=CARTESIAN_POINT('Ctrl Pts',(0.169798099063322,0.0330368685268242,
1.14259470310454));
#17014=CARTESIAN_POINT('Ctrl Pts',(0.0643214233134591,0.160578901573361,
1.15053369274185));
#17015=CARTESIAN_POINT('Ctrl Pts',(-0.100037107244844,0.141121955420339,
1.15847268237915));
#17016=CARTESIAN_POINT('Ctrl Pts',(-0.172818522111203,-0.00752246920075927,
1.16641167201646));
#17017=CARTESIAN_POINT('Ctrl Pts',(-0.0873964240115842,-0.149280588817046,
1.17435066165376));
#17018=CARTESIAN_POINT('Ctrl Pts',(0.0780311106025284,-0.154382560238235,
1.18228965129107));
#17019=CARTESIAN_POINT('Ctrl Pts',(0.172026511281289,-0.01815787828917,
1.19022864092837));
#17020=CARTESIAN_POINT('Ctrl Pts',(0.10854343062882,0.134689096792963,1.19816763056568));
#17021=CARTESIAN_POINT('Ctrl Pts',(-0.0543037217972188,0.164237434607784,
1.20610662020299));
#17022=CARTESIAN_POINT('Ctrl Pts',(-0.167439538594998,0.0434376569656869,
1.21404560984029));
#17023=CARTESIAN_POINT('Ctrl Pts',(-0.127295933190098,-0.117126318651471,
1.2219845994776));
#17024=CARTESIAN_POINT('Ctrl Pts',(0.0293783748903316,-0.170469176734012,
1.2299235891149));
#17025=CARTESIAN_POINT('Ctrl Pts',(0.159158794190081,-0.0677591865323411,
1.23786257875221));
#17026=CARTESIAN_POINT('Ctrl Pts',(0.143240245273553,0.0969796950995427,
1.24580156838952));
#17027=CARTESIAN_POINT('Ctrl Pts',(-0.00380493129617075,0.172940312320012,
1.25374055802682));
#17028=CARTESIAN_POINT('Ctrl Pts',(-0.147366954032488,0.0905859259858403,
1.26167954766413));
#17029=CARTESIAN_POINT('Ctrl Pts',(-0.156024630070406,-0.074693667330688,
1.26961853730143));
#17030=CARTESIAN_POINT('Ctrl Pts',(-0.0218524503424686,-0.171596327294885,
1.27755752693874));
#17031=CARTESIAN_POINT('Ctrl Pts',(0.132324150022753,-0.111414309889572,
1.28549651657604));
#17032=CARTESIAN_POINT('Ctrl Pts',(0.165367059817933,0.0507598725070622,
1.29343550621335));
#17033=CARTESIAN_POINT('Ctrl Pts',(0.0470277596764783,0.166466870408131,
1.30137449585065));
#17034=CARTESIAN_POINT('Ctrl Pts',(-0.114362231391601,0.129784857201791,
1.30931348548797));
#17035=CARTESIAN_POINT('Ctrl Pts',(-0.171061437441431,-0.0257062980954763,
1.31725247512526));
#17036=CARTESIAN_POINT('Ctrl Pts',(-0.071165620995849,-0.157665099140374,
1.32519146476257));
#17037=CARTESIAN_POINT('Ctrl Pts',(0.0938774439379855,-0.145292307632914,
1.33313045439988));
#17038=CARTESIAN_POINT('Ctrl Pts',(0.172982143233999,8.56343898915854E-5,
1.34106944403719));
#17039=CARTESIAN_POINT('Ctrl Pts',(0.0937335447930804,0.145385183220099,
1.34900843367449));
#17040=CARTESIAN_POINT('Ctrl Pts',(-0.0713216883190155,0.157594562185848,
1.3569474233118));
#17041=CARTESIAN_POINT('Ctrl Pts',(-0.171086806821499,0.0255369173285507,
1.3648864129491));
#17042=CARTESIAN_POINT('Ctrl Pts',(-0.114233673229396,-0.129898019862958,
1.37282540258641));
#17043=CARTESIAN_POINT('Ctrl Pts',(0.0471925482590101,-0.166420232464351,
1.38076439222371));
#17044=CARTESIAN_POINT('Ctrl Pts',(0.165417247017141,-0.0505961085897048,
1.38870338186102));
#17045=CARTESIAN_POINT('Ctrl Pts',(0.132213753266125,0.111545248710567,
1.39664237149832));
#17046=CARTESIAN_POINT('Ctrl Pts',(-0.0220222951247444,0.17157464463752,
1.40458136113563));
#17047=CARTESIAN_POINT('Ctrl Pts',(-0.156098584526576,0.0745390809398717,
1.41252035077293));
#17048=CARTESIAN_POINT('Ctrl Pts',(-0.147277046608992,-0.0907316537045687,
1.42045934041024));
#17049=CARTESIAN_POINT('Ctrl Pts',(-0.00363398118293899,-0.172944250658386,
1.42839833004755));
#17050=CARTESIAN_POINT('Ctrl Pts',(0.143336722904634,-0.0968373407211472,
1.43633731968485));
#17051=CARTESIAN_POINT('Ctrl Pts',(0.159090624036536,0.0679158129692223,
1.44427630932216));
#17052=CARTESIAN_POINT('Ctrl Pts',(0.0292114869387437,0.170499931406899,
1.45221529895946));
#17053=CARTESIAN_POINT('Ctrl Pts',(-0.127415456569397,0.116996902323752,
1.46015428859677));
#17054=CARTESIAN_POINT('Ctrl Pts',(-0.167389576437263,-0.0435971050111283,
1.46809327823408));
#17055=CARTESIAN_POINT('Ctrl Pts',(-0.0541541359620402,-0.164303103757731,
1.47603226787138));
#17056=CARTESIAN_POINT('Ctrl Pts',(0.108701533888403,-0.13455879509903,
1.48397125750869));
#17057=CARTESIAN_POINT('Ctrl Pts',(0.171961157005542,0.0182848320604298,
1.49191024714599));
#17058=CARTESIAN_POINT('Ctrl Pts',(0.0779697431325927,0.154543202561513,
1.4998492367833));
#17059=CARTESIAN_POINT('Ctrl Pts',(-0.0877325682749983,0.149025855561406,
1.5077882264206));
#17060=CARTESIAN_POINT('Ctrl Pts',(-0.144149484752264,0.0548439265155397,
1.51308088617881));
#17061=CARTESIAN_POINT('Ctrl Pts',(-0.146217781693078,0.00621955116994065,
1.51572721605791));
#17062=CARTESIAN_POINT('Ctrl Pts',(0.0795408277542855,-0.111329858282327,
-0.0109985226280624));
#17063=CARTESIAN_POINT('Ctrl Pts',(0.116563307192903,-0.0848787452970238,
-0.00835219274896048));
#17064=CARTESIAN_POINT('Ctrl Pts',(0.16150817751539,0.00739908052493189,
-0.00305953299075667));
#17065=CARTESIAN_POINT('Ctrl Pts',(0.0812084309002137,0.139981433724326,
0.00487945664654907));
#17066=CARTESIAN_POINT('Ctrl Pts',(-0.0734975292821143,0.144003850402812,
0.0128184462838548));
#17067=CARTESIAN_POINT('Ctrl Pts',(-0.160887120581772,0.0164101388376342,
0.0207574359211605));
#17068=CARTESIAN_POINT('Ctrl Pts',(-0.101013704785435,-0.126315124179183,
0.0286964255584662));
#17069=CARTESIAN_POINT('Ctrl Pts',(0.0513403816191153,-0.153350170642076,
0.0366354151957719));
#17070=CARTESIAN_POINT('Ctrl Pts',(0.156690838735662,-0.0400338514845966,
0.0445744048330777));
#17071=CARTESIAN_POINT('Ctrl Pts',(0.118604220350264,0.109946623274354,
0.0525133944703833));
#17072=CARTESIAN_POINT('Ctrl Pts',(-0.0280578283917351,0.15927012049393,
0.0604523841076892));
#17073=CARTESIAN_POINT('Ctrl Pts',(-0.14903412333264,0.0627971513379326,
0.0683913737449947));
#17074=CARTESIAN_POINT('Ctrl Pts',(-0.133580279395553,-0.0911646307683348,
0.0763303633823007));
#17075=CARTESIAN_POINT('Ctrl Pts',(0.0041573593468571,-0.161670216863261,
0.0842693530196062));
#17076=CARTESIAN_POINT('Ctrl Pts',(0.138089113144455,-0.0841784443595545,
0.0922083426569122));
#17077=CARTESIAN_POINT('Ctrl Pts',(0.14560980428584,0.0703732645446943,
0.100147332294218));
#17078=CARTESIAN_POINT('Ctrl Pts',(0.0198346691022095,0.160502893816501,
0.108086321931524));
#17079=CARTESIAN_POINT('Ctrl Pts',(-0.124097730593135,0.103703218031488,
0.116025311568829));
#17080=CARTESIAN_POINT('Ctrl Pts',(-0.154427171169137,-0.0480296962598115,
0.123964301206135));
#17081=CARTESIAN_POINT('Ctrl Pts',(-0.0433891157712434,-0.155794689166463,
0.13190329084344));
#17082=CARTESIAN_POINT('Ctrl Pts',(0.107368699171666,-0.12094033522185,
0.139842280480747));
#17083=CARTESIAN_POINT('Ctrl Pts',(0.15983782968835,0.0246266142906177,
0.147781270118052));
#17084=CARTESIAN_POINT('Ctrl Pts',(0.0659863808909888,0.147649582370873,
0.155720259755358));
#17085=CARTESIAN_POINT('Ctrl Pts',(-0.0882710769349216,0.135509478890084,
0.163659249392663));
#17086=CARTESIAN_POINT('Ctrl Pts',(-0.161722413615419,-0.00068026650363694,
0.171598239029969));
#17087=CARTESIAN_POINT('Ctrl Pts',(-0.0871279640988751,-0.136247273976568,
0.179537228667275));
#17088=CARTESIAN_POINT('Ctrl Pts',(0.0672261652318651,-0.147089240053593,
0.187476218304581));
#17089=CARTESIAN_POINT('Ctrl Pts',(0.160039347628626,-0.023281087390596,
0.195415207941886));
#17090=CARTESIAN_POINT('Ctrl Pts',(0.106347475470598,0.121839305139765,
0.203354197579192));
#17091=CARTESIAN_POINT('Ctrl Pts',(-0.0446982220051161,0.15542416405057,
0.211293187216498));
#17092=CARTESIAN_POINT('Ctrl Pts',(-0.154825760608133,0.0467288526640558,
0.219232176853804));
#17093=CARTESIAN_POINT('Ctrl Pts',(-0.12322092627477,-0.104743520787053,
0.227171166491109));
#17094=CARTESIAN_POINT('Ctrl Pts',(0.0211842211805034,-0.160330379506191,
0.235110156128415));
#17095=CARTESIAN_POINT('Ctrl Pts',(0.146196665995071,-0.0691457639426259,
0.24304914576572));
#17096=CARTESIAN_POINT('Ctrl Pts',(0.137376082602736,0.0853370596399817,
0.250988135403027));
#17097=CARTESIAN_POINT('Ctrl Pts',(0.00279711058556459,0.161699653653757,
0.258927125040332));
#17098=CARTESIAN_POINT('Ctrl Pts',(-0.134342424474264,0.0900372967480426,
0.266866114677638));
#17099=CARTESIAN_POINT('Ctrl Pts',(-0.148500677015507,-0.0640480346713102,
0.274805104314944));
#17100=CARTESIAN_POINT('Ctrl Pts',(-0.0267167371651392,-0.159501779847699,
0.282744093952249));
#17101=CARTESIAN_POINT('Ctrl Pts',(0.119524544542348,-0.108942576944327,
0.290683083589556));
#17102=CARTESIAN_POINT('Ctrl Pts',(0.156349297273321,0.0413460888291301,
0.29862207322686));
#17103=CARTESIAN_POINT('Ctrl Pts',(0.0500469836677093,0.153785243912065,
0.306561062864167));
#17104=CARTESIAN_POINT('Ctrl Pts',(-0.102069913541897,0.125444547784578,
0.314500052501472));
#17105=CARTESIAN_POINT('Ctrl Pts',(-0.160748800211922,-0.0177320345633525,
0.322439042138778));
#17106=CARTESIAN_POINT('Ctrl Pts',(-0.0722731771226978,-0.144676154524232,
0.330378031776084));
#17107=CARTESIAN_POINT('Ctrl Pts',(0.082363586418043,-0.139179170322594,
0.338317021413389));
#17108=CARTESIAN_POINT('Ctrl Pts',(0.16160213133829,-0.00627319426210969,
0.346256011050695));
#17109=CARTESIAN_POINT('Ctrl Pts',(0.0929050003357002,0.132375461215256,
0.354195000688001));
#17110=CARTESIAN_POINT('Ctrl Pts',(-0.0608402912787218,0.149843454232904,
0.362133990325306));
#17111=CARTESIAN_POINT('Ctrl Pts',(-0.158890465884947,0.0301400343429239,
0.370072979962613));
#17112=CARTESIAN_POINT('Ctrl Pts',(-0.1114873084483,-0.117154521356547,
0.378011969599918));
#17113=CARTESIAN_POINT('Ctrl Pts',(0.0379748391485164,-0.157202141877815,
0.385950959237223));
#17114=CARTESIAN_POINT('Ctrl Pts',(0.152673624090564,-0.0533419752763387,
0.39388994887453));
#17115=CARTESIAN_POINT('Ctrl Pts',(0.127610169584502,0.0993491139263089,
0.401828938511835));
#17116=CARTESIAN_POINT('Ctrl Pts',(-0.014271649480085,0.16109289816887,
0.409767928149142));
#17117=CARTESIAN_POINT('Ctrl Pts',(-0.143088751545671,0.0753671745551693,
0.417706917786446));
#17118=CARTESIAN_POINT('Ctrl Pts',(-0.140917908083783,-0.0793520321139836,
0.425645907423752));
#17119=CARTESIAN_POINT('Ctrl Pts',(-0.00974637750615997,-0.161429891732714,
0.433584897061058));
#17120=CARTESIAN_POINT('Ctrl Pts',(0.130347293715478,-0.0957297489831606,
0.441523886698364));
#17121=CARTESIAN_POINT('Ctrl Pts',(0.15111695082405,0.0576044181723055,
0.449462876335669));
#17122=CARTESIAN_POINT('Ctrl Pts',(0.0335493961742207,0.158205688379633,
0.457401865972975));
#17123=CARTESIAN_POINT('Ctrl Pts',(-0.114730331382826,0.113980493419335,
0.465340855610281));
#17124=CARTESIAN_POINT('Ctrl Pts',(-0.157982303542021,-0.03458603167299,
0.473279845247587));
#17125=CARTESIAN_POINT('Ctrl Pts',(-0.0566123040428622,-0.151491415104245,
0.481218834884892));
#17126=CARTESIAN_POINT('Ctrl Pts',(0.0965823799129518,-0.129716790392294,
0.489157824522198));
#17127=CARTESIAN_POINT('Ctrl Pts',(0.161362514281243,0.0108046658515635,
0.497096814159504));
#17128=CARTESIAN_POINT('Ctrl Pts',(0.0784263257203939,0.141435191000425,
0.50503580379681));
#17129=CARTESIAN_POINT('Ctrl Pts',(-0.076303789130349,0.14259149197508,
0.512974793434115));
#17130=CARTESIAN_POINT('Ctrl Pts',(-0.161183014472451,0.0132150544797126,
0.520913783071421));
#17131=CARTESIAN_POINT('Ctrl Pts',(-0.0985102366584373,-0.128258859705,
0.528852772708727));
#17132=CARTESIAN_POINT('Ctrl Pts',(0.0543419114689404,-0.152320577983508,
0.536791762346032));
#17133=CARTESIAN_POINT('Ctrl Pts',(0.157447763940923,-0.0369432463290883,
0.544730751983338));
#17134=CARTESIAN_POINT('Ctrl Pts',(0.116420979124965,0.112253095453589,
0.552669741620643));
#17135=CARTESIAN_POINT('Ctrl Pts',(-0.0311812332291155,0.158689421555565,
0.56060873125795));
#17136=CARTESIAN_POINT('Ctrl Pts',(-0.150239163551416,0.0598564579197502,
0.568547720895255));
#17137=CARTESIAN_POINT('Ctrl Pts',(-0.131763436204723,-0.0937709907106254,
0.576486710532561));
#17138=CARTESIAN_POINT('Ctrl Pts',(0.00733268664935855,-0.161557523891122,
0.584425700169866));
#17139=CARTESIAN_POINT('Ctrl Pts',(0.139716237417787,-0.0814492162095161,
0.592364689807173));
#17140=CARTESIAN_POINT('Ctrl Pts',(0.144199148209332,0.0732202668325601,
0.600303679444478));
#17141=CARTESIAN_POINT('Ctrl Pts',(0.0166776214282734,0.160861613702037,
0.608242669081784));
#17142=CARTESIAN_POINT('Ctrl Pts',(-0.126111124778327,0.101245177793678,
0.616181658719089));
#17143=CARTESIAN_POINT('Ctrl Pts',(-0.153453779210204,-0.0510542795996006,
0.624120648356396));
#17144=CARTESIAN_POINT('Ctrl Pts',(-0.0403200156494649,-0.156617042997737,
0.6320596379937));
#17145=CARTESIAN_POINT('Ctrl Pts',(0.10972395892722,-0.118807637198397,
0.639998627631007));
#17146=CARTESIAN_POINT('Ctrl Pts',(0.159323168980049,0.0277620180369333,
0.647937617268312));
#17147=CARTESIAN_POINT('Ctrl Pts',(0.0630729369615192,0.148917448414806,
0.655876606905618));
#17148=CARTESIAN_POINT('Ctrl Pts',(-0.0909162461746061,0.133749160748195,
0.663815596542924));
#17149=CARTESIAN_POINT('Ctrl Pts',(-0.161677836835157,-0.00385731715476066,
0.671754586180229));
#17150=CARTESIAN_POINT('Ctrl Pts',(-0.0844344483789265,-0.137932685561743,
0.679693575817536));
#17151=CARTESIAN_POINT('Ctrl Pts',(0.0701028908975481,-0.145740133481257,
0.687632565454841));
#17152=CARTESIAN_POINT('Ctrl Pts',(0.1604658380222,-0.0201324774223393,
0.695571555092147));
#17153=CARTESIAN_POINT('Ctrl Pts',(0.10393330787963,0.123905081947942,0.703510544729453));
#17154=CARTESIAN_POINT('Ctrl Pts',(-0.0477430426119635,0.15451603056473,
0.711449534366758));
#17155=CARTESIAN_POINT('Ctrl Pts',(-0.155713909636705,0.0436781428746717,
0.719388524004064));
#17156=CARTESIAN_POINT('Ctrl Pts',(-0.121139364160222,-0.10714409115852,
0.72732751364137));
#17157=CARTESIAN_POINT('Ctrl Pts',(0.0243299669821161,-0.159883252800214,
0.735266503278675));
#17158=CARTESIAN_POINT('Ctrl Pts',(0.147526880793862,-0.0662602540182413,
0.743205492915981));
#17159=CARTESIAN_POINT('Ctrl Pts',(0.135673045916277,0.0880194662056535,
0.751144482553287));
#17160=CARTESIAN_POINT('Ctrl Pts',(-0.000380164216571841,0.161723397486253,
0.759083472190592));
#17161=CARTESIAN_POINT('Ctrl Pts',(-0.136085360063504,0.0873806419964673,
0.767022461827899));
#17162=CARTESIAN_POINT('Ctrl Pts',(-0.147213735311121,-0.0669531026545853,
0.774961451465203));
#17163=CARTESIAN_POINT('Ctrl Pts',(-0.023578025097595,-0.159995870421162,
0.78290044110251));
#17164=CARTESIAN_POINT('Ctrl Pts',(0.121641751185188,-0.106573384050283,
0.790839430739816));
#17165=CARTESIAN_POINT('Ctrl Pts',(0.155506840911589,0.0444097314676148,
0.798778420377121));
#17166=CARTESIAN_POINT('Ctrl Pts',(0.047016075363265,0.15473878142458,0.806717410014428));
#17167=CARTESIAN_POINT('Ctrl Pts',(-0.104514684958047,0.123415081928621,
0.814656399651731));
#17168=CARTESIAN_POINT('Ctrl Pts',(-0.16036941405942,-0.020886666885039,
0.82259538928904));
#17169=CARTESIAN_POINT('Ctrl Pts',(-0.0694169354231278,-0.146068103622213,
0.830534378926343));
#17170=CARTESIAN_POINT('Ctrl Pts',(0.085081990139753,-0.137534202194171,
0.838473368563651));
#17171=CARTESIAN_POINT('Ctrl Pts',(0.161694184779289,-0.00309716449182502,
0.846412358200955));
#17172=CARTESIAN_POINT('Ctrl Pts',(0.0902864348795877,0.134175115040242,
0.854351347838261));
#17173=CARTESIAN_POINT('Ctrl Pts',(-0.0637723584188847,0.148619272374149,
0.862290337475567));
#17174=CARTESIAN_POINT('Ctrl Pts',(-0.159451928190027,0.0270126713934565,
0.870229327112872));
#17175=CARTESIAN_POINT('Ctrl Pts',(-0.109164185657521,-0.119322178948671,
0.878168316750179));
#17176=CARTESIAN_POINT('Ctrl Pts',(0.0410558873341998,-0.156425752146281,
0.886107306387484));
#17177=CARTESIAN_POINT('Ctrl Pts',(0.153692109215179,-0.0503322698109037,
0.894046296024789));
#17178=CARTESIAN_POINT('Ctrl Pts',(0.125633738317809,0.101836956040625,
0.901985285662096));
#17179=CARTESIAN_POINT('Ctrl Pts',(-0.0174337097671096,0.160781427979367,
0.909924275299401));
#17180=CARTESIAN_POINT('Ctrl Pts',(-0.144541791370401,0.072541521673891,
0.917863264936708));
#17181=CARTESIAN_POINT('Ctrl Pts',(-0.13933176907,-0.082105176128868,0.925802254574012));
#17182=CARTESIAN_POINT('Ctrl Pts',(-0.00657306121577474,-0.161590212220858,
0.933741244211319));
#17183=CARTESIAN_POINT('Ctrl Pts',(0.132202833700187,-0.0931504835251481,
0.941680233848624));
#17184=CARTESIAN_POINT('Ctrl Pts',(0.149956094815541,0.0605621288182698,
0.949619223485929));
#17185=CARTESIAN_POINT('Ctrl Pts',(0.0304348282896272,0.158834262822317,
0.957558213123236));
#17186=CARTESIAN_POINT('Ctrl Pts',(-0.116947437700435,0.111704514835484,
0.965497202760542));
#17187=CARTESIAN_POINT('Ctrl Pts',(-0.157272339407096,-0.0376830608728604,
0.973436192397847));
#17188=CARTESIAN_POINT('Ctrl Pts',(-0.0536251929639052,-0.152574376940928,
0.981375182035153));
#17189=CARTESIAN_POINT('Ctrl Pts',(0.0991121424632477,-0.127794307524525,
0.989314171672459));
#17190=CARTESIAN_POINT('Ctrl Pts',(0.161119104064031,0.0139726921146952,
0.997253161309763));
#17191=CARTESIAN_POINT('Ctrl Pts',(0.0756325681075411,0.142948649734045,
1.00519215094707));
#17192=CARTESIAN_POINT('Ctrl Pts',(-0.0790904005129918,0.141064915432658,
1.01313114058437));
#17193=CARTESIAN_POINT('Ctrl Pts',(-0.161411527883023,0.0100459188627121,
1.02107013022168));
#17194=CARTESIAN_POINT('Ctrl Pts',(-0.095971463730607,-0.130169427934261,
1.02900911985899));
#17195=CARTESIAN_POINT('Ctrl Pts',(0.0573238981132153,-0.151223584550935,
1.03694810949629));
#17196=CARTESIAN_POINT('Ctrl Pts',(0.158143159897702,-0.0338429135403315,
1.0448870991336));
#17197=CARTESIAN_POINT('Ctrl Pts',(0.114193197054413,0.114518625410106,
1.0528260887709));
#17198=CARTESIAN_POINT('Ctrl Pts',(-0.0342928115212847,0.158046211271557,
1.06076507840821));
#17199=CARTESIAN_POINT('Ctrl Pts',(-0.151386101389109,0.0568933223281485,
1.06870406804552));
#17200=CARTESIAN_POINT('Ctrl Pts',(-0.129895790602315,-0.0963415040526547,
1.07664305768282));
#17201=CARTESIAN_POINT('Ctrl Pts',(0.0105052141409744,-0.161382286187737,
1.08458204732013));
#17202=CARTESIAN_POINT('Ctrl Pts',(0.141289415307547,-0.0786886455683398,
1.09252103695743));
#17203=CARTESIAN_POINT('Ctrl Pts',(0.14273283995608,0.076039057183793,1.10046002659474));
#17204=CARTESIAN_POINT('Ctrl Pts',(0.013514131745196,0.161158214381091,
1.10839901623204));
#17205=CARTESIAN_POINT('Ctrl Pts',(-0.128075837894479,0.0987480712062529,
1.11633800586935));
#17206=CARTESIAN_POINT('Ctrl Pts',(-0.152421155552179,-0.0540591635106084,
1.12427699550666));
#17207=CARTESIAN_POINT('Ctrl Pts',(-0.0372353514058616,-0.157378938949945,
1.13221598514396));
#17208=CARTESIAN_POINT('Ctrl Pts',(0.11203686504723,-0.116629081663695,
1.14015497478127));
#17209=CARTESIAN_POINT('Ctrl Pts',(0.158747009937404,0.0308867067726846,
1.14809396441857));
#17210=CARTESIAN_POINT('Ctrl Pts',(0.0601351468730053,0.150127831962932,
1.15603295405588));
#17211=CARTESIAN_POINT('Ctrl Pts',(-0.0935263218228598,0.13193721592339,
1.16397194369318));
#17212=CARTESIAN_POINT('Ctrl Pts',(-0.161570852667341,-0.00703287904607843,
1.17191093333049));
#17213=CARTESIAN_POINT('Ctrl Pts',(-0.0817083410685703,-0.13956485524354,
1.17984992296779));
#17214=CARTESIAN_POINT('Ctrl Pts',(0.0729525569401478,-0.144334771469742,
1.1877889126051));
#17215=CARTESIAN_POINT('Ctrl Pts',(0.160830388835411,-0.016976096323307,
1.19572790224241));
#17216=CARTESIAN_POINT('Ctrl Pts',(0.101479022178261,0.125923031559255,
1.20366689187971));
#17217=CARTESIAN_POINT('Ctrl Pts',(-0.0507694344715009,0.153548254118279,
1.21160588151702));
#17218=CARTESIAN_POINT('Ctrl Pts',(-0.15654195331917,0.0406105733811438,
1.21954487115432));
#17219=CARTESIAN_POINT('Ctrl Pts',(-0.119011042423884,-0.109503304062093,
1.22748386079163));
#17220=CARTESIAN_POINT('Ctrl Pts',(0.0274663214511058,-0.159374411387982,
1.23542285042894));
#17221=CARTESIAN_POINT('Ctrl Pts',(0.148800150427453,-0.0633491677300162,
1.24336184006624));
#17222=CARTESIAN_POINT('Ctrl Pts',(0.133917639627974,0.0906678973829495,
1.25130082970354));
#17223=CARTESIAN_POINT('Ctrl Pts',(-0.00355729227603857,0.161684716318317,
1.25923981934086));
#17224=CARTESIAN_POINT('Ctrl Pts',(-0.137775766897813,0.0846902584421788,
1.26717880897816));
#17225=CARTESIAN_POINT('Ctrl Pts',(-0.14586996931591,-0.0698323268364953,
1.27511779861547));
#17226=CARTESIAN_POINT('Ctrl Pts',(-0.0204302119447119,-0.160428202816007,
1.28305678825277));
#17227=CARTESIAN_POINT('Ctrl Pts',(0.123712004283314,-0.104163053984564,
1.29099577789008));
#17228=CARTESIAN_POINT('Ctrl Pts',(0.15460435913624,0.0474562320176185,
1.29893476752738));
#17229=CARTESIAN_POINT('Ctrl Pts',(0.043967018911749,0.155632589980133,
1.30687375716469));
#17230=CARTESIAN_POINT('Ctrl Pts',(-0.106919113837756,0.121337978043289,
1.31481274680199));
#17231=CARTESIAN_POINT('Ctrl Pts',(-0.159928125575155,-0.0240332370134145,
1.3227517364393));
#17232=CARTESIAN_POINT('Ctrl Pts',(-0.0665338988230771,-0.147403670583407,
1.33069072607661));
#17233=CARTESIAN_POINT('Ctrl Pts',(0.0877675522160205,-0.135836146169277,
1.33862971571391));
#17234=CARTESIAN_POINT('Ctrl Pts',(0.161723824721502,8.00609866524728E-5,
1.34656870535122));
#17235=CARTESIAN_POINT('Ctrl Pts',(0.0876330185603928,0.135922977069285,
1.35450769498852));
#17236=CARTESIAN_POINT('Ctrl Pts',(-0.0666798087068602,0.147337724435113,
1.36244668462583));
#17237=CARTESIAN_POINT('Ctrl Pts',(-0.159951843822013,0.0238748801740983,
1.37038567426313));
#17238=CARTESIAN_POINT('Ctrl Pts',(-0.106798922716859,-0.121443775659372,
1.37832466390044));
#17239=CARTESIAN_POINT('Ctrl Pts',(0.0441210824430389,-0.155588987406456,
1.38626365353774));
#17240=CARTESIAN_POINT('Ctrl Pts',(0.154651279966657,-0.0473031264624986,
1.39420264317505));
#17241=CARTESIAN_POINT('Ctrl Pts',(0.123608792556459,0.10428547082216,1.40214163281236));
#17242=CARTESIAN_POINT('Ctrl Pts',(-0.020589002599541,0.160407931346284,
1.41008062244966));
#17243=CARTESIAN_POINT('Ctrl Pts',(-0.145939110542184,0.0696878015005003,
1.41801961208697));
#17244=CARTESIAN_POINT('Ctrl Pts',(-0.137691710982408,-0.0848265016612731,
1.42595860172427));
#17245=CARTESIAN_POINT('Ctrl Pts',(-0.00339746822928561,-0.161688398335044,
1.43389759136158));
#17246=CARTESIAN_POINT('Ctrl Pts',(0.134007838137522,-0.0905348079547059,
1.44183658099889));
#17247=CARTESIAN_POINT('Ctrl Pts',(0.148736417039967,0.0634956003383226,
1.44977557063619));
#17248=CARTESIAN_POINT('Ctrl Pts',(0.0273102951854726,0.159403164432859,
1.4577145602735));
#17249=CARTESIAN_POINT('Ctrl Pts',(-0.119122786779006,0.109382310628272,
1.4656535499108));
#17250=CARTESIAN_POINT('Ctrl Pts',(-0.156495242883694,-0.0407596439572756,
1.47359253954811));
#17251=CARTESIAN_POINT('Ctrl Pts',(-0.0506295842364637,-0.153609649276743,
1.48153152918541));
#17252=CARTESIAN_POINT('Ctrl Pts',(0.10162683549218,-0.125801210382132,
1.48947051882272));
#17253=CARTESIAN_POINT('Ctrl Pts',(0.160769288057966,0.017094787472962,
1.49740950846002));
#17254=CARTESIAN_POINT('Ctrl Pts',(0.0728951834924312,0.144484958595688,
1.50534849809733));
#17255=CARTESIAN_POINT('Ctrl Pts',(-0.0820226078184241,0.139326700971572,
1.51328748773464));
#17256=CARTESIAN_POINT('Ctrl Pts',(-0.134767702434085,0.0512744806661359,
1.51858014749284));
#17257=CARTESIAN_POINT('Ctrl Pts',(-0.136701386950156,0.00581475974600206,
1.52122647737194));
#17258=CARTESIAN_POINT('Ctrl Pts',(0.0740036351041134,-0.103579689087085,
-0.0054992613140312));
#17259=CARTESIAN_POINT('Ctrl Pts',(0.108448814220036,-0.0789699563406641,
-0.00285293143492929));
#17260=CARTESIAN_POINT('Ctrl Pts',(0.150264871169078,0.00688399744800666,
0.00243972832327453));
#17261=CARTESIAN_POINT('Ctrl Pts',(0.0755551489391376,0.130236700260234,
0.0103787179605803));
#17262=CARTESIAN_POINT('Ctrl Pts',(-0.0683810376584167,0.133979098529349,
0.0183177075978859));
#17263=CARTESIAN_POINT('Ctrl Pts',(-0.14968704878538,0.0152677557027674,
0.0262566972351917));
#17264=CARTESIAN_POINT('Ctrl Pts',(-0.0939816891590436,-0.11752176362514,
0.0341956868724974));
#17265=CARTESIAN_POINT('Ctrl Pts',(0.0477663481097245,-0.142674779628989,
0.0421346765098031));
#17266=CARTESIAN_POINT('Ctrl Pts',(0.14578288888032,-0.0372469160898187,
0.0500736661471088));
#17267=CARTESIAN_POINT('Ctrl Pts',(0.110347650287512,0.102292747252513,
0.0580126557844146));
#17268=CARTESIAN_POINT('Ctrl Pts',(-0.0261045975097209,0.148182615303324,
0.0659516454217203));
#17269=CARTESIAN_POINT('Ctrl Pts',(-0.13865919166998,0.0584255608647477,
0.073890635059026));
#17270=CARTESIAN_POINT('Ctrl Pts',(-0.124281158904105,-0.0848182532198701,
0.0818296246963318));
#17271=CARTESIAN_POINT('Ctrl Pts',(0.00386794697500161,-0.15041563023346,
0.0897686143336374));
#17272=CARTESIAN_POINT('Ctrl Pts',(0.128476112576568,-0.0783184064825255,
0.0977076039709433));
#17273=CARTESIAN_POINT('Ctrl Pts',(0.135473254782295,0.0654742669580799,
0.105646593608249));
#17274=CARTESIAN_POINT('Ctrl Pts',(0.0184538891044151,0.149329569763132,
0.113585583245555));
#17275=CARTESIAN_POINT('Ctrl Pts',(-0.115458732720671,0.096483973363118,
0.12152457288286));
#17276=CARTESIAN_POINT('Ctrl Pts',(-0.143676805334049,-0.0446861343604874,
0.129463562520166));
#17277=CARTESIAN_POINT('Ctrl Pts',(-0.0403686054279526,-0.144949124289353,
0.137402552157472));
#17278=CARTESIAN_POINT('Ctrl Pts',(0.0998942839726139,-0.112521137758025,
0.145341541794778));
#17279=CARTESIAN_POINT('Ctrl Pts',(0.14871080372247,0.0229122455632766,
0.153280531432083));
#17280=CARTESIAN_POINT('Ctrl Pts',(0.0613927738894439,0.137371034794898,
0.161219521069389));
#17281=CARTESIAN_POINT('Ctrl Pts',(-0.0821261326059948,0.126076058196294,
0.169158510706695));
#17282=CARTESIAN_POINT('Ctrl Pts',(-0.150464193336327,-0.000632910110818063,
0.177097500344));
#17283=CARTESIAN_POINT('Ctrl Pts',(-0.0810625969653723,-0.126762492068094,
0.185036489981306));
#17284=CARTESIAN_POINT('Ctrl Pts',(0.0625462512992226,-0.136849700411639,
0.192975479618612));
#17285=CARTESIAN_POINT('Ctrl Pts',(0.148898293097928,-0.0216603868066741,
0.200914469255917));
#17286=CARTESIAN_POINT('Ctrl Pts',(0.0989441522193119,0.113357526360621,
0.208853458893223));
#17287=CARTESIAN_POINT('Ctrl Pts',(-0.0415865789238149,0.144604393083411,
0.216792448530529));
#17288=CARTESIAN_POINT('Ctrl Pts',(-0.144047647180085,0.0434758483035601,
0.224731438167835));
#17289=CARTESIAN_POINT('Ctrl Pts',(-0.114642966671137,-0.0974518559926297,
0.232670427805141));
#17290=CARTESIAN_POINT('Ctrl Pts',(0.0197094928286333,-0.149169064945282,
0.240609417442446));
#17291=CARTESIAN_POINT('Ctrl Pts',(0.136019262424063,-0.0643322181611298,
0.248548407079752));
#17292=CARTESIAN_POINT('Ctrl Pts',(0.127812719278849,0.0793963653730636,
0.256487396717058));
#17293=CARTESIAN_POINT('Ctrl Pts',(0.00260239121171357,0.150443017797356,
0.264426386354363));
#17294=CARTESIAN_POINT('Ctrl Pts',(-0.124990247656303,0.0837693979610897,
0.272365375991669));
#17295=CARTESIAN_POINT('Ctrl Pts',(-0.138162880936044,-0.0595893646165358,
0.280304365628975));
#17296=CARTESIAN_POINT('Ctrl Pts',(-0.0248568656394851,-0.148398147813718,
0.288243355266281));
#17297=CARTESIAN_POINT('Ctrl Pts',(0.111203906597776,-0.101358597076653,
0.296182344903586));
#17298=CARTESIAN_POINT('Ctrl Pts',(0.145465123646218,0.0384678027257296,
0.304121334540892));
#17299=CARTESIAN_POINT('Ctrl Pts',(0.0465629893725541,0.143079565503422,
0.312060324178198));
#17300=CARTESIAN_POINT('Ctrl Pts',(-0.0949643705016135,0.116711791945748,
0.319999313815503));
#17301=CARTESIAN_POINT('Ctrl Pts',(-0.149558357514911,-0.0164976283567656,
0.327938303452809));
#17302=CARTESIAN_POINT('Ctrl Pts',(-0.0672419181269484,-0.134604600554976,
0.335877293090115));
#17303=CARTESIAN_POINT('Ctrl Pts',(0.0766298889166206,-0.12949028600085,
0.343816282727421));
#17304=CARTESIAN_POINT('Ctrl Pts',(0.150352284446295,-0.00583648916182633,
0.351755272364726));
#17305=CARTESIAN_POINT('Ctrl Pts',(0.0864374678803939,0.123160213504125,
0.359694262002032));
#17306=CARTESIAN_POINT('Ctrl Pts',(-0.0566049265834532,0.139412181427728,
0.367633251639338));
#17307=CARTESIAN_POINT('Ctrl Pts',(-0.147829390149123,0.0280418517950267,
0.375572241276644));
#17308=CARTESIAN_POINT('Ctrl Pts',(-0.103726178443039,-0.108998871322406,
0.383511230913949));
#17309=CARTESIAN_POINT('Ctrl Pts',(0.0353312408083745,-0.146258597924691,
0.391450220551255));
#17310=CARTESIAN_POINT('Ctrl Pts',(0.142045330507792,-0.0496286018832686,
0.399389210188561));
#17311=CARTESIAN_POINT('Ctrl Pts',(0.118726655129599,0.0924329779120693,
0.407328199825866));
#17312=CARTESIAN_POINT('Ctrl Pts',(-0.0132781361506635,0.1498785012746,
0.415267189463172));
#17313=CARTESIAN_POINT('Ctrl Pts',(-0.133127703795094,0.0701205285647604,
0.423206179100478));
#17314=CARTESIAN_POINT('Ctrl Pts',(-0.131107982452518,-0.0738279823724454,
0.431145168737783));
#17315=CARTESIAN_POINT('Ctrl Pts',(-0.00906788859151817,-0.150192035209753,
0.439084158375089));
#17316=CARTESIAN_POINT('Ctrl Pts',(0.121273235812024,-0.0890655731449414,
0.447023148012395));
#17317=CARTESIAN_POINT('Ctrl Pts',(0.14059702422731,0.0535943170716914,
0.4549621376497));
#17318=CARTESIAN_POINT('Ctrl Pts',(0.031213872705855,0.14719228306762,0.462901127287006));
#17319=CARTESIAN_POINT('Ctrl Pts',(-0.106743440051405,0.106045801661112,
0.470840116924312));
#17320=CARTESIAN_POINT('Ctrl Pts',(-0.146984449047318,-0.0321783433727119,
0.478779106561618));
#17321=CARTESIAN_POINT('Ctrl Pts',(-0.0526712684425847,-0.140945420374714,
0.486718096198923));
#17322=CARTESIAN_POINT('Ctrl Pts',(0.0898588486235595,-0.120686624644175,
0.49465708583623));
#17323=CARTESIAN_POINT('Ctrl Pts',(0.150129348203927,0.0100525047535443,
0.502596075473534));
#17324=CARTESIAN_POINT('Ctrl Pts',(0.0729667185397875,0.131589254992538,
0.510535065110842));
#17325=CARTESIAN_POINT('Ctrl Pts',(-0.0709919412117167,0.132665060686482,
0.518474054748145));
#17326=CARTESIAN_POINT('Ctrl Pts',(-0.149962344179375,0.0122950954523496,
0.526413044385453));
#17327=CARTESIAN_POINT('Ctrl Pts',(-0.0916524986414713,-0.119330187030486,
0.534352034022757));
#17328=CARTESIAN_POINT('Ctrl Pts',(0.0505589280467443,-0.141716861518734,
0.542291023660064));
#17329=CARTESIAN_POINT('Ctrl Pts',(0.146487121137799,-0.0343714617774037,
0.550230013297369));
#17330=CARTESIAN_POINT('Ctrl Pts',(0.108316394245265,0.104438655591022,
0.558169002934674));
#17331=CARTESIAN_POINT('Ctrl Pts',(-0.0290105681715044,0.147642341414387,
0.566107992571982));
#17332=CARTESIAN_POINT('Ctrl Pts',(-0.139780343651344,0.0556895822633619,
0.574046982209285));
#17333=CARTESIAN_POINT('Ctrl Pts',(-0.122590794290966,-0.0872431727934394,
0.581985971846593));
#17334=CARTESIAN_POINT('Ctrl Pts',(0.00682222554696161,-0.150310782322966,
0.589924961483898));
#17335=CARTESIAN_POINT('Ctrl Pts',(0.129989965454297,-0.0757791721064987,
0.597863951121203));
#17336=CARTESIAN_POINT('Ctrl Pts',(0.134160800782372,0.0681230766876274,
0.60580294075851));
#17337=CARTESIAN_POINT('Ctrl Pts',(0.015516617634347,0.149663317553585,
0.613741930395814));
#17338=CARTESIAN_POINT('Ctrl Pts',(-0.117331965534667,0.0941970482962578,
0.621680920033121));
#17339=CARTESIAN_POINT('Ctrl Pts',(-0.142771175541451,-0.0475001629309618,
0.629619909670426));
#17340=CARTESIAN_POINT('Ctrl Pts',(-0.0375131590877193,-0.145714230393655,
0.637558899307733));
#17341=CARTESIAN_POINT('Ctrl Pts',(0.102085583566124,-0.110536906379362,
0.645497888945037));
#17342=CARTESIAN_POINT('Ctrl Pts',(0.148231970847143,0.0258293798362968,
0.653436878582344));
#17343=CARTESIAN_POINT('Ctrl Pts',(0.0586821478180281,0.138550639014834,
0.661375868219649));
#17344=CARTESIAN_POINT('Ctrl Pts',(-0.0845871597882484,0.124438283670714,
0.669314857856955));
#17345=CARTESIAN_POINT('Ctrl Pts',(-0.150422719745043,-0.00358879206139753,
0.67725384749426));
#17346=CARTESIAN_POINT('Ctrl Pts',(-0.078556588917505,-0.128330574617282,
0.685192837131567));
#17347=CARTESIAN_POINT('Ctrl Pts',(0.065222715229363,-0.135594511179713,
0.693131826768872));
#17348=CARTESIAN_POINT('Ctrl Pts',(0.149295093588351,-0.0187309656558678,
0.701070816406178));
#17349=CARTESIAN_POINT('Ctrl Pts',(0.0966980456281902,0.11527949520901,
0.709009806043483));
#17350=CARTESIAN_POINT('Ctrl Pts',(-0.044419435954706,0.14375947882982,
0.716948795680789));
#17351=CARTESIAN_POINT('Ctrl Pts',(-0.144873968183829,0.0406375120624596,
0.724887785318095));
#17352=CARTESIAN_POINT('Ctrl Pts',(-0.112706311402131,-0.099685311927494,
0.732826774955401));
#17353=CARTESIAN_POINT('Ctrl Pts',(0.0226362492002416,-0.148753064728429,
0.740765764592706));
#17354=CARTESIAN_POINT('Ctrl Pts',(0.137256875023267,-0.0616475814838108,
0.748704754230013));
#17355=CARTESIAN_POINT('Ctrl Pts',(0.126228238590478,0.0818920376245527,
0.756643743867318));
#17356=CARTESIAN_POINT('Ctrl Pts',(-0.000353699285724532,0.150465108715513,
0.764582733504624));
#17357=CARTESIAN_POINT('Ctrl Pts',(-0.126611849706441,0.0812976848247803,
0.772521723141928));
#17358=CARTESIAN_POINT('Ctrl Pts',(-0.136965528997667,-0.0622921978288208,
0.780460712779236));
#17359=CARTESIAN_POINT('Ctrl Pts',(-0.0219366533522686,-0.148857842533265,
0.788399702416541));
#17360=CARTESIAN_POINT('Ctrl Pts',(0.113173725020093,-0.0991543342927188,
0.796338692053846));
#17361=CARTESIAN_POINT('Ctrl Pts',(0.144681314438483,0.0413181715024817,
0.804277681691154));
#17362=CARTESIAN_POINT('Ctrl Pts',(0.0437430761464933,0.143966723006387,
0.812216671328456));
#17363=CARTESIAN_POINT('Ctrl Pts',(-0.0972389504488157,0.114823606281847,
0.820155660965765));
#17364=CARTESIAN_POINT('Ctrl Pts',(-0.149205382128735,-0.0194326526180533,
0.828094650603069));
#17365=CARTESIAN_POINT('Ctrl Pts',(-0.0645845121824554,-0.135899649852787,
0.836033640240376));
#17366=CARTESIAN_POINT('Ctrl Pts',(0.0791590524011713,-0.127959831458565,
0.843972629877681));
#17367=CARTESIAN_POINT('Ctrl Pts',(0.150437929635691,-0.00288155702400619,
0.851911619514986));
#17368=CARTESIAN_POINT('Ctrl Pts',(0.0840011924733913,0.12483458538003,
0.859850609152293));
#17369=CARTESIAN_POINT('Ctrl Pts',(-0.0593328794206009,0.138273220341526,
0.867789598789597));
#17370=CARTESIAN_POINT('Ctrl Pts',(-0.148351766552825,0.0251321985630355,
0.875728588426904));
#17371=CARTESIAN_POINT('Ctrl Pts',(-0.1015647786165,-0.111015628577859,
0.883667578064211));
#17372=CARTESIAN_POINT('Ctrl Pts',(0.0381978034543637,-0.145536256153639,
0.891606567701514));
#17373=CARTESIAN_POINT('Ctrl Pts',(0.142992914329196,-0.046828415471795,
0.899545557338823));
#17374=CARTESIAN_POINT('Ctrl Pts',(0.116887812080083,0.0947476302135675,
0.907484546976125));
#17375=CARTESIAN_POINT('Ctrl Pts',(-0.0162200712834111,0.149588713917584,
0.915423536613434));
#17376=CARTESIAN_POINT('Ctrl Pts',(-0.134479591021026,0.067491582014154,
0.923362526250738));
#17377=CARTESIAN_POINT('Ctrl Pts',(-0.129632261667175,-0.0763894677230377,
0.931301515888044));
#17378=CARTESIAN_POINT('Ctrl Pts',(-0.00611548103612966,-0.150341195071919,
0.93924050552535));
#17379=CARTESIAN_POINT('Ctrl Pts',(0.122999603362204,-0.0866658618874593,
0.947179495162656));
#17380=CARTESIAN_POINT('Ctrl Pts',(0.139516980595786,0.0563461282555487,
0.95511848479996));
#17381=CARTESIAN_POINT('Ctrl Pts',(0.0283161238170646,0.147777099632969,
0.963057474437267));
#17382=CARTESIAN_POINT('Ctrl Pts',(-0.108806203685475,0.103928264122473,
0.970996464074573));
#17383=CARTESIAN_POINT('Ctrl Pts',(-0.146323908690103,-0.0350597745230392,
0.978935453711877));
#17384=CARTESIAN_POINT('Ctrl Pts',(-0.049892103521326,-0.14195299239598,
0.986874443349185));
#17385=CARTESIAN_POINT('Ctrl Pts',(0.0922125030920605,-0.118897974404329,
0.994813432986488));
#17386=CARTESIAN_POINT('Ctrl Pts',(0.149902882860231,0.0129999905441286,
1.0027524226238));
#17387=CARTESIAN_POINT('Ctrl Pts',(0.0703674468853664,0.132997355096976,
1.0106914122611));
#17388=CARTESIAN_POINT('Ctrl Pts',(-0.0735845641169637,0.131244755962562,
1.01863040189841));
#17389=CARTESIAN_POINT('Ctrl Pts',(-0.150174949749745,0.00934657753497952,
1.02656939153571));
#17390=CARTESIAN_POINT('Ctrl Pts',(-0.0892904610481016,-0.121107752063083,
1.03450838117302));
#17391=CARTESIAN_POINT('Ctrl Pts',(0.0533333252681307,-0.140696234703703,
1.04244737081032));
#17392=CARTESIAN_POINT('Ctrl Pts',(0.147134107472884,-0.031486957015783,
1.05038636044763));
#17393=CARTESIAN_POINT('Ctrl Pts',(0.106243698045146,0.106546471877992,
1.05832535008494));
#17394=CARTESIAN_POINT('Ctrl Pts',(-0.0319055355867657,0.147043907874068,
1.06626433972224));
#17395=CARTESIAN_POINT('Ctrl Pts',(-0.14084743801815,0.0529327237885883,
1.07420332935955));
#17396=CARTESIAN_POINT('Ctrl Pts',(-0.120853163849259,-0.0896347412088629,
1.08214231899685));
#17397=CARTESIAN_POINT('Ctrl Pts',(0.00977389921538986,-0.150147743699608,
1.09008130863416));
#17398=CARTESIAN_POINT('Ctrl Pts',(0.13145362739741,-0.0732107771302755,
1.09802029827146));
#17399=CARTESIAN_POINT('Ctrl Pts',(0.132796568802552,0.0707456384395876,
1.10595928790877));
#17400=CARTESIAN_POINT('Ctrl Pts',(0.0125733526121963,0.149939270533256,
1.11389827754607));
#17401=CARTESIAN_POINT('Ctrl Pts',(-0.119159906186493,0.0918737764630459,
1.12183726718338));
#17402=CARTESIAN_POINT('Ctrl Pts',(-0.141810437433163,-0.0502958634379693,
1.12977625682069));
#17403=CARTESIAN_POINT('Ctrl Pts',(-0.0346432321137694,-0.146423087362162,
1.13771524645799));
#17404=CARTESIAN_POINT('Ctrl Pts',(0.104237477950025,-0.108510009835838,
1.1456542360953));
#17405=CARTESIAN_POINT('Ctrl Pts',(0.147695920811486,0.0287365450185451,
1.1535932257326));
#17406=CARTESIAN_POINT('Ctrl Pts',(0.0559488704325515,0.139676762352502,
1.16153221536991));
#17407=CARTESIAN_POINT('Ctrl Pts',(-0.0870155364008756,0.12275247642644,
1.16947120500722));
#17408=CARTESIAN_POINT('Ctrl Pts',(-0.150323183223479,-0.00654328889139735,
1.17741019464452));
#17409=CARTESIAN_POINT('Ctrl Pts',(-0.0760202581255566,-0.129849121670035,
1.18534918428183));
#17410=CARTESIAN_POINT('Ctrl Pts',(0.0678740032777675,-0.134286982701248,
1.19328817391913));
#17411=CARTESIAN_POINT('Ctrl Pts',(0.149634266389533,-0.0157943143574443,
1.20122716355644));
#17412=CARTESIAN_POINT('Ctrl Pts',(0.0944146137277022,0.117156966325547,
1.20916615319374));
#17413=CARTESIAN_POINT('Ctrl Pts',(-0.047235147145783,0.142859073628774,
1.21710514283105));
#17414=CARTESIAN_POINT('Ctrl Pts',(-0.145644368043342,0.037783489796601,
1.22504413246835));
#17415=CARTESIAN_POINT('Ctrl Pts',(-0.11072615165767,-0.101880289472715,
1.23298312210566));
#17416=CARTESIAN_POINT('Ctrl Pts',(0.0255542680118797,-0.148279646041953,
1.24092211174296));
#17417=CARTESIAN_POINT('Ctrl Pts',(0.138441506664824,-0.0589391489276913,
1.24886110138027));
#17418=CARTESIAN_POINT('Ctrl Pts',(0.124595033982396,0.0843560996663564,
1.25680009101758));
#17419=CARTESIAN_POINT('Ctrl Pts',(-0.00330965325590636,0.150429120316621,
1.26473908065488));
#17420=CARTESIAN_POINT('Ctrl Pts',(-0.128184579763139,0.0787945908985174,
1.27267807029219));
#17421=CARTESIAN_POINT('Ctrl Pts',(-0.135715308561414,-0.0649709863423027,
1.2806170599295));
#17422=CARTESIAN_POINT('Ctrl Pts',(-0.0190079735469551,-0.149260078337129,
1.2885560495668));
#17423=CARTESIAN_POINT('Ctrl Pts',(0.115099858543875,-0.0969117980795561,
1.29649503920411));
#17424=CARTESIAN_POINT('Ctrl Pts',(0.143841658454547,0.0441525915281748,
1.30443402884141));
#17425=CARTESIAN_POINT('Ctrl Pts',(0.0409062781470196,0.144798309552134,
1.31237301847872));
#17426=CARTESIAN_POINT('Ctrl Pts',(-0.0994759962839106,0.112891098884786,
1.32031200811602));
#17427=CARTESIAN_POINT('Ctrl Pts',(-0.148794813708878,-0.0223601759313527,
1.32825099775333));
#17428=CARTESIAN_POINT('Ctrl Pts',(-0.0619021766503053,-0.13714224202644,
1.33618998739064));
#17429=CARTESIAN_POINT('Ctrl Pts',(0.0816576604940555,-0.126379984705639,
1.34412897702794));
#17430=CARTESIAN_POINT('Ctrl Pts',(0.150465506209006,7.4487583413377E-5,
1.35206796666525));
#17431=CARTESIAN_POINT('Ctrl Pts',(0.0815324923277053,0.126460770918471,
1.36000695630255));
#17432=CARTESIAN_POINT('Ctrl Pts',(-0.062037929094705,0.137080886684378,
1.36794594593986));
#17433=CARTESIAN_POINT('Ctrl Pts',(-0.148816880822527,0.0222128430196456,
1.37588493557716));
#17434=CARTESIAN_POINT('Ctrl Pts',(-0.0993641722043223,-0.112989531455785,
1.38382392521447));
#17435=CARTESIAN_POINT('Ctrl Pts',(0.0410496166270677,-0.144757742348562,
1.39176291485178));
#17436=CARTESIAN_POINT('Ctrl Pts',(0.143885312916173,-0.0440101443352923,
1.39970190448908));
#17437=CARTESIAN_POINT('Ctrl Pts',(0.115003831846793,0.0970256929337524,
1.40764089412639));
#17438=CARTESIAN_POINT('Ctrl Pts',(-0.0191557100743377,0.149241218055048,
1.41557988376369));
#17439=CARTESIAN_POINT('Ctrl Pts',(-0.135779636557791,0.0648365220611291,
1.423518873401));
#17440=CARTESIAN_POINT('Ctrl Pts',(-0.128106375355825,-0.0789213496179777,
1.4314578630383));
#17441=CARTESIAN_POINT('Ctrl Pts',(-0.00316095527563228,-0.150432546011701,
1.43939685267561));
#17442=CARTESIAN_POINT('Ctrl Pts',(0.12467895337041,-0.0842322751882648,
1.44733584231291));
#17443=CARTESIAN_POINT('Ctrl Pts',(0.138382210043398,0.0590753877074232,
1.45527483195022));
#17444=CARTESIAN_POINT('Ctrl Pts',(0.0254091034322018,0.148306397458819,
1.46321382158753));
#17445=CARTESIAN_POINT('Ctrl Pts',(-0.110830116988615,0.101767718932792,
1.47115281122483));
#17446=CARTESIAN_POINT('Ctrl Pts',(-0.145600909330124,-0.0379221829034233,
1.47909180086214));
#17447=CARTESIAN_POINT('Ctrl Pts',(-0.0471050325108872,-0.142916194795756,
1.48703079049945));
#17448=CARTESIAN_POINT('Ctrl Pts',(0.0945521370959566,-0.117043625665234,
1.49496978013675));
#17449=CARTESIAN_POINT('Ctrl Pts',(0.14957741911039,0.0159047428854941,
1.50290876977406));
#17450=CARTESIAN_POINT('Ctrl Pts',(0.0678206238522695,0.134426714629862,
1.51084775941136));
#17451=CARTESIAN_POINT('Ctrl Pts',(-0.0763126473618499,0.129627546381738,
1.51878674904867));
#17452=CARTESIAN_POINT('Ctrl Pts',(-0.125385920115907,0.0477050348167321,
1.52407940880687));
#17453=CARTESIAN_POINT('Ctrl Pts',(-0.127184992207234,0.00540996832206346,
1.52672573868597));
#17454=CARTESIAN_POINT('Ctrl Pts',(0.0684664424539414,-0.095829519891843,
-1.38777878078145E-17));
#17455=CARTESIAN_POINT('Ctrl Pts',(0.100334321247169,-0.0730611673843044,
0.00264632987910189));
#17456=CARTESIAN_POINT('Ctrl Pts',(0.139021564822767,0.00636891437108143,
0.00793898963730573));
#17457=CARTESIAN_POINT('Ctrl Pts',(0.0699018669780613,0.120491966796142,
0.0158779792746114));
#17458=CARTESIAN_POINT('Ctrl Pts',(-0.0632645460347191,0.123954346655885,
0.0238169689119172));
#17459=CARTESIAN_POINT('Ctrl Pts',(-0.138486976988987,0.0141253725679007,
0.0317559585492228));
#17460=CARTESIAN_POINT('Ctrl Pts',(-0.0869496735326521,-0.108728403071097,
0.0396949481865287));
#17461=CARTESIAN_POINT('Ctrl Pts',(0.0441923146003338,-0.131999388615902,
0.0476339378238343));
#17462=CARTESIAN_POINT('Ctrl Pts',(0.134874939024977,-0.034459980695041,
0.0555729274611401));
#17463=CARTESIAN_POINT('Ctrl Pts',(0.102091080224759,0.094638871230671,
0.0635119170984456));
#17464=CARTESIAN_POINT('Ctrl Pts',(-0.0241513666277066,0.137095110112719,
0.0714509067357516));
#17465=CARTESIAN_POINT('Ctrl Pts',(-0.128284260007319,0.0540539703915629,
0.0793898963730571));
#17466=CARTESIAN_POINT('Ctrl Pts',(-0.114982038412656,-0.0784718756714057,
0.0873288860103631));
#17467=CARTESIAN_POINT('Ctrl Pts',(0.00357853460314598,-0.139161043603659,
0.0952678756476685));
#17468=CARTESIAN_POINT('Ctrl Pts',(0.118863112008681,-0.0724583686054966,
0.103206865284975));
#17469=CARTESIAN_POINT('Ctrl Pts',(0.125336705278751,0.0605752693714656,
0.11114585492228));
#17470=CARTESIAN_POINT('Ctrl Pts',(0.0170731091066207,0.138156245709763,
0.119084844559586));
#17471=CARTESIAN_POINT('Ctrl Pts',(-0.106819734848208,0.0892647286947484,
0.127023834196891));
#17472=CARTESIAN_POINT('Ctrl Pts',(-0.132926439498961,-0.0413425724611633,
0.134962823834197));
#17473=CARTESIAN_POINT('Ctrl Pts',(-0.0373480950846616,-0.134103559412242,
0.142901813471503));
#17474=CARTESIAN_POINT('Ctrl Pts',(0.0924198687735613,-0.104101940294199,
0.150840803108809));
#17475=CARTESIAN_POINT('Ctrl Pts',(0.137583777756591,0.0211978768359354,
0.158779792746114));
#17476=CARTESIAN_POINT('Ctrl Pts',(0.0567991668878991,0.127092487218924,
0.16671878238342));
#17477=CARTESIAN_POINT('Ctrl Pts',(-0.075981188277068,0.116642637502503,
0.174657772020726));
#17478=CARTESIAN_POINT('Ctrl Pts',(-0.139205973057234,-0.000585553717998882,
0.182596761658032));
#17479=CARTESIAN_POINT('Ctrl Pts',(-0.0749972298318695,-0.11727771015962,
0.190535751295337));
#17480=CARTESIAN_POINT('Ctrl Pts',(0.0578663373665801,-0.126610160769685,
0.198474740932643));
#17481=CARTESIAN_POINT('Ctrl Pts',(0.13775723856723,-0.0200396862227523,
0.206413730569949));
#17482=CARTESIAN_POINT('Ctrl Pts',(0.091540828968026,0.104875747581476,
0.214352720207254));
#17483=CARTESIAN_POINT('Ctrl Pts',(-0.0384749358425138,0.133784622116252,
0.22229170984456));
#17484=CARTESIAN_POINT('Ctrl Pts',(-0.133269533752038,0.0402228439430644,
0.230230699481866));
#17485=CARTESIAN_POINT('Ctrl Pts',(-0.106065007067505,-0.0901601911982067,
0.238169689119172));
#17486=CARTESIAN_POINT('Ctrl Pts',(0.0182347644767634,-0.138007750384372,
0.246108678756477));
#17487=CARTESIAN_POINT('Ctrl Pts',(0.125841858853055,-0.0595186723796334,
0.254047668393783));
#17488=CARTESIAN_POINT('Ctrl Pts',(0.118249355954961,0.073455671106145,
0.261986658031089));
#17489=CARTESIAN_POINT('Ctrl Pts',(0.00240767183786234,0.139186381940956,
0.269925647668394));
#17490=CARTESIAN_POINT('Ctrl Pts',(-0.115638070838342,0.0775014991741366,
0.277864637305701));
#17491=CARTESIAN_POINT('Ctrl Pts',(-0.12782508485658,-0.0551306945617612,
0.285803626943006));
#17492=CARTESIAN_POINT('Ctrl Pts',(-0.0229969941138309,-0.137294515779738,
0.293742616580312));
#17493=CARTESIAN_POINT('Ctrl Pts',(0.102883268653204,-0.0937746172089793,
0.301681606217617));
#17494=CARTESIAN_POINT('Ctrl Pts',(0.134580950019115,0.0355895166223291,
0.309620595854923));
#17495=CARTESIAN_POINT('Ctrl Pts',(0.0430789950773988,0.13237388709478,
0.317559585492229));
#17496=CARTESIAN_POINT('Ctrl Pts',(-0.0878588274613298,0.107979036106918,
0.325498575129534));
#17497=CARTESIAN_POINT('Ctrl Pts',(-0.1383679148179,-0.0152632221501787,
0.33343756476684));
#17498=CARTESIAN_POINT('Ctrl Pts',(-0.0622106591311991,-0.12453304658572,
0.341376554404146));
#17499=CARTESIAN_POINT('Ctrl Pts',(0.0708961914151981,-0.119801401679107,
0.349315544041452));
#17500=CARTESIAN_POINT('Ctrl Pts',(0.1391024375543,-0.00539978406154301,
0.357254533678757));
#17501=CARTESIAN_POINT('Ctrl Pts',(0.0799699354250877,0.113944965792994,
0.365193523316063));
#17502=CARTESIAN_POINT('Ctrl Pts',(-0.0523695618881846,0.128980908622551,
0.373132512953369));
#17503=CARTESIAN_POINT('Ctrl Pts',(-0.136768314413298,0.0259436692471295,
0.381071502590675));
#17504=CARTESIAN_POINT('Ctrl Pts',(-0.0959650484377783,-0.100843221288265,
0.38901049222798));
#17505=CARTESIAN_POINT('Ctrl Pts',(0.0326876424682324,-0.135315053971568,
0.396949481865287));
#17506=CARTESIAN_POINT('Ctrl Pts',(0.13141703692502,-0.0459152284901983,
0.404888471502591));
#17507=CARTESIAN_POINT('Ctrl Pts',(0.109843140674695,0.0855168418978295,
0.412827461139898));
#17508=CARTESIAN_POINT('Ctrl Pts',(-0.0122846228212416,0.13866410438033,
0.420766450777203));
#17509=CARTESIAN_POINT('Ctrl Pts',(-0.123166656044517,0.0648738825743514,
0.428705440414509));
#17510=CARTESIAN_POINT('Ctrl Pts',(-0.121298056821252,-0.0683039326309071,
0.436644430051815));
#17511=CARTESIAN_POINT('Ctrl Pts',(-0.00838939967687663,-0.138954178686792,
0.44458341968912));
#17512=CARTESIAN_POINT('Ctrl Pts',(0.11219917790857,-0.0824013973067221,
0.452522409326426));
#17513=CARTESIAN_POINT('Ctrl Pts',(0.13007709763057,0.0495842159710775,
0.460461398963732));
#17514=CARTESIAN_POINT('Ctrl Pts',(0.0288783492374893,0.136178877755608,
0.468400388601037));
#17515=CARTESIAN_POINT('Ctrl Pts',(-0.0987565487199846,0.0981111099028881,
0.476339378238344));
#17516=CARTESIAN_POINT('Ctrl Pts',(-0.135986594552616,-0.0297706550724338,
0.484278367875649));
#17517=CARTESIAN_POINT('Ctrl Pts',(-0.0487302328423073,-0.130399425645183,
0.492217357512954));
#17518=CARTESIAN_POINT('Ctrl Pts',(0.0831353173341669,-0.111656458896056,
0.50015634715026));
#17519=CARTESIAN_POINT('Ctrl Pts',(0.13889618212661,0.00930034365552528,
0.508095336787567));
#17520=CARTESIAN_POINT('Ctrl Pts',(0.0675071113591811,0.12174331898465,
0.516034326424871));
#17521=CARTESIAN_POINT('Ctrl Pts',(-0.0656800932930844,0.122738629397884,
0.523973316062178));
#17522=CARTESIAN_POINT('Ctrl Pts',(-0.138741673886299,0.0113751364249866,
0.531912305699483));
#17523=CARTESIAN_POINT('Ctrl Pts',(-0.0847947606245053,-0.110401514355972,
0.539851295336789));
#17524=CARTESIAN_POINT('Ctrl Pts',(0.0467759446245483,-0.131113145053959,
0.547790284974095));
#17525=CARTESIAN_POINT('Ctrl Pts',(0.135526478334676,-0.031799677225719,
0.555729274611401));
#17526=CARTESIAN_POINT('Ctrl Pts',(0.100211809365564,0.0966242157284558,
0.563668264248707));
#17527=CARTESIAN_POINT('Ctrl Pts',(-0.0268399031138932,0.136595261273209,
0.571607253886012));
#17528=CARTESIAN_POINT('Ctrl Pts',(-0.129321523751272,0.0515227066069736,
0.579546243523318));
#17529=CARTESIAN_POINT('Ctrl Pts',(-0.113418152377209,-0.0807153548762533,
0.587485233160623));
#17530=CARTESIAN_POINT('Ctrl Pts',(0.00631176444456456,-0.139064040754811,
0.595424222797929));
#17531=CARTESIAN_POINT('Ctrl Pts',(0.120263693490807,-0.0701091280034811,
0.603363212435234));
#17532=CARTESIAN_POINT('Ctrl Pts',(0.124122453355413,0.0630258865426945,
0.611302202072541));
#17533=CARTESIAN_POINT('Ctrl Pts',(0.0143556138404206,0.138465021405133,
0.619241191709845));
#17534=CARTESIAN_POINT('Ctrl Pts',(-0.108552806291007,0.0871489187988374,
0.627180181347153));
#17535=CARTESIAN_POINT('Ctrl Pts',(-0.132088571872698,-0.043946046262323,
0.635119170984457));
#17536=CARTESIAN_POINT('Ctrl Pts',(-0.0347063025259737,-0.134811417789573,
0.643058160621763));
#17537=CARTESIAN_POINT('Ctrl Pts',(0.0944472082050275,-0.102266175560326,
0.65099715025907));
#17538=CARTESIAN_POINT('Ctrl Pts',(0.137140772714236,0.0238967416356601,
0.658936139896373));
#17539=CARTESIAN_POINT('Ctrl Pts',(0.054291358674537,0.128183829614862,
0.666875129533682));
#17540=CARTESIAN_POINT('Ctrl Pts',(-0.0782580734018908,0.115127406593233,
0.674814119170985));
#17541=CARTESIAN_POINT('Ctrl Pts',(-0.139167602654929,-0.00332026696803425,
0.682753108808293));
#17542=CARTESIAN_POINT('Ctrl Pts',(-0.0726787294560835,-0.118728463672822,
0.690692098445597));
#17543=CARTESIAN_POINT('Ctrl Pts',(0.0603425395611779,-0.125448888878168,
0.698631088082904));
#17544=CARTESIAN_POINT('Ctrl Pts',(0.138124349154501,-0.0173294538893964,
0.706570077720209));
#17545=CARTESIAN_POINT('Ctrl Pts',(0.0894627833767505,0.106653908470079,
0.714509067357515));
#17546=CARTESIAN_POINT('Ctrl Pts',(-0.0410958292974484,0.133002927094911,
0.72244805699482));
#17547=CARTESIAN_POINT('Ctrl Pts',(-0.134034026730954,0.0375968812502473,
0.730387046632127));
#17548=CARTESIAN_POINT('Ctrl Pts',(-0.104273258644039,-0.0922265326964679,
0.738326036269432));
#17549=CARTESIAN_POINT('Ctrl Pts',(0.0209425314183671,-0.137622876656644,
0.746265025906738));
#17550=CARTESIAN_POINT('Ctrl Pts',(0.126986869252672,-0.0570349089493802,
0.754204015544043));
#17551=CARTESIAN_POINT('Ctrl Pts',(0.11678343126468,0.0757646090434518,
0.762143005181349));
#17552=CARTESIAN_POINT('Ctrl Pts',(-0.000327234354877375,0.139206819944772,
0.770081994818654));
#17553=CARTESIAN_POINT('Ctrl Pts',(-0.117138339349379,0.0752147276530931,
0.778020984455961));
#17554=CARTESIAN_POINT('Ctrl Pts',(-0.126717322684213,-0.0576312930030564,
0.785959974093266));
#17555=CARTESIAN_POINT('Ctrl Pts',(-0.0202952816069424,-0.137719814645367,
0.793898963730571));
#17556=CARTESIAN_POINT('Ctrl Pts',(0.104705698854998,-0.0917352845351548,
0.801837953367879));
#17557=CARTESIAN_POINT('Ctrl Pts',(0.133855787965376,0.0382266115373486,
0.809776943005182));
#17558=CARTESIAN_POINT('Ctrl Pts',(0.0404700769297216,0.133194664588195,
0.81771593264249));
#17559=CARTESIAN_POINT('Ctrl Pts',(-0.0899632159395838,0.106232130635072,
0.825654922279794));
#17560=CARTESIAN_POINT('Ctrl Pts',(-0.13804135019805,-0.0179786383510676,
0.833593911917101));
#17561=CARTESIAN_POINT('Ctrl Pts',(-0.059752088941783,-0.125731196083361,
0.841532901554406));
#17562=CARTESIAN_POINT('Ctrl Pts',(0.0732361146625898,-0.118385460722959,
0.849471891191712));
#17563=CARTESIAN_POINT('Ctrl Pts',(0.139181674492094,-0.00266594955618734,
0.857410880829018));
#17564=CARTESIAN_POINT('Ctrl Pts',(0.077715950067195,0.115494055719818,
0.865349870466323));
#17565=CARTESIAN_POINT('Ctrl Pts',(-0.0548934004223171,0.127927168308903,
0.87328886010363));
#17566=CARTESIAN_POINT('Ctrl Pts',(-0.137251604915624,0.0232517257326144,
0.881227849740934));
#17567=CARTESIAN_POINT('Ctrl Pts',(-0.0939653715754795,-0.102709078207047,
0.889166839378241));
#17568=CARTESIAN_POINT('Ctrl Pts',(0.0353397195745277,-0.134646760160997,
0.897105829015547));
#17569=CARTESIAN_POINT('Ctrl Pts',(0.132293719443212,-0.0433245611326863,
0.905044818652852));
#17570=CARTESIAN_POINT('Ctrl Pts',(0.108141885842356,0.0876583043865096,
0.912983808290157));
#17571=CARTESIAN_POINT('Ctrl Pts',(-0.0150064327997127,0.138395999855801,
0.920922797927463));
#17572=CARTESIAN_POINT('Ctrl Pts',(-0.124417390671652,0.0624416423544169,
0.928861787564769));
#17573=CARTESIAN_POINT('Ctrl Pts',(-0.119932754264349,-0.0706737593172073,
0.936800777202075));
#17574=CARTESIAN_POINT('Ctrl Pts',(-0.00565790085648466,-0.139092177922979,
0.944739766839381));
#17575=CARTESIAN_POINT('Ctrl Pts',(0.113796373024222,-0.0801812402497705,
0.952678756476687));
#17576=CARTESIAN_POINT('Ctrl Pts',(0.129077866376032,0.0521301276928276,
0.960617746113992));
#17577=CARTESIAN_POINT('Ctrl Pts',(0.026197419344502,0.13671993644362,0.968556735751298));
#17578=CARTESIAN_POINT('Ctrl Pts',(-0.100664969670515,0.0961520134094621,
0.976495725388603));
#17579=CARTESIAN_POINT('Ctrl Pts',(-0.13537547797311,-0.0324364881732178,
0.98443471502591));
#17580=CARTESIAN_POINT('Ctrl Pts',(-0.0461590140787468,-0.131331607851033,
0.992373704663214));
#17581=CARTESIAN_POINT('Ctrl Pts',(0.0853128637208732,-0.110001641284132,
1.00031269430052));
#17582=CARTESIAN_POINT('Ctrl Pts',(0.138686661656432,0.0120272889735618,
1.00825168393783));
#17583=CARTESIAN_POINT('Ctrl Pts',(0.0651023256631918,0.123046060459907,
1.01619067357513));
#17584=CARTESIAN_POINT('Ctrl Pts',(-0.0680787277209358,0.121424596492465,
1.02412966321244));
#17585=CARTESIAN_POINT('Ctrl Pts',(-0.138938371616466,0.00864723620724691,
1.03206865284975));
#17586=CARTESIAN_POINT('Ctrl Pts',(-0.0826094583655966,-0.112046076191904,
1.04000764248705));
#17587=CARTESIAN_POINT('Ctrl Pts',(0.0493427524230464,-0.130168884856471,
1.04794663212436));
#17588=CARTESIAN_POINT('Ctrl Pts',(0.136125055048066,-0.0291310004912345,
1.05588562176166));
#17589=CARTESIAN_POINT('Ctrl Pts',(0.0982941990358779,0.0985743183458784,
1.06382461139897));
#17590=CARTESIAN_POINT('Ctrl Pts',(-0.0295182596522469,0.136041604476578,
1.07176360103627));
#17591=CARTESIAN_POINT('Ctrl Pts',(-0.130308774647192,0.0489721252490281,
1.07970259067358));
#17592=CARTESIAN_POINT('Ctrl Pts',(-0.111810537096203,-0.0829279783650712,
1.08764158031088));
#17593=CARTESIAN_POINT('Ctrl Pts',(0.00904258428980543,-0.13891320121148,
1.09558056994819));
#17594=CARTESIAN_POINT('Ctrl Pts',(0.121617839487272,-0.067732908692211,
1.1035195595855));
#17595=CARTESIAN_POINT('Ctrl Pts',(0.122860297649024,0.0654522196953821,
1.1114585492228));
#17596=CARTESIAN_POINT('Ctrl Pts',(0.0116325734791967,0.138720326685422,
1.11939753886011));
#17597=CARTESIAN_POINT('Ctrl Pts',(-0.110243974478508,0.0849994817198388,
1.12733652849741));
#17598=CARTESIAN_POINT('Ctrl Pts',(-0.131199719314147,-0.0465325633653302,
1.13527551813472));
#17599=CARTESIAN_POINT('Ctrl Pts',(-0.0320511128216771,-0.13546723577438,
1.14321450777202));
#17600=CARTESIAN_POINT('Ctrl Pts',(0.0964380908528195,-0.100390938007982,
1.15115349740933));
#17601=CARTESIAN_POINT('Ctrl Pts',(0.136644831685568,0.0265863832644056,
1.15909248704664));
#17602=CARTESIAN_POINT('Ctrl Pts',(0.0517625939920979,0.129225692742072,
1.16703147668394));
#17603=CARTESIAN_POINT('Ctrl Pts',(-0.0805047509788913,0.113567736929491,
1.17497046632125));
#17604=CARTESIAN_POINT('Ctrl Pts',(-0.139075513779617,-0.00605369873671642,
1.18290945595855));
#17605=CARTESIAN_POINT('Ctrl Pts',(-0.0703321751825429,-0.12013338809653,
1.19084844559586));
#17606=CARTESIAN_POINT('Ctrl Pts',(0.0627954496153871,-0.124239193932754,
1.19878743523316));
#17607=CARTESIAN_POINT('Ctrl Pts',(0.138438143943654,-0.0146125323915816,
1.20672642487047));
#17608=CARTESIAN_POINT('Ctrl Pts',(0.0873502052771435,0.108390901091839,
1.21466541450777));
#17609=CARTESIAN_POINT('Ctrl Pts',(-0.043700859820065,0.132169893139269,
1.22260440414508));
#17610=CARTESIAN_POINT('Ctrl Pts',(-0.134746782767514,0.0349564062120582,
1.23054339378239));
#17611=CARTESIAN_POINT('Ctrl Pts',(-0.102441260891455,-0.0942572748833364,
1.23848238341969));
#17612=CARTESIAN_POINT('Ctrl Pts',(0.0236422145726536,-0.137184880695923,
1.246421373057));
#17613=CARTESIAN_POINT('Ctrl Pts',(0.128082862902196,-0.0545291301253663,
1.2543603626943));
#17614=CARTESIAN_POINT('Ctrl Pts',(0.115272428336817,0.0780443019497631,
1.26229935233161));
#17615=CARTESIAN_POINT('Ctrl Pts',(-0.00306201423577413,0.139173524314926,
1.27023834196891));
#17616=CARTESIAN_POINT('Ctrl Pts',(-0.118593392628464,0.0728989233548558,
1.27817733160622));
#17617=CARTESIAN_POINT('Ctrl Pts',(-0.125560647806918,-0.06010964584811,
1.28611632124353));
#17618=CARTESIAN_POINT('Ctrl Pts',(-0.0175857351491984,-0.138091953858251,
1.29405531088083));
#17619=CARTESIAN_POINT('Ctrl Pts',(0.106487712804436,-0.089660542174548,
1.30199430051814));
#17620=CARTESIAN_POINT('Ctrl Pts',(0.133078957772855,0.0408489510387311,
1.30993329015544));
#17621=CARTESIAN_POINT('Ctrl Pts',(0.0378455373822902,0.133964029124136,
1.31787227979275));
#17622=CARTESIAN_POINT('Ctrl Pts',(-0.0920328787300654,0.104444219726284,
1.32581126943006));
#17623=CARTESIAN_POINT('Ctrl Pts',(-0.137661501842601,-0.0206871148492911,
1.33375025906736));
#17624=CARTESIAN_POINT('Ctrl Pts',(-0.0572704544775333,-0.126880813469472,
1.34168924870467));
#17625=CARTESIAN_POINT('Ctrl Pts',(0.0755477687720905,-0.116923823242002,
1.34962823834197));
#17626=CARTESIAN_POINT('Ctrl Pts',(0.13920718769651,6.89141801743488E-5,
1.35756722797928));
#17627=CARTESIAN_POINT('Ctrl Pts',(0.0754319660950179,0.116998564767658,
1.36550621761658));
#17628=CARTESIAN_POINT('Ctrl Pts',(-0.0573960494825499,0.126824048933643,
1.37344520725389));
#17629=CARTESIAN_POINT('Ctrl Pts',(-0.13768191782304,0.0205508058651932,
1.38138419689119));
#17630=CARTESIAN_POINT('Ctrl Pts',(-0.0919294216917856,-0.104535287252199,
1.3893231865285));
#17631=CARTESIAN_POINT('Ctrl Pts',(0.0379781508110965,-0.133926497290667,
1.39726217616581));
#17632=CARTESIAN_POINT('Ctrl Pts',(0.133119345865688,-0.0407171622080862,
1.40520116580311));
#17633=CARTESIAN_POINT('Ctrl Pts',(0.106398871137127,0.0897659150453452,
1.41314015544042));
#17634=CARTESIAN_POINT('Ctrl Pts',(-0.0177224175491345,0.138074504763813,
1.42107914507772));
#17635=CARTESIAN_POINT('Ctrl Pts',(-0.125620162573399,0.0599852426217579,
1.42901813471503));
#17636=CARTESIAN_POINT('Ctrl Pts',(-0.118521039729242,-0.0730161975746823,
1.43695712435233));
#17637=CARTESIAN_POINT('Ctrl Pts',(-0.00292444232197888,-0.139176693688359,
1.44489611398964));
#17638=CARTESIAN_POINT('Ctrl Pts',(0.115350068603298,-0.0779297424218237,
1.45283510362695));
#17639=CARTESIAN_POINT('Ctrl Pts',(0.128028003046829,0.0546551750765237,
1.46077409326425));
#17640=CARTESIAN_POINT('Ctrl Pts',(0.0235079116789307,0.137209630484779,
1.46871308290156));
#17641=CARTESIAN_POINT('Ctrl Pts',(-0.102537447198224,0.0941531272373115,
1.47665207253886));
#17642=CARTESIAN_POINT('Ctrl Pts',(-0.134706575776555,-0.0350847218495708,
1.48459106217617));
#17643=CARTESIAN_POINT('Ctrl Pts',(-0.0435804807853106,-0.132222740314769,
1.49253005181348));
#17644=CARTESIAN_POINT('Ctrl Pts',(0.0874774386997331,-0.108286040948335,
1.50046904145078));
#17645=CARTESIAN_POINT('Ctrl Pts',(0.138385550162814,0.0147146982980264,
1.50840803108809));
#17646=CARTESIAN_POINT('Ctrl Pts',(0.0627460642121078,0.124368470664037,
1.51634702072539));
#17647=CARTESIAN_POINT('Ctrl Pts',(-0.0706026869052757,0.119928391791904,
1.5242860103627));
#17648=CARTESIAN_POINT('Ctrl Pts',(-0.116004137797729,0.0441355889673283,
1.5295786701209));
#17649=CARTESIAN_POINT('Ctrl Pts',(-0.117668597464313,0.00500517689812487,
1.532225));
#17650=CARTESIAN_POINT('',(0.0684664424539461,-0.0958295198918396,0.));
#17651=CARTESIAN_POINT('Ctrl Pts',(0.0684664424539414,-0.095829519891843,
-1.38777878078145E-17));
#17652=CARTESIAN_POINT('Ctrl Pts',(0.100334321247169,-0.0730611673843044,
0.00264632987910189));
#17653=CARTESIAN_POINT('Ctrl Pts',(0.139021564822767,0.00636891437108143,
0.00793898963730573));
#17654=CARTESIAN_POINT('Ctrl Pts',(0.0699018669780613,0.120491966796142,
0.0158779792746114));
#17655=CARTESIAN_POINT('Ctrl Pts',(-0.0632645460347191,0.123954346655885,
0.0238169689119172));
#17656=CARTESIAN_POINT('Ctrl Pts',(-0.11596266760442,0.0470121293552651,
0.0293787386625077));
#17657=CARTESIAN_POINT('Ctrl Pts',(-0.117944740497024,0.00404481602818191,
0.0322941785339964));
#17658=CARTESIAN_POINT('Ctrl Pts',(-0.117917485785546,7.60014832213644E-5,
0.0325632885263832));
#17659=CARTESIAN_POINT('Ctrl Pts',(0.0635546915223951,0.132092229195826,
-2.16840434497101E-19));
#17660=CARTESIAN_POINT('Ctrl Pts',(0.0668114782730532,0.13015255741457,
-1.00603861447787E-18));
#17661=CARTESIAN_POINT('Ctrl Pts',(0.0699821360194518,0.12808121947321,
-2.9262196004085E-17));
#17662=CARTESIAN_POINT('Ctrl Pts',(0.0730575207853233,0.125877721325919,
-2.71050543121376E-17));
#17663=CARTESIAN_POINT('Ctrl Pts',(0.0789281193465506,0.121671466161783,
-2.36378102375718E-17));
#17664=CARTESIAN_POINT('Ctrl Pts',(0.0844522091809674,0.11698398814956,
1.43782932504085E-18));
#17665=CARTESIAN_POINT('Ctrl Pts',(0.0895990070394484,0.111875963994554,
9.97465998686664E-18));
#17666=CARTESIAN_POINT('Ctrl Pts',(0.0928865546640729,0.108613183302742,
1.54276111490851E-17));
#17667=CARTESIAN_POINT('Ctrl Pts',(0.0960206821069302,0.105176950779614,
-2.53636710091701E-17));
#17668=CARTESIAN_POINT('Ctrl Pts',(0.098978417360439,0.101599719103904,
-1.56125112837913E-17));
#17669=CARTESIAN_POINT('Ctrl Pts',(0.103148772110026,0.0965558852815647,
-1.86354736740503E-18));
#17670=CARTESIAN_POINT('Ctrl Pts',(0.106976174326278,0.0912251680483688,
1.1337629845105E-17));
#17671=CARTESIAN_POINT('Ctrl Pts',(0.110435561611279,0.0856523061447448,
2.03830008427275E-17));
#17672=CARTESIAN_POINT('Ctrl Pts',(0.112407683932559,0.0824753373788608,
2.55395723911076E-17));
#17673=CARTESIAN_POINT('Ctrl Pts',(0.114261188142284,0.0792174064057451,
2.29308760465575E-17));
#17674=CARTESIAN_POINT('Ctrl Pts',(0.115986535786665,0.0758936579718971,
2.08166817117217E-17));
#17675=CARTESIAN_POINT('Ctrl Pts',(0.120573220307724,0.0670577659456877,
1.51962825639422E-17));
#17676=CARTESIAN_POINT('Ctrl Pts',(0.124235263225439,0.0578042025119142,
2.52358375750583E-18));
#17677=CARTESIAN_POINT('Ctrl Pts',(0.126883306113679,0.0482911783993335,
1.30104260698261E-17));
#17678=CARTESIAN_POINT('Ctrl Pts',(0.128478610866444,0.0425600882242624,
1.93281898253259E-17));
#17679=CARTESIAN_POINT('Ctrl Pts',(0.129704960854084,0.0367345196138549,
-5.78096029915021E-19));
#17680=CARTESIAN_POINT('Ctrl Pts',(0.130533291754837,0.0308494671050701,
0.));
#17681=CARTESIAN_POINT('Ctrl Pts',(0.131003715791213,0.0275072397983871,
3.2831114661813E-19));
#17682=CARTESIAN_POINT('Ctrl Pts',(0.131345346899704,0.0241444941465381,
-1.7128612844445E-18));
#17683=CARTESIAN_POINT('Ctrl Pts',(0.131551728167405,0.0207857616715298,
2.60208521396521E-18));
#17684=CARTESIAN_POINT('Ctrl Pts',(0.131851321606701,0.0159100565018035,
8.86587880453295E-18));
#17685=CARTESIAN_POINT('Ctrl Pts',(0.131867617692795,0.0110341713389591,
-1.68111772803455E-17));
#17686=CARTESIAN_POINT('Ctrl Pts',(0.131586936334964,0.0061777758930637,
-6.93889390390723E-18));
#17687=CARTESIAN_POINT('Ctrl Pts',(0.131099036368572,-0.00226395031615145,
9.98510028643051E-18));
#17688=CARTESIAN_POINT('Ctrl Pts',(0.129715139118287,-0.0106479390144509,
1.03491660509995E-17));
#17689=CARTESIAN_POINT('Ctrl Pts',(0.127493709984164,-0.018859987399606,
1.04083408558608E-17));
#17690=CARTESIAN_POINT('Ctrl Pts',(0.126553994220251,-0.0223338732882013,
1.04333731632617E-17));
#17691=CARTESIAN_POINT('Ctrl Pts',(0.125463061762623,-0.0257782540966497,
1.75224609115742E-17));
#17692=CARTESIAN_POINT('Ctrl Pts',(0.124232565886791,-0.0291638780753137,
1.73472347597681E-17));
#17693=CARTESIAN_POINT('Ctrl Pts',(0.12170396813588,-0.0361211392462112,
1.69871551674183E-17));
#17694=CARTESIAN_POINT('Ctrl Pts',(0.118582485980247,-0.0428512226170345,
-6.45748389186585E-19));
#17695=CARTESIAN_POINT('Ctrl Pts',(0.114911168983798,-0.0492778939609075,
3.46944695195361E-18));
#17696=CARTESIAN_POINT('Ctrl Pts',(0.112347970921096,-0.0537647937721124,
6.34254691478841E-18));
#17697=CARTESIAN_POINT('Ctrl Pts',(0.109516356061708,-0.0581036184196785,
-1.05628593522785E-17));
#17698=CARTESIAN_POINT('Ctrl Pts',(0.106427098863261,-0.0622637901458048,
-1.21430643318376E-17));
#17699=CARTESIAN_POINT('Ctrl Pts',(0.104287070791936,-0.0651456752410043,
-1.32377232732828E-17));
#17700=CARTESIAN_POINT('Ctrl Pts',(0.102021590876101,-0.067943056099314,
-1.03088264066386E-17));
#17701=CARTESIAN_POINT('Ctrl Pts',(0.0996491962474235,-0.0706287444932102,
-1.04083408558608E-17));
#17702=CARTESIAN_POINT('Ctrl Pts',(0.0938611946766418,-0.0771810981592459,
-1.06511292104842E-17));
#17703=CARTESIAN_POINT('Ctrl Pts',(0.0874218747326319,-0.0830961188460978,
9.460259835177E-18));
#17704=CARTESIAN_POINT('Ctrl Pts',(0.0803902102994179,-0.0882260767030795,
2.94902990916057E-17));
#17705=CARTESIAN_POINT('Ctrl Pts',(0.0765868618375105,-0.091000813397402,
4.03243227742548E-17));
#17706=CARTESIAN_POINT('Ctrl Pts',(0.0726097989303321,-0.0935451549285004,
-2.49510848448888E-18));
#17707=CARTESIAN_POINT('Ctrl Pts',(0.0684664424539416,-0.0958295198918429,
0.));
#17708=CARTESIAN_POINT('Ctrl Pts',(-0.00156962371674571,0.146072546381438,
1.50365));
#17709=CARTESIAN_POINT('Ctrl Pts',(0.0218361081466035,0.146362061217761,
1.50238307892777));
#17710=CARTESIAN_POINT('Ctrl Pts',(0.0452966847593804,0.141345883428421,
1.50111615785553));
#17711=CARTESIAN_POINT('Ctrl Pts',(0.0660179268768178,0.130913916311315,
1.4998492367833));
#17712=CARTESIAN_POINT('Ctrl Pts',(0.109300214423576,0.109123745727819,
1.4972029069042));
#17713=CARTESIAN_POINT('Ctrl Pts',(0.140630685714559,0.0637042888941242,
1.49455657702509));
#17714=CARTESIAN_POINT('Ctrl Pts',(0.145752650840527,0.0155206226173656,
1.49191024714599));
#17715=CARTESIAN_POINT('Ctrl Pts',(0.150874615966495,-0.0326630436593903,
1.48926391726689));
#17716=CARTESIAN_POINT('Ctrl Pts',(0.129788074927449,-0.0836109193792113,
1.48661758738779));
#17717=CARTESIAN_POINT('Ctrl Pts',(0.0921021927661857,-0.114042242015571,
1.48397125750869));
#17718=CARTESIAN_POINT('Ctrl Pts',(0.0544163106049216,-0.144473564651931,
1.48132492762959));
#17719=CARTESIAN_POINT('Ctrl Pts',(0.000131087321441313,-0.154388334204831,
1.47867859775048));
#17720=CARTESIAN_POINT('Ctrl Pts',(-0.0458840977328367,-0.139228052523514,
1.47603226787138));
#17721=CARTESIAN_POINT('Ctrl Pts',(-0.0918992827871148,-0.124067770842196,
1.47338593799228));
#17722=CARTESIAN_POINT('Ctrl Pts',(-0.129644429612189,-0.0838324379266627,
1.47073960811318));
#17723=CARTESIAN_POINT('Ctrl Pts',(-0.141854649713415,-0.0369491035797489,
1.46809327823408));
#17724=CARTESIAN_POINT('Ctrl Pts',(-0.14497337938942,-0.0249741805295802,
1.46741735368415));
#17725=CARTESIAN_POINT('Ctrl Pts',(-0.146426231435716,-0.0125655473306973,
1.46674142913422));
#17726=CARTESIAN_POINT('Ctrl Pts',(-0.14631473222987,-0.000131398079681141,
1.46606550458429));
#17727=CARTESIAN_POINT('Origin',(0.,0.,-0.0924367114736175));
#17728=CARTESIAN_POINT('',(-0.0684664424539507,-0.0958295198918364,0.));
#17729=CARTESIAN_POINT('Ctrl Pts',(-0.0686146973663072,-0.0959584553529141,
8.16675286424706E-17));
#17730=CARTESIAN_POINT('Ctrl Pts',(-0.0391968190522335,-0.116741470120209,
0.00244290680874874));
#17731=CARTESIAN_POINT('Ctrl Pts',(0.0436301113039178,-0.130476273073809,
0.0075332029917574));
#17732=CARTESIAN_POINT('Ctrl Pts',(0.134092250525203,-0.0374520209666004,
0.0152708885490261));
#17733=CARTESIAN_POINT('Ctrl Pts',(0.104134301645602,0.0924305194826295,
0.023213056671806));
#17734=CARTESIAN_POINT('Ctrl Pts',(-0.0212379681243542,0.137589894578696,
0.0311552247945861));
#17735=CARTESIAN_POINT('Ctrl Pts',(-0.106685947947232,0.0723488109778776,
0.0375631097285225));
#17736=CARTESIAN_POINT('Ctrl Pts',(-0.117663533972591,0.0165813593984342,
0.041323605288199));
#17737=CARTESIAN_POINT('Ctrl Pts',(-0.117600989619072,5.04992496179954E-5,
0.0424367114736154));
#17738=CARTESIAN_POINT('Origin',(0.,0.,0.));
#17739=CARTESIAN_POINT('Ctrl Pts',(-0.0510216505388318,0.106149619882943,
-0.0164977839420939));
#17740=CARTESIAN_POINT('Ctrl Pts',(-0.0863355867949722,0.0891756983861136,
-0.0138503945678339));
#17741=CARTESIAN_POINT('Ctrl Pts',(-0.13808023131828,0.0175094743621551,
-0.00855561581931395));
#17742=CARTESIAN_POINT('Ctrl Pts',(-0.0894531427980795,-0.106808298616542,
-0.000613447696533924));
#17743=CARTESIAN_POINT('Ctrl Pts',(0.0412394829729132,-0.132934609947913,
0.00732872042624606));
#17744=CARTESIAN_POINT('Ctrl Pts',(0.134092250525203,-0.0374520209666004,
0.0152708885490261));
#17745=CARTESIAN_POINT('Ctrl Pts',(0.104134301645602,0.0924305194826295,
0.023213056671806));
#17746=CARTESIAN_POINT('Ctrl Pts',(-0.0212379681243542,0.137589894578696,
0.0311552247945861));
#17747=CARTESIAN_POINT('Ctrl Pts',(-0.127145335141994,0.0567276974868182,
0.039097392917366));
#17748=CARTESIAN_POINT('Ctrl Pts',(-0.116579117211717,-0.0761160149501382,
0.0470395610401461));
#17749=CARTESIAN_POINT('Ctrl Pts',(0.000787973702835166,-0.139222729671589,
0.054981729162926));
#17750=CARTESIAN_POINT('Ctrl Pts',(0.117431922513572,-0.0747907597173192,
0.0629238972857061));
#17751=CARTESIAN_POINT('Ctrl Pts',(0.126496838785129,0.0581591461343325,
0.070866065408486));
#17752=CARTESIAN_POINT('Ctrl Pts',(0.0196773008918215,0.137828289815661,
0.0788082335312661));
#17753=CARTESIAN_POINT('Ctrl Pts',(-0.105168479521776,0.0912330920368172,
0.0867504016540459));
#17754=CARTESIAN_POINT('Ctrl Pts',(-0.133669226619255,-0.0389412707994331,
0.0946925697768262));
#17755=CARTESIAN_POINT('Ctrl Pts',(-0.0397151780004399,-0.133441281507892,
0.102634737899606));
#17756=CARTESIAN_POINT('Ctrl Pts',(0.0906220264938673,-0.105695447092796,
0.110576906022386));
#17757=CARTESIAN_POINT('Ctrl Pts',(0.137940159127448,0.0188783162799928,
0.118519074145166));
#17758=CARTESIAN_POINT('Ctrl Pts',(0.0588909273047484,0.126157580947307,
0.126461242267946));
#17759=CARTESIAN_POINT('Ctrl Pts',(-0.074108440039672,0.117863552156501,
0.134403410390726));
#17760=CARTESIAN_POINT('Ctrl Pts',(-0.139216864956951,0.00159439502933392,
0.142345578513506));
#17761=CARTESIAN_POINT('Ctrl Pts',(-0.0767883381764272,-0.116135388594389,
0.150287746636286));
#17762=CARTESIAN_POINT('Ctrl Pts',(0.0559861945572589,-0.127473226882309,
0.158229914759066));
#17763=CARTESIAN_POINT('Ctrl Pts',(0.137471621702818,-0.0220324926503626,
0.166172082881846));
#17764=CARTESIAN_POINT('Ctrl Pts',(0.0930189202108026,0.103592267873211,
0.174114251004626));
#17765=CARTESIAN_POINT('Ctrl Pts',(-0.0366486683060043,0.134315868829211,
0.182056419127406));
#17766=CARTESIAN_POINT('Ctrl Pts',(-0.132742311638566,0.0419923350165386,
0.189998587250186));
#17767=CARTESIAN_POINT('Ctrl Pts',(-0.107230360350792,-0.0888004916405464,
0.197940755372966));
#17768=CARTESIAN_POINT('Ctrl Pts',(0.0165156171993534,-0.138242945169174,
0.205882923495746));
#17769=CARTESIAN_POINT('Ctrl Pts',(0.125131592687617,-0.061040658666823,
0.213825091618526));
#17770=CARTESIAN_POINT('Ctrl Pts',(0.119114174013628,0.0720811421096423,
0.221767259741306));
#17771=CARTESIAN_POINT('Ctrl Pts',(0.0039759348809324,0.139169211541763,
0.229709427864086));
#17772=CARTESIAN_POINT('Ctrl Pts',(-0.114804669066963,0.0787639858025777,
0.237651595986866));
#17773=CARTESIAN_POINT('Ctrl Pts',(-0.128412401817242,-0.0537971426620367,
0.245593764109646));
#17774=CARTESIAN_POINT('Ctrl Pts',(-0.024381182195918,-0.137074561658528,
0.253535932232426));
#17775=CARTESIAN_POINT('Ctrl Pts',(0.101985705091022,-0.094777599970642,
0.261478100355206));
#17776=CARTESIAN_POINT('Ctrl Pts',(0.134923209124943,0.0343453801629359,
0.269420268477986));
#17777=CARTESIAN_POINT('Ctrl Pts',(0.0442571924125319,0.132004463632409,
0.277362436600766));
#17778=CARTESIAN_POINT('Ctrl Pts',(-0.0869529592639067,0.108733897080731,
0.285304604723546));
#17779=CARTESIAN_POINT('Ctrl Pts',(-0.138505267237684,-0.0141480898545381,
0.293246772846326));
#17780=CARTESIAN_POINT('Ctrl Pts',(-0.0631725212350128,-0.124068972994571,
0.301188940969106));
#17781=CARTESIAN_POINT('Ctrl Pts',(0.0700327441786229,-0.12032993078169,
0.309131109091886));
#17782=CARTESIAN_POINT('Ctrl Pts',(0.139080821187468,-0.00635631000930847,
0.317073277214666));
#17783=CARTESIAN_POINT('Ctrl Pts',(0.0807165776729536,0.11344034374014,
0.325015445337446));
#17784=CARTESIAN_POINT('Ctrl Pts',(-0.0515923433190751,0.129313988454311,
0.332957613460226));
#17785=CARTESIAN_POINT('Ctrl Pts',(-0.136637377548019,0.026722734813544,
0.340899781583006));
#17786=CARTESIAN_POINT('Ctrl Pts',(-0.0965085366518414,-0.100349289247285,
0.348841949705786));
#17787=CARTESIAN_POINT('Ctrl Pts',(0.0320320385160992,-0.135491055083419,
0.356784117828566));
#17788=CARTESIAN_POINT('Ctrl Pts',(0.131227975626944,-0.0465090949381858,
0.364726285951346));
#17789=CARTESIAN_POINT('Ctrl Pts',(0.110205605501345,0.0850799742312894,
0.372668454074126));
#17790=CARTESIAN_POINT('Ctrl Pts',(-0.0117764211155082,0.138727046407055,
0.380610622196906));
#17791=CARTESIAN_POINT('Ctrl Pts',(-0.122970036152848,0.065285892102983,
0.388552790319686));
#17792=CARTESIAN_POINT('Ctrl Pts',(-0.121510464882371,-0.0679638464419502,
0.396494958442466));
#17793=CARTESIAN_POINT('Ctrl Pts',(-0.00873482453528946,-0.138951719454826,
0.404437126565246));
#17794=CARTESIAN_POINT('Ctrl Pts',(0.112042812448737,-0.0826455423945668,
0.412379294688026));
#17795=CARTESIAN_POINT('Ctrl Pts',(0.130177722634257,0.049372441998279,
0.420321462810806));
#17796=CARTESIAN_POINT('Ctrl Pts',(0.0290564652212241,0.136160197297018,
0.428263630933586));
#17797=CARTESIAN_POINT('Ctrl Pts',(-0.098683499418539,0.098211223603141,
0.436205799056366));
#17798=CARTESIAN_POINT('Ctrl Pts',(-0.136019240449831,-0.0297093205335648,
0.444147967179146));
#17799=CARTESIAN_POINT('Ctrl Pts',(-0.0487473834415776,-0.130413074907061,
0.452090135301926));
#17800=CARTESIAN_POINT('Ctrl Pts',(0.0831820848081396,-0.111645054821459,
0.460032303424706));
#17801=CARTESIAN_POINT('Ctrl Pts',(0.138908217753341,0.00940130521287039,
0.467974471547486));
#17802=CARTESIAN_POINT('Ctrl Pts',(0.0673801526530663,0.121835103839429,
0.475916639670265));
#17803=CARTESIAN_POINT('Ctrl Pts',(-0.0658750545035054,0.12265543075329,
0.483858807793047));
#17804=CARTESIAN_POINT('Ctrl Pts',(-0.138781944133385,0.0111107822259715,
0.491800975915825));
#17805=CARTESIAN_POINT('Ctrl Pts',(-0.084550315326251,-0.110612484274364,
0.499743144038607));
#17806=CARTESIAN_POINT('Ctrl Pts',(0.0471380885036503,-0.131003351527116,
0.507685312161385));
#17807=CARTESIAN_POINT('Ctrl Pts',(0.135643160584381,-0.031381690295376,
0.515627480284167));
#17808=CARTESIAN_POINT('Ctrl Pts',(0.0998851624184703,0.0969888232104648,
0.523569648406945));
#17809=CARTESIAN_POINT('Ctrl Pts',(-0.0273779061153799,0.136507610615132,
0.531511816529727));
#17810=CARTESIAN_POINT('Ctrl Pts',(-0.129560000008381,0.0509714027366644,
0.539453984652505));
#17811=CARTESIAN_POINT('Ctrl Pts',(-0.113051823689188,-0.0812598465397498,
0.547396152775286));
#17812=CARTESIAN_POINT('Ctrl Pts',(0.00702343738442799,-0.139048728244533,
0.555338320898066));
#17813=CARTESIAN_POINT('Ctrl Pts',(0.12066450826877,-0.0694546898587181,
0.563280489020846));
#17814=CARTESIAN_POINT('Ctrl Pts',(0.123764493242992,0.063766979789076,
0.571222657143626));
#17815=CARTESIAN_POINT('Ctrl Pts',(0.0134834875971477,0.13857154491934,
0.579164825266405));
#17816=CARTESIAN_POINT('Ctrl Pts',(-0.109149777898995,0.0864303389077871,
0.587106993389186));
#17817=CARTESIAN_POINT('Ctrl Pts',(-0.131790633456927,-0.0448899368693808,
0.595049161511966));
#17818=CARTESIAN_POINT('Ctrl Pts',(-0.0336977294021144,-0.135086418755761,
0.602991329634746));
#17819=CARTESIAN_POINT('Ctrl Pts',(0.0952657566843092,-0.101529863106778,
0.610933497757526));
#17820=CARTESIAN_POINT('Ctrl Pts',(0.136956022624868,0.025038477707157,
0.618875665880307));
#17821=CARTESIAN_POINT('Ctrl Pts',(0.0531805018142573,0.128669000640787,
0.626817834003085));
#17822=CARTESIAN_POINT('Ctrl Pts',(-0.0793138220987445,0.114425500318782,
0.634760002125867));
#17823=CARTESIAN_POINT('Ctrl Pts',(-0.139148536750765,-0.00464351367351466,
0.642702170248646));
#17824=CARTESIAN_POINT('Ctrl Pts',(-0.0715088964667609,-0.119458592094588,
0.650644338371427));
#17825=CARTESIAN_POINT('Ctrl Pts',(0.0616402393688536,-0.124837327709565,
0.658586506494205));
#17826=CARTESIAN_POINT('Ctrl Pts',(0.138320583400205,-0.0158522461166236,
0.666528674616987));
#17827=CARTESIAN_POINT('Ctrl Pts',(0.0882850628235238,0.107655121482266,
0.674470842739765));
#17828=CARTESIAN_POINT('Ctrl Pts',(-0.0426286451686149,0.132539337972556,
0.682413010862546));
#17829=CARTESIAN_POINT('Ctrl Pts',(-0.13449013477919,0.0360039045964495,
0.690355178985326));
#17830=CARTESIAN_POINT('Ctrl Pts',(-0.103144844235522,-0.0935148042116587,
0.698297347108106));
#17831=CARTESIAN_POINT('Ctrl Pts',(0.022691720100341,-0.137364345221032,
0.706239515230886));
#17832=CARTESIAN_POINT('Ctrl Pts',(0.127740337615313,-0.0553740340325759,
0.714181683353665));
#17833=CARTESIAN_POINT('Ctrl Pts',(0.115765682611161,0.077344581120379,
0.722123851476446));
#17834=CARTESIAN_POINT('Ctrl Pts',(-0.00226223072526165,0.139207614056346,
0.730066019599226));
#17835=CARTESIAN_POINT('Ctrl Pts',(-0.118217708309552,0.0735421711751344,
0.738008187722006));
#17836=CARTESIAN_POINT('Ctrl Pts',(-0.125873620115675,-0.059495455776806,
0.745950355844786));
#17837=CARTESIAN_POINT('Ctrl Pts',(-0.0182163644075178,-0.138029133036789,
0.753892523967566));
#17838=CARTESIAN_POINT('Ctrl Pts',(0.106128952536144,-0.0901139441634624,
0.761834692090347));
#17839=CARTESIAN_POINT('Ctrl Pts',(0.133249245915149,0.0403548753208232,
0.769776860213125));
#17840=CARTESIAN_POINT('Ctrl Pts',(0.0382995408207276,0.133854483197375,
0.777719028335907));
#17841=CARTESIAN_POINT('Ctrl Pts',(-0.0917364783268051,0.104729633071593,
0.785661196458685));
#17842=CARTESIAN_POINT('Ctrl Pts',(-0.137732458880487,-0.0203383202317681,
0.793603364581467));
#17843=CARTESIAN_POINT('Ctrl Pts',(-0.0575513573065257,-0.126774282767806,
0.801545532704245));
#17844=CARTESIAN_POINT('Ctrl Pts',(0.0753527000357912,-0.117071978271622,
0.809487700827026));
#17845=CARTESIAN_POINT('Ctrl Pts',(0.139225942868322,-0.000119714417332432,
0.817429868949805));
#17846=CARTESIAN_POINT('Ctrl Pts',(0.0755539188089132,0.116942220141962,
0.825372037072586));
#17847=CARTESIAN_POINT('Ctrl Pts',(-0.0573332568284509,0.12687306712048,
0.833314205195366));
#17848=CARTESIAN_POINT('Ctrl Pts',(-0.13769727914169,0.0205751504512258,
0.841256373318145));
#17849=CARTESIAN_POINT('Ctrl Pts',(-0.0919164475821765,-0.104571717796869,
0.849198541440926));
#17850=CARTESIAN_POINT('Ctrl Pts',(0.0380692928980519,-0.133920149482284,
0.857140709563706));
#17851=CARTESIAN_POINT('Ctrl Pts',(0.133179650076608,-0.0405839661022353,
0.865082877686486));
#17852=CARTESIAN_POINT('Ctrl Pts',(0.106283765719693,0.0899312995767124,
0.873025045809266));
#17853=CARTESIAN_POINT('Ctrl Pts',(-0.0179789669825735,0.138060255849953,
0.880967213932046));
#17854=CARTESIAN_POINT('Ctrl Pts',(-0.125771118879347,0.0597118342956578,
0.888909382054826));
#17855=CARTESIAN_POINT('Ctrl Pts',(-0.118344004924669,-0.0733387619032726,
0.896851550177606));
#17856=CARTESIAN_POINT('Ctrl Pts',(-0.00250162451743248,-0.139203517821528,
0.904793718300386));
#17857=CARTESIAN_POINT('Ctrl Pts',(0.115632500949424,-0.0775435504945224,
0.912735886423165));
#17858=CARTESIAN_POINT('Ctrl Pts',(0.127835376168433,0.0551542754370876,
0.920678054545947));
#17859=CARTESIAN_POINT('Ctrl Pts',(0.0229279137899797,0.137325118854324,
0.928620222668725));
#17860=CARTESIAN_POINT('Ctrl Pts',(-0.102983873094174,0.0936920454555137,
0.936562390791507));
#17861=CARTESIAN_POINT('Ctrl Pts',(-0.134551852288801,-0.0357725669300891,
0.944504558914285));
#17862=CARTESIAN_POINT('Ctrl Pts',(-0.0428565117498991,-0.132465832952297,
0.952446727037066));
#17863=CARTESIAN_POINT('Ctrl Pts',(0.0880997963686447,-0.107806787258123,
0.960388895159846));
#17864=CARTESIAN_POINT('Ctrl Pts',(0.138347640177547,0.0156143509765511,
0.968331063282625));
#17865=CARTESIAN_POINT('Ctrl Pts',(0.061854832590724,0.124731139593481,
0.976273231405407));
#17866=CARTESIAN_POINT('Ctrl Pts',(-0.0713033562375951,0.119581390225944,
0.984215399528185));
#17867=CARTESIAN_POINT('Ctrl Pts',(-0.139140345480169,0.00488280234845834,
0.992157567650966));
#17868=CARTESIAN_POINT('Ctrl Pts',(-0.0795104838321055,-0.114288934109561,
1.00009973577375));
#17869=CARTESIAN_POINT('Ctrl Pts',(0.0529591494285269,-0.128760265574912,
1.00804190389653));
#17870=CARTESIAN_POINT('Ctrl Pts',(0.136912761112491,-0.0252739657289669,
1.0159840720193));
#17871=CARTESIAN_POINT('Ctrl Pts',(0.0954402180350474,0.101365883217864,
1.02392624014209));
#17872=CARTESIAN_POINT('Ctrl Pts',(-0.0334653697086341,0.135144169424284,
1.03186840826486));
#17873=CARTESIAN_POINT('Ctrl Pts',(-0.131713240771149,0.0451165125500212,
1.03981057638765));
#17874=CARTESIAN_POINT('Ctrl Pts',(-0.109298251871946,-0.0862425048155002,
1.04775274451043));
#17875=CARTESIAN_POINT('Ctrl Pts',(0.0132451643780021,-0.13859452774087,
1.05569491263321));
#17876=CARTESIAN_POINT('Ctrl Pts',(0.123654649330263,-0.0639797248987874,
1.06363708075599));
#17877=CARTESIAN_POINT('Ctrl Pts',(0.120783771971213,0.0692470788374567,
1.07157924887876));
#17878=CARTESIAN_POINT('Ctrl Pts',(0.00726255089817806,0.139036444335888,
1.07952141700155));
#17879=CARTESIAN_POINT('Ctrl Pts',(-0.112911912907791,0.0814541430660127,
1.08746358512433));
#17880=CARTESIAN_POINT('Ctrl Pts',(-0.129647464608677,-0.0507485213543897,
1.09540575324711));
#17881=CARTESIAN_POINT('Ctrl Pts',(-0.0276126195379174,-0.136460326620484,
1.10334792136989));
#17882=CARTESIAN_POINT('Ctrl Pts',(0.0997182217817603,-0.0971604536002107,
1.11129008949267));
#17883=CARTESIAN_POINT('Ctrl Pts',(0.135696927507188,0.0311483765905046,
1.11923225761545));
#17884=CARTESIAN_POINT('Ctrl Pts',(0.0473633069609982,0.130922093830007,
1.12717442573822));
#17885=CARTESIAN_POINT('Ctrl Pts',(-0.0843599685788644,0.110757722983492,
1.13511659386101));
#17886=CARTESIAN_POINT('Ctrl Pts',(-0.138800846271631,-0.0108721006891078,
1.14305876198379));
#17887=CARTESIAN_POINT('Ctrl Pts',(-0.0660858892268601,-0.122541963197144,
1.15100093010657));
#17888=CARTESIAN_POINT('Ctrl Pts',(0.0671705316110708,-0.121950798202395,
1.15894309822935));
#17889=CARTESIAN_POINT('Ctrl Pts',(0.138891844802359,-0.00964017357273747,
1.16688526635212));
#17890=CARTESIAN_POINT('Ctrl Pts',(0.0833739592533277,0.111501840422208,
1.17482743447491));
#17891=CARTESIAN_POINT('Ctrl Pts',(-0.0485230383040216,0.130496713571114,
1.18276960259768));
#17892=CARTESIAN_POINT('Ctrl Pts',(-0.135967947813762,0.0299431906521225,
1.19071177072047));
#17893=CARTESIAN_POINT('Ctrl Pts',(-0.0988522486080867,-0.0980413710850678,
1.19865393884324));
#17894=CARTESIAN_POINT('Ctrl Pts',(0.0288222657999454,-0.136209964735594,
1.20659610696603));
#17895=CARTESIAN_POINT('Ctrl Pts',(0.130092623711363,-0.0495962373069701,
1.21453827508881));
#17896=CARTESIAN_POINT('Ctrl Pts',(0.112184773380136,0.082452738709893,
1.22248044321158));
#17897=CARTESIAN_POINT('Ctrl Pts',(-0.00849585454694533,0.138966535376798,
1.23042261133437));
#17898=CARTESIAN_POINT('Ctrl Pts',(-0.121393406896754,0.0681727090639588,
1.23836477945715));
#17899=CARTESIAN_POINT('Ctrl Pts',(-0.123082127310551,-0.0650743223999996,
1.24630694757992));
#17900=CARTESIAN_POINT('Ctrl Pts',(-0.0120149744006178,-0.138706589206355,
1.25424911570271));
#17901=CARTESIAN_POINT('Ctrl Pts',(0.110059129405696,-0.0852693704304675,
1.26219128382548));
#17902=CARTESIAN_POINT('Ctrl Pts',(0.13130776387206,0.0462833517151888,
1.27013345194827));
#17903=CARTESIAN_POINT('Ctrl Pts',(0.0322649968732001,0.135435768819968,
1.27807562007105));
#17904=CARTESIAN_POINT('Ctrl Pts',(-0.0963358219719167,0.100515107841202,
1.28601778819382));
#17905=CARTESIAN_POINT('Ctrl Pts',(-0.136683130933199,-0.0264877182308561,
1.29395995631661));
#17906=CARTESIAN_POINT('Ctrl Pts',(-0.0518146499729274,-0.129225073214149,
1.30190212443939));
#17907=CARTESIAN_POINT('Ctrl Pts',(0.0805213734929343,-0.11357898534207,
1.30984429256217));
#17908=CARTESIAN_POINT('Ctrl Pts',(0.1390915465469,0.0061171215252809,1.31778646068495));
#17909=CARTESIAN_POINT('Ctrl Pts',(0.0702395735793815,0.120209316621791,
1.32572862880773));
#17910=CARTESIAN_POINT('Ctrl Pts',(-0.0629590648350173,0.124177428154433,
1.33367079693051));
#17911=CARTESIAN_POINT('Ctrl Pts',(-0.138480731711197,0.0143862582011507,
1.34161296505328));
#17912=CARTESIAN_POINT('Ctrl Pts',(-0.0871398218994898,-0.108584202098263,
1.34955513317607));
#17913=CARTESIAN_POINT('Ctrl Pts',(0.0440301174146577,-0.132080378229483,
1.35749730129884));
#17914=CARTESIAN_POINT('Ctrl Pts',(0.13486394497766,-0.0345773583278084,
1.36543946942163));
#17915=CARTESIAN_POINT('Ctrl Pts',(0.102148545386143,0.0946020732301706,
1.3733816375444));
#17916=CARTESIAN_POINT('Ctrl Pts',(-0.0241454188302812,0.137116288461919,
1.38132380566719));
#17917=CARTESIAN_POINT('Ctrl Pts',(-0.128319693277533,0.0540178939468163,
1.38926597378996));
#17918=CARTESIAN_POINT('Ctrl Pts',(-0.114939956470138,-0.0785664351508689,
1.39720814191275));
#17919=CARTESIAN_POINT('Ctrl Pts',(0.00373660876362508,-0.139175849115243,
1.40515031003553));
#17920=CARTESIAN_POINT('Ctrl Pts',(0.118990018389619,-0.0722858665142316,
1.41309247815831));
#17921=CARTESIAN_POINT('Ctrl Pts',(0.125236419206141,0.0608253567263532,
1.42103464628109));
#17922=CARTESIAN_POINT('Ctrl Pts',(0.0167532566496359,0.13821437898841,
1.42897681440387));
#17923=CARTESIAN_POINT('Ctrl Pts',(-0.107077349343502,0.0889846891406984,
1.43691898252665));
#17924=CARTESIAN_POINT('Ctrl Pts',(-0.132814597987359,-0.0417638487589672,
1.44486115064943));
#17925=CARTESIAN_POINT('Ctrl Pts',(-0.0368790902657646,-0.134252921254984,
1.45280331877221));
#17926=CARTESIAN_POINT('Ctrl Pts',(0.0928396680879532,-0.103751556080299,
1.46074548689499));
#17927=CARTESIAN_POINT('Ctrl Pts',(0.137511141307062,0.0217950526079239,
1.46868765501776));
#17928=CARTESIAN_POINT('Ctrl Pts',(0.0562018483347667,0.127378648737854,
1.47662982314055));
#17929=CARTESIAN_POINT('Ctrl Pts',(-0.0765818961642769,0.116263681173923,
1.48457199126332));
#17930=CARTESIAN_POINT('Ctrl Pts',(-0.13923195096087,-0.00134816270381636,
1.49251415938611));
#17931=CARTESIAN_POINT('Ctrl Pts',(-0.0742871760264013,-0.117748889605885,
1.50045632750888));
#17932=CARTESIAN_POINT('Ctrl Pts',(0.0586284551779338,-0.126233948370975,
1.50839849563167));
#17933=CARTESIAN_POINT('Ctrl Pts',(0.137995068118234,-0.019163470063063,
1.51634066375444));
#17934=CARTESIAN_POINT('Ctrl Pts',(0.0906261803825392,0.105639137646141,
1.52428283187723));
#17935=CARTESIAN_POINT('Ctrl Pts',(0.00417072711528833,0.124051375507138,
1.52957761062575));
#17936=CARTESIAN_POINT('Ctrl Pts',(-0.0334019664627544,0.1129391839063,
1.53222500000001));
#17937=CARTESIAN_POINT('Ctrl Pts',(-0.0551480035117261,0.114734422509858,
-0.0109985226280628));
#17938=CARTESIAN_POINT('Ctrl Pts',(-0.093317938433455,0.0963877427684319,
-0.00835113325380276));
#17939=CARTESIAN_POINT('Ctrl Pts',(-0.149247407742026,0.0189255452031589,
-0.00305635450528277));
#17940=CARTESIAN_POINT('Ctrl Pts',(-0.0966876253720675,-0.115446371588928,
0.00488581361749726));
#17941=CARTESIAN_POINT('Ctrl Pts',(0.0445747075563756,-0.143685636564375,
0.0128279817402772));
#17942=CARTESIAN_POINT('Ctrl Pts',(0.144936900801175,-0.0404809362687151,
0.0207701498630572));
#17943=CARTESIAN_POINT('Ctrl Pts',(0.112556116319125,0.0999057960529736,
0.0287123179858373));
#17944=CARTESIAN_POINT('Ctrl Pts',(-0.0229555792165621,0.148717415239805,
0.0366544861086172));
#17945=CARTESIAN_POINT('Ctrl Pts',(-0.137428156769908,0.0613155244327884,
0.0445966542313972));
#17946=CARTESIAN_POINT('Ctrl Pts',(-0.126007400730642,-0.0822718633254329,
0.0525388223541772));
#17947=CARTESIAN_POINT('Ctrl Pts',(0.000851700720621877,-0.150482305134309,
0.0604809904769572));
#17948=CARTESIAN_POINT('Ctrl Pts',(0.126929176276611,-0.0808394286734405,
0.0684231585997372));
#17949=CARTESIAN_POINT('Ctrl Pts',(0.136727213562698,0.0628627408439891,
0.0763653267225173));
#17950=CARTESIAN_POINT('Ctrl Pts',(0.0212686937255662,0.148975090584026,
0.0843074948452972));
#17951=CARTESIAN_POINT('Ctrl Pts',(-0.113673932864549,0.0986115272026031,
0.0922496629680772));
#17952=CARTESIAN_POINT('Ctrl Pts',(-0.144479665027646,-0.0420906285100245,
0.100191831090857));
#17953=CARTESIAN_POINT('Ctrl Pts',(-0.0429271251068198,-0.144233284958223,
0.108133999213637));
#17954=CARTESIAN_POINT('Ctrl Pts',(0.0979510420095061,-0.114243518700172,
0.116076167336417));
#17955=CARTESIAN_POINT('Ctrl Pts',(0.149096007275942,0.0204050915936607,
0.124018335459197));
#17956=CARTESIAN_POINT('Ctrl Pts',(0.0636537044864716,0.136360518400275,
0.131960503581977));
#17957=CARTESIAN_POINT('Ctrl Pts',(-0.0801019266996435,0.127395713772213,
0.139902671704757));
#17958=CARTESIAN_POINT('Ctrl Pts',(-0.15047596611352,0.00172334100814176,
0.147844839827537));
#17959=CARTESIAN_POINT('Ctrl Pts',(-0.0829985603893774,-0.125527785761544,
0.155787007950317));
#17960=CARTESIAN_POINT('Ctrl Pts',(0.0605140527882773,-0.137782566606816,
0.163729176073097));
#17961=CARTESIAN_POINT('Ctrl Pts',(0.148589577098441,-0.0238143605552183,
0.171671344195877));
#17962=CARTESIAN_POINT('Ctrl Pts',(0.100541783424623,0.111970245809892,
0.179613512318657));
#17963=CARTESIAN_POINT('Ctrl Pts',(-0.0396126128240685,0.145178604134651,
0.187555680441437));
#17964=CARTESIAN_POINT('Ctrl Pts',(-0.143477786216001,0.0453884461694337,
0.195497848564217));
#17965=CARTESIAN_POINT('Ctrl Pts',(-0.115902567375552,-0.095982191346566,
0.203440016686997));
#17966=CARTESIAN_POINT('Ctrl Pts',(0.0178513102906219,-0.149423281002214,
0.211382184809777));
#17967=CARTESIAN_POINT('Ctrl Pts',(0.135251553802876,-0.0659772944027704,
0.219324352932557));
#17968=CARTESIAN_POINT('Ctrl Pts',(0.128747479107914,0.07791067196398,0.227266521055337));
#17969=CARTESIAN_POINT('Ctrl Pts',(0.00429748682099232,0.150424458749874,
0.235208689178117));
#17970=CARTESIAN_POINT('Ctrl Pts',(-0.124089444892588,0.0851339876261335,
0.243150857300897));
#17971=CARTESIAN_POINT('Ctrl Pts',(-0.138797696890977,-0.0581479623084488,
0.251093025423677));
#17972=CARTESIAN_POINT('Ctrl Pts',(-0.0263529993083425,-0.148160405002171,
0.259035193546457));
#17973=CARTESIAN_POINT('Ctrl Pts',(0.110233752987369,-0.102442695616748,
0.266977361669237));
#17974=CARTESIAN_POINT('Ctrl Pts',(0.145835062802846,0.0371230472913779,
0.274919529792017));
#17975=CARTESIAN_POINT('Ctrl Pts',(0.0478364728857143,0.142680265085169,
0.282861697914797));
#17976=CARTESIAN_POINT('Ctrl Pts',(-0.0939852406223356,0.117527701960322,
0.290803866037577));
#17977=CARTESIAN_POINT('Ctrl Pts',(-0.14970681824969,-0.01529231023972,
0.298746034160357));
#17978=CARTESIAN_POINT('Ctrl Pts',(-0.0682815703945392,-0.134102995221473,
0.306688202283137));
#17979=CARTESIAN_POINT('Ctrl Pts',(0.0756966107742644,-0.1300615596562,
0.314630370405917));
#17980=CARTESIAN_POINT('Ctrl Pts',(0.150328919865546,-0.00687037371415525,
0.322572538528697));
#17981=CARTESIAN_POINT('Ctrl Pts',(0.0872444944832666,0.122614780370367,
0.330514706651477));
#17982=CARTESIAN_POINT('Ctrl Pts',(-0.0557648508131485,0.139772198940638,
0.338456874774257));
#17983=CARTESIAN_POINT('Ctrl Pts',(-0.147687863823926,0.0288839239377102,
0.346399042897038));
#17984=CARTESIAN_POINT('Ctrl Pts',(-0.104313621021262,-0.10846499275041,
0.354341211019817));
#17985=CARTESIAN_POINT('Ctrl Pts',(0.0346226151823369,-0.146448833047075,
0.362283379142597));
#17986=CARTESIAN_POINT('Ctrl Pts',(0.141840978962514,-0.0502704970123603,
0.370225547265377));
#17987=CARTESIAN_POINT('Ctrl Pts',(0.119118434135606,0.0919607787700563,
0.378167715388157));
#17988=CARTESIAN_POINT('Ctrl Pts',(-0.0127288338612142,0.149946533709345,
0.386109883510937));
#17989=CARTESIAN_POINT('Ctrl Pts',(-0.132915182358376,0.070565859178174,
0.394052051633717));
#17990=CARTESIAN_POINT('Ctrl Pts',(-0.131337568919768,-0.0734603918663599,
0.401994219756497));
#17991=CARTESIAN_POINT('Ctrl Pts',(-0.00944124952954395,-0.150189377088511,
0.409936387879277));
#17992=CARTESIAN_POINT('Ctrl Pts',(0.121104224366159,-0.0893294633566384,
0.417878556002057));
#17993=CARTESIAN_POINT('Ctrl Pts',(0.140705787232781,0.0533654159743681,
0.425820724124838));
#17994=CARTESIAN_POINT('Ctrl Pts',(0.0314063937394313,0.147172091835368,
0.433762892247617));
#17995=CARTESIAN_POINT('Ctrl Pts',(-0.106664482920656,0.106154012011714,
0.441705060370398));
#17996=CARTESIAN_POINT('Ctrl Pts',(-0.147019735166745,-0.032112048430678,
0.449647228493177));
#17997=CARTESIAN_POINT('Ctrl Pts',(-0.052689806088835,-0.14096017351449,
0.457589396615958));
#17998=CARTESIAN_POINT('Ctrl Pts',(0.0899093983958942,-0.120674298270189,
0.465531564738737));
#17999=CARTESIAN_POINT('Ctrl Pts',(0.15014235720654,0.0101616315312987,
0.473473732861518));
#18000=CARTESIAN_POINT('Ctrl Pts',(0.0728294921055832,0.131688462906045,
0.481415900984297));
#18001=CARTESIAN_POINT('Ctrl Pts',(-0.071202669822089,0.132575133389036,
0.489358069107078));
#18002=CARTESIAN_POINT('Ctrl Pts',(-0.150005871264529,0.012009361726732,
0.497300237229857));
#18003=CARTESIAN_POINT('Ctrl Pts',(-0.0913882839399832,-0.119558219045865,
0.505242405352637));
#18004=CARTESIAN_POINT('Ctrl Pts',(0.0509503601487159,-0.141598188489932,
0.513184573475417));
#18005=CARTESIAN_POINT('Ctrl Pts',(0.146613240011817,-0.0339196703426114,
0.521126741598197));
#18006=CARTESIAN_POINT('Ctrl Pts',(0.107963329873666,0.104832750538675,
0.529068909720978));
#18007=CARTESIAN_POINT('Ctrl Pts',(-0.0295920819230583,0.147547602048875,
0.537011077843756));
#18008=CARTESIAN_POINT('Ctrl Pts',(-0.140038106568177,0.055093691941219,
0.544953245966537));
#18009=CARTESIAN_POINT('Ctrl Pts',(-0.122194838935542,-0.0878316999746162,
0.552895414089317));
#18010=CARTESIAN_POINT('Ctrl Pts',(0.00759145471482065,-0.150294231420327,
0.560837582212097));
#18011=CARTESIAN_POINT('Ctrl Pts',(0.130423195946632,-0.0750718065719766,
0.568779750334878));
#18012=CARTESIAN_POINT('Ctrl Pts',(0.133773890807325,0.0689241055160235,
0.576721918457657));
#18013=CARTESIAN_POINT('Ctrl Pts',(0.0145739585745413,0.149778456108953,
0.584664086580438));
#18014=CARTESIAN_POINT('Ctrl Pts',(-0.117977216952174,0.0934203535806499,
0.592606254703216));
#18015=CARTESIAN_POINT('Ctrl Pts',(-0.142449141490696,-0.0485203902651028,
0.600548422825998));
#18016=CARTESIAN_POINT('Ctrl Pts',(-0.036423018067407,-0.146011471938939,
0.608490590948776));
#18017=CARTESIAN_POINT('Ctrl Pts',(0.102970331784443,-0.109741044988262,
0.616432759071558));
#18018=CARTESIAN_POINT('Ctrl Pts',(0.148032279177632,0.0270634532975707,
0.624374927194337));
#18019=CARTESIAN_POINT('Ctrl Pts',(0.0574814509102497,0.139075048028633,
0.632317095317117));
#18020=CARTESIAN_POINT('Ctrl Pts',(-0.0857282916847416,0.123679611042927,
0.640259263439898));
#18021=CARTESIAN_POINT('Ctrl Pts',(-0.150402111894479,-0.00501905574730406,
0.648201431562677));
#18022=CARTESIAN_POINT('Ctrl Pts',(-0.0772921462128499,-0.129119751845818,
0.656143599685457));
#18023=CARTESIAN_POINT('Ctrl Pts',(0.0666253659236285,-0.134933490277457,
0.664085767808237));
#18024=CARTESIAN_POINT('Ctrl Pts',(0.14950719819016,-0.0171342893707992,
0.672027935931017));
#18025=CARTESIAN_POINT('Ctrl Pts',(0.0954250774564579,0.11636168087194,
0.679970104053797));
#18026=CARTESIAN_POINT('Ctrl Pts',(-0.0460762176180427,0.143258397146306,
0.687912272176577));
#18027=CARTESIAN_POINT('Ctrl Pts',(-0.145366963764729,0.0389157041403328,
0.695854440299358));
#18028=CARTESIAN_POINT('Ctrl Pts',(-0.111486636987321,-0.101077771820372,
0.703796608422136));
#18029=CARTESIAN_POINT('Ctrl Pts',(0.02452690272786,-0.148473624679578,
0.711738776544918));
#18030=CARTESIAN_POINT('Ctrl Pts',(0.138071279799868,-0.0598523840572839,
0.719680944667696));
#18031=CARTESIAN_POINT('Ctrl Pts',(0.125128179973684,0.0835997892305201,
0.727623112790477));
#18032=CARTESIAN_POINT('Ctrl Pts',(-0.00244518761474098,0.150465967050502,
0.735565280913257));
#18033=CARTESIAN_POINT('Ctrl Pts',(-0.127778512144395,0.0794898610961098,
0.743507449036036));
#18034=CARTESIAN_POINT('Ctrl Pts',(-0.136053592364468,-0.0643071239260258,
0.751449617158818));
#18035=CARTESIAN_POINT('Ctrl Pts',(-0.019689604662082,-0.149192176910068,
0.759391785281597));
#18036=CARTESIAN_POINT('Ctrl Pts',(0.114712083700712,-0.0974018687498071,
0.767333953404378));
#18037=CARTESIAN_POINT('Ctrl Pts',(0.144025718573537,0.0436185576594447,
0.775276121527157));
#18038=CARTESIAN_POINT('Ctrl Pts',(0.0413969989087525,0.14467990414796,
0.783218289649938));
#18039=CARTESIAN_POINT('Ctrl Pts',(-0.0991556246317344,0.113199594905656,
0.791160457772717));
#18040=CARTESIAN_POINT('Ctrl Pts',(-0.148871509365196,-0.021983172706469,
0.799102625895497));
#18041=CARTESIAN_POINT('Ctrl Pts',(-0.062205797368885,-0.137027095702329,
0.807044794018277));
#18042=CARTESIAN_POINT('Ctrl Pts',(0.081446815661698,-0.126540121706451,
0.814986962141057));
#18043=CARTESIAN_POINT('Ctrl Pts',(0.150485778196879,-0.000129396266831759,
0.822929130263837));
#18044=CARTESIAN_POINT('Ctrl Pts',(0.0816643079123276,0.126399869446589,
0.830871298386618));
#18045=CARTESIAN_POINT('Ctrl Pts',(-0.0619700581130299,0.137133869194964,
0.838813466509397));
#18046=CARTESIAN_POINT('Ctrl Pts',(-0.148833484480893,0.0222391564630926,
0.846755634632177));
#18047=CARTESIAN_POINT('Ctrl Pts',(-0.0993501488194509,-0.113028908304323,
0.854697802754957));
#18048=CARTESIAN_POINT('Ctrl Pts',(0.041148129789194,-0.144750881164039,
0.862639970877736));
#18049=CARTESIAN_POINT('Ctrl Pts',(0.143950494202948,-0.0438661760544617,
0.870582139000517));
#18050=CARTESIAN_POINT('Ctrl Pts',(0.114879417330645,0.0972044528644933,
0.878524307123298));
#18051=CARTESIAN_POINT('Ctrl Pts',(-0.0194330078274841,0.149225816766708,
0.886466475246077));
#18052=CARTESIAN_POINT('Ctrl Pts',(-0.135942801386891,0.0645410019599824,
0.894408643368857));
#18053=CARTESIAN_POINT('Ctrl Pts',(-0.127915022941288,-0.0792700011911429,
0.902350811491637));
#18054=CARTESIAN_POINT('Ctrl Pts',(-0.00270394227186439,-0.150461539534541,
0.910292979614417));
#18055=CARTESIAN_POINT('Ctrl Pts',(0.124984227305131,-0.0838148501630433,
0.918235147737197));
#18056=CARTESIAN_POINT('Ctrl Pts',(0.138174004553101,0.0596148525845174,
0.926177315859977));
#18057=CARTESIAN_POINT('Ctrl Pts',(0.0247821984756025,0.148431225898158,
0.934119483982757));
#18058=CARTESIAN_POINT('Ctrl Pts',(-0.11131264737753,0.101269347369872,
0.942061652105537));
#18059=CARTESIAN_POINT('Ctrl Pts',(-0.145433672650089,-0.0386656571445607,
0.950003820228317));
#18060=CARTESIAN_POINT('Ctrl Pts',(-0.0463225128062989,-0.143178947440692,
0.957945988351097));
#18061=CARTESIAN_POINT('Ctrl Pts',(0.0952248276606132,-0.116525612549003,
0.965888156473877));
#18062=CARTESIAN_POINT('Ctrl Pts',(0.149536443172165,0.0168771545685866,
0.973830324596656));
#18063=CARTESIAN_POINT('Ctrl Pts',(0.0668573142755158,0.134818714245386,
0.981772492719438));
#18064=CARTESIAN_POINT('Ctrl Pts',(-0.0770699830103684,0.129252481220654,
0.989714660842216));
#18065=CARTESIAN_POINT('Ctrl Pts',(-0.15039325815857,0.00527769678589187,
0.997656828964997));
#18066=CARTESIAN_POINT('Ctrl Pts',(-0.0859408583470751,-0.123532000103139,
1.00559899708778));
#18067=CARTESIAN_POINT('Ctrl Pts',(0.0572421967501742,-0.139173693973137,
1.01354116521056));
#18068=CARTESIAN_POINT('Ctrl Pts',(0.147985518909957,-0.0273179863069172,
1.02148333333334));
#18069=CARTESIAN_POINT('Ctrl Pts',(0.103158902618224,0.109563803299803,
1.02942550145612));
#18070=CARTESIAN_POINT('Ctrl Pts',(-0.0361718663885326,0.146073893166727,
1.0373676695789));
#18071=CARTESIAN_POINT('Ctrl Pts',(-0.142365489706367,0.0487652901517079,
1.04530983770168));
#18072=CARTESIAN_POINT('Ctrl Pts',(-0.118137698690712,-0.0932173284908804,
1.05325200582446));
#18073=CARTESIAN_POINT('Ctrl Pts',(0.0143163610725534,-0.149803297655807,
1.06119417394724));
#18074=CARTESIAN_POINT('Ctrl Pts',(0.133655163317704,-0.0691540562905145,
1.06913634207002));
#18075=CARTESIAN_POINT('Ctrl Pts',(0.130552105047211,0.0748474051030229,
1.0770785101928));
#18076=CARTESIAN_POINT('Ctrl Pts',(0.0078499064261323,0.150280954056111,
1.08502067831558));
#18077=CARTESIAN_POINT('Ctrl Pts',(-0.122043612932812,0.0880417101447944,
1.09296284643836));
#18078=CARTESIAN_POINT('Ctrl Pts',(-0.140132644828567,-0.0548527851276936,
1.10090501456114));
#18079=CARTESIAN_POINT('Ctrl Pts',(-0.0298457776877653,-0.147496493982489,
1.10884718268392));
#18080=CARTESIAN_POINT('Ctrl Pts',(0.107782887988268,-0.10501826145877,
1.1167893508067));
#18081=CARTESIAN_POINT('Ctrl Pts',(0.146671355310253,0.033667487497105,
1.12473151892948));
#18082=CARTESIAN_POINT('Ctrl Pts',(0.0511937930472066,0.141510359113225,
1.13267368705226));
#18083=CARTESIAN_POINT('Ctrl Pts',(-0.0911825429852659,0.119715203870077,
1.14061585517504));
#18084=CARTESIAN_POINT('Ctrl Pts',(-0.150026302104679,-0.0117513769282424,
1.14855802329782));
#18085=CARTESIAN_POINT('Ctrl Pts',(-0.0714305557085884,-0.132452489195471,
1.1565001914206));
#18086=CARTESIAN_POINT('Ctrl Pts',(0.0726029180563751,-0.131813513998426,
1.16444235954338));
#18087=CARTESIAN_POINT('Ctrl Pts',(0.150124660100533,-0.010419818262018,
1.17238452766616));
#18088=CARTESIAN_POINT('Ctrl Pts',(0.0901167906002831,0.120519501471002,
1.18032669578894));
#18089=CARTESIAN_POINT('Ctrl Pts',(-0.0524473171394798,0.141050576417769,
1.18826886391172));
#18090=CARTESIAN_POINT('Ctrl Pts',(-0.146964294261872,0.0323648326895764,
1.1962110320345));
#18091=CARTESIAN_POINT('Ctrl Pts',(-0.106846879624786,-0.105970422747861,
1.20415320015727));
#18092=CARTESIAN_POINT('Ctrl Pts',(0.0311532535456026,-0.14722588419309,
1.21209536828006));
#18093=CARTESIAN_POINT('Ctrl Pts',(0.140613805972886,-0.0536073106276968,
1.22003753640283));
#18094=CARTESIAN_POINT('Ctrl Pts',(0.121257666323848,0.0891210667609394,
1.22797970452562));
#18095=CARTESIAN_POINT('Ctrl Pts',(-0.00918295295119051,0.150205391241489,
1.2359218726484));
#18096=CARTESIAN_POINT('Ctrl Pts',(-0.131211043922368,0.0736861461587066,
1.24386404077118));
#18097=CARTESIAN_POINT('Ctrl Pts',(-0.133036338837895,-0.0703371788708997,
1.25180620889396));
#18098=CARTESIAN_POINT('Ctrl Pts',(-0.0129866800356469,-0.149924422041766,
1.25974837701674));
#18099=CARTESIAN_POINT('Ctrl Pts',(0.118960111851797,-0.0921654923014072,
1.26769054513952));
#18100=CARTESIAN_POINT('Ctrl Pts',(0.141927220045961,0.050026496908035,
1.2756327132623));
#18101=CARTESIAN_POINT('Ctrl Pts',(0.0348744139414821,0.146389075532006,
1.28357488138508));
#18102=CARTESIAN_POINT('Ctrl Pts',(-0.104126938119509,0.108644221848311,
1.29151704950786));
#18103=CARTESIAN_POINT('Ctrl Pts',(-0.147737317493493,-0.0286299004949125,
1.29945921763064));
#18104=CARTESIAN_POINT('Ctrl Pts',(-0.0560051364173496,-0.139676092720537,
1.30740138575342));
#18105=CARTESIAN_POINT('Ctrl Pts',(0.0870335032532438,-0.122764634549313,
1.3153435538762));
#18106=CARTESIAN_POINT('Ctrl Pts',(0.150340512633584,0.00661184096937889,
1.32328572199898));
#18107=CARTESIAN_POINT('Ctrl Pts',(0.0759201674095095,0.129931190880528,
1.33122789012176));
#18108=CARTESIAN_POINT('Ctrl Pts',(-0.0680508508044829,0.134220221643466,
1.33917005824454));
#18109=CARTESIAN_POINT('Ctrl Pts',(-0.149680298423566,0.0155497403439283,
1.34711222636732));
#18110=CARTESIAN_POINT('Ctrl Pts',(-0.0941872156892785,-0.117365900463673,
1.3550543944901));
#18111=CARTESIAN_POINT('Ctrl Pts',(0.0475910332998192,-0.142762319241037,
1.36299656261288));
#18112=CARTESIAN_POINT('Ctrl Pts',(0.145771005694385,-0.0373737865856905,
1.37093873073566));
#18113=CARTESIAN_POINT('Ctrl Pts',(0.110409762917901,0.10225297323032,1.37888089885844));
#18114=CARTESIAN_POINT('Ctrl Pts',(-0.0260981686868614,0.148205506441964,
1.38682306698121));
#18115=CARTESIAN_POINT('Ctrl Pts',(-0.138697490589939,0.0583865667538053,
1.394765235104));
#18116=CARTESIAN_POINT('Ctrl Pts',(-0.124235673603468,-0.0849204601545819,
1.40270740322677));
#18117=CARTESIAN_POINT('Ctrl Pts',(0.0040388053119065,-0.150431633134115,
1.41064957134956));
#18118=CARTESIAN_POINT('Ctrl Pts',(0.12861328245382,-0.0781319533624403,
1.41859173947234));
#18119=CARTESIAN_POINT('Ctrl Pts',(0.1353648581188,0.0657445800149866,1.42653390759512));
#18120=CARTESIAN_POINT('Ctrl Pts',(0.0181081687242482,0.149392404544468,
1.43447607571789));
#18121=CARTESIAN_POINT('Ctrl Pts',(-0.115737181672069,0.0961812857364522,
1.44241824384068));
#18122=CARTESIAN_POINT('Ctrl Pts',(-0.143555918690644,-0.0451414811888502,
1.45036041196346));
#18123=CARTESIAN_POINT('Ctrl Pts',(-0.0398616700558823,-0.145110565703753,
1.45830258008624));
#18124=CARTESIAN_POINT('Ctrl Pts',(0.100348034367198,-0.112142416378873,
1.46624474820902));
#18125=CARTESIAN_POINT('Ctrl Pts',(0.14863229283285,0.0235577176564554,
1.4741869163318));
#18126=CARTESIAN_POINT('Ctrl Pts',(0.0607471474677608,0.137680339497592,
1.48212908445458));
#18127=CARTESIAN_POINT('Ctrl Pts',(-0.0827754224726193,0.125666453945577,
1.49007125257736));
#18128=CARTESIAN_POINT('Ctrl Pts',(-0.150492272191201,-0.00145719475437189,
1.49801342070014));
#18129=CARTESIAN_POINT('Ctrl Pts',(-0.0802951178786721,-0.12727177793954,
1.50595558882292));
#18130=CARTESIAN_POINT('Ctrl Pts',(0.0633700050447994,-0.136443062004882,
1.5138977569457));
#18131=CARTESIAN_POINT('Ctrl Pts',(0.149155357006591,-0.0207133070603065,
1.52183992506848));
#18132=CARTESIAN_POINT('Ctrl Pts',(0.0979555318420461,0.114182655252422,
1.52978209319126));
#18133=CARTESIAN_POINT('Ctrl Pts',(0.00450803278943675,0.134083974545181,
1.53507687193978));
#18134=CARTESIAN_POINT('Ctrl Pts',(-0.0361033354337414,0.122073089461022,
1.53772426131404));
#18135=CARTESIAN_POINT('Ctrl Pts',(-0.0592743564846203,0.123319225136773,
-0.00549926131403157));
#18136=CARTESIAN_POINT('Ctrl Pts',(-0.100300290071938,0.10359978715075,
-0.00285187193977157));
#18137=CARTESIAN_POINT('Ctrl Pts',(-0.160414584165772,0.0203416160441626,
0.00244290680874841));
#18138=CARTESIAN_POINT('Ctrl Pts',(-0.103922107946056,-0.124084444561314,
0.0103850749315284));
#18139=CARTESIAN_POINT('Ctrl Pts',(0.0479099321398382,-0.154436663180837,
0.0183272430543084));
#18140=CARTESIAN_POINT('Ctrl Pts',(0.155781551077148,-0.0435098515708298,
0.0262694111770884));
#18141=CARTESIAN_POINT('Ctrl Pts',(0.120977930992648,0.107381072623318,
0.0342115792998684));
#18142=CARTESIAN_POINT('Ctrl Pts',(-0.0246731903087699,0.159844935900913,
0.0421537474226484));
#18143=CARTESIAN_POINT('Ctrl Pts',(-0.147710978397823,0.0659033513787588,
0.0500959155454284));
#18144=CARTESIAN_POINT('Ctrl Pts',(-0.135435684249567,-0.0884277117007276,
0.0580380836682085));
#18145=CARTESIAN_POINT('Ctrl Pts',(0.000915427738408385,-0.16174188059703,
0.0659802517909884));
#18146=CARTESIAN_POINT('Ctrl Pts',(0.13642643003965,-0.0868880976295618,
0.0739224199137684));
#18147=CARTESIAN_POINT('Ctrl Pts',(0.146957588340267,0.0675663355536457,
0.0818645880365484));
#18148=CARTESIAN_POINT('Ctrl Pts',(0.0228600865593111,0.160121891352391,
0.0898067561593285));
#18149=CARTESIAN_POINT('Ctrl Pts',(-0.122179386207322,0.105989962368389,
0.0977489242821083));
#18150=CARTESIAN_POINT('Ctrl Pts',(-0.155290103436038,-0.0452399862206161,
0.105691092404888));
#18151=CARTESIAN_POINT('Ctrl Pts',(-0.0461390722131997,-0.155025288408554,
0.113633260527668));
#18152=CARTESIAN_POINT('Ctrl Pts',(0.105280057525145,-0.122791590307548,
0.121575428650448));
#18153=CARTESIAN_POINT('Ctrl Pts',(0.160251855424436,0.0219318669073289,
0.129517596773229));
#18154=CARTESIAN_POINT('Ctrl Pts',(0.0684164816681947,0.146563455853242,
0.137459764896008));
#18155=CARTESIAN_POINT('Ctrl Pts',(-0.086095413359615,0.136927875387926,
0.145401933018789));
#18156=CARTESIAN_POINT('Ctrl Pts',(-0.16173506727009,0.00185228698694943,
0.153344101141568));
#18157=CARTESIAN_POINT('Ctrl Pts',(-0.0892087826023274,-0.134920182928699,
0.161286269264348));
#18158=CARTESIAN_POINT('Ctrl Pts',(0.0650419110192955,-0.148091906331324,
0.169228437387128));
#18159=CARTESIAN_POINT('Ctrl Pts',(0.159707532494063,-0.025596228460074,
0.177170605509908));
#18160=CARTESIAN_POINT('Ctrl Pts',(0.108064646638443,0.120348223746572,
0.185112773632688));
#18161=CARTESIAN_POINT('Ctrl Pts',(-0.0425765573421325,0.156041339440091,
0.193054941755468));
#18162=CARTESIAN_POINT('Ctrl Pts',(-0.154213260793436,0.0487845573223287,
0.200997109878248));
#18163=CARTESIAN_POINT('Ctrl Pts',(-0.124574774400312,-0.103163891052585,
0.208939278001028));
#18164=CARTESIAN_POINT('Ctrl Pts',(0.0191870033818907,-0.160603616835255,
0.216881446123808));
#18165=CARTESIAN_POINT('Ctrl Pts',(0.145371514918136,-0.0709139301387177,
0.224823614246588));
#18166=CARTESIAN_POINT('Ctrl Pts',(0.138380784202201,0.0837402018183176,
0.232765782369368));
#18167=CARTESIAN_POINT('Ctrl Pts',(0.00461903876105218,0.161679705957985,
0.240707950492149));
#18168=CARTESIAN_POINT('Ctrl Pts',(-0.133374220718213,0.0915039894496894,
0.248650118614928));
#18169=CARTESIAN_POINT('Ctrl Pts',(-0.149182991964712,-0.0624987819548612,
0.256592286737709));
#18170=CARTESIAN_POINT('Ctrl Pts',(-0.0283248164207669,-0.159246248345813,
0.264534454860488));
#18171=CARTESIAN_POINT('Ctrl Pts',(0.118481800883715,-0.110107791262854,
0.272476622983269));
#18172=CARTESIAN_POINT('Ctrl Pts',(0.156746916480749,0.0399007144198201,
0.280418791106048));
#18173=CARTESIAN_POINT('Ctrl Pts',(0.0514157533588968,0.153356066537929,
0.288360959228829));
#18174=CARTESIAN_POINT('Ctrl Pts',(-0.101017521980764,0.126321506839912,
0.296303127351608));
#18175=CARTESIAN_POINT('Ctrl Pts',(-0.160908369261695,-0.0164365306249019,
0.304245295474388));
#18176=CARTESIAN_POINT('Ctrl Pts',(-0.0733906195540655,-0.144137017448375,
0.312187463597168));
#18177=CARTESIAN_POINT('Ctrl Pts',(0.0813604773699057,-0.13979318853071,
0.320129631719948));
#18178=CARTESIAN_POINT('Ctrl Pts',(0.161577018543625,-0.00738443741900211,
0.328071799842729));
#18179=CARTESIAN_POINT('Ctrl Pts',(0.0937724112935796,0.131789217000595,
0.336013967965508));
#18180=CARTESIAN_POINT('Ctrl Pts',(-0.0599373583072218,0.150230409426965,
0.343956136088289));
#18181=CARTESIAN_POINT('Ctrl Pts',(-0.158738350099833,0.0310451130618767,
0.351898304211068));
#18182=CARTESIAN_POINT('Ctrl Pts',(-0.112118705390683,-0.116580696253536,
0.359840472333849));
#18183=CARTESIAN_POINT('Ctrl Pts',(0.0372131918485748,-0.15740661101073,
0.367782640456628));
#18184=CARTESIAN_POINT('Ctrl Pts',(0.152453982298084,-0.0540318990865351,
0.375724808579408));
#18185=CARTESIAN_POINT('Ctrl Pts',(0.128031262769868,0.0988415833088236,
0.383666976702188));
#18186=CARTESIAN_POINT('Ctrl Pts',(-0.0136812466069205,0.161166021011634,
0.391609144824968));
#18187=CARTESIAN_POINT('Ctrl Pts',(-0.142860328563903,0.0758458262533652,
0.399551312947749));
#18188=CARTESIAN_POINT('Ctrl Pts',(-0.141164672957165,-0.0789569372907697,
0.407493481070528));
#18189=CARTESIAN_POINT('Ctrl Pts',(-0.0101476745237983,-0.161427034722196,
0.415435649193308));
#18190=CARTESIAN_POINT('Ctrl Pts',(0.130165636283581,-0.0960133843187101,
0.423377817316089));
#18191=CARTESIAN_POINT('Ctrl Pts',(0.151233851831306,0.0573583899504574,
0.431319985438868));
#18192=CARTESIAN_POINT('Ctrl Pts',(0.0337563222576384,0.158183986373718,
0.439262153561649));
#18193=CARTESIAN_POINT('Ctrl Pts',(-0.114645466422773,0.114096800420287,
0.447204321684428));
#18194=CARTESIAN_POINT('Ctrl Pts',(-0.158020229883659,-0.0345147763277912,
0.455146489807208));
#18195=CARTESIAN_POINT('Ctrl Pts',(-0.0566322287360923,-0.151507272121918,
0.463088657929988));
#18196=CARTESIAN_POINT('Ctrl Pts',(0.0966367119836487,-0.129703541718919,
0.471030826052768));
#18197=CARTESIAN_POINT('Ctrl Pts',(0.161376496659739,0.0109219578497271,
0.478972994175549));
#18198=CARTESIAN_POINT('Ctrl Pts',(0.0782788315581001,0.141541821972661,
0.486915162298328));
#18199=CARTESIAN_POINT('Ctrl Pts',(-0.0765302851406724,0.142494836024782,
0.494857330421108));
#18200=CARTESIAN_POINT('Ctrl Pts',(-0.161229798395673,0.0129079412274925,
0.502799498543889));
#18201=CARTESIAN_POINT('Ctrl Pts',(-0.0982262525537151,-0.128503953817366,
0.510741666666668));
#18202=CARTESIAN_POINT('Ctrl Pts',(0.0547626317937811,-0.152193025452748,
0.518683834789449));
#18203=CARTESIAN_POINT('Ctrl Pts',(0.157583319439253,-0.0364576503898468,
0.526626002912228));
#18204=CARTESIAN_POINT('Ctrl Pts',(0.116041497328862,0.112676677866884,
0.534568171035008));
#18205=CARTESIAN_POINT('Ctrl Pts',(-0.0318062577307366,0.158587593482618,
0.542510339157789));
#18206=CARTESIAN_POINT('Ctrl Pts',(-0.150516213127973,0.0592159811457737,
0.550452507280567));
#18207=CARTESIAN_POINT('Ctrl Pts',(-0.131337854181896,-0.0944035534094825,
0.558394675403349));
#18208=CARTESIAN_POINT('Ctrl Pts',(0.00815947204521347,-0.161539734596121,
0.566336843526128));
#18209=CARTESIAN_POINT('Ctrl Pts',(0.140181883624494,-0.080688923285235,
0.574279011648909));
#18210=CARTESIAN_POINT('Ctrl Pts',(0.143783288371658,0.0740812312429708,
0.582221179771688));
#18211=CARTESIAN_POINT('Ctrl Pts',(0.0156644295519346,0.160985367298567,
0.590163347894469));
#18212=CARTESIAN_POINT('Ctrl Pts',(-0.126804656005353,0.100410368253513,
0.598105516017247));
#18213=CARTESIAN_POINT('Ctrl Pts',(-0.153107649524464,-0.0521508436608248,
0.606047684140029));
#18214=CARTESIAN_POINT('Ctrl Pts',(-0.0391483067326994,-0.156936525122116,
0.613989852262808));
#18215=CARTESIAN_POINT('Ctrl Pts',(0.110674906884577,-0.117952226869747,
0.621932020385589));
#18216=CARTESIAN_POINT('Ctrl Pts',(0.159108535730396,0.0290884288879846,
0.629874188508368));
#18217=CARTESIAN_POINT('Ctrl Pts',(0.061782400006242,0.14948109541648,0.637816356631148));
#18218=CARTESIAN_POINT('Ctrl Pts',(-0.0921427612707386,0.132933721767072,
0.645758524753929));
#18219=CARTESIAN_POINT('Ctrl Pts',(-0.161655687038194,-0.0053945978210935,
0.653700692876707));
#18220=CARTESIAN_POINT('Ctrl Pts',(-0.0830753959589387,-0.138780911597048,
0.661642860999489));
#18221=CARTESIAN_POINT('Ctrl Pts',(0.0716104924784035,-0.145029652845349,
0.669585029122267));
#18222=CARTESIAN_POINT('Ctrl Pts',(0.160693812980115,-0.0184163326249747,
0.677527197245049));
#18223=CARTESIAN_POINT('Ctrl Pts',(0.102565092089392,0.125068240261613,
0.685469365367828));
#18224=CARTESIAN_POINT('Ctrl Pts',(-0.0495237900674707,0.153977456320057,
0.693411533490608));
#18225=CARTESIAN_POINT('Ctrl Pts',(-0.156243792750268,0.0418275036842162,
0.701353701613389));
#18226=CARTESIAN_POINT('Ctrl Pts',(-0.119828429739121,-0.108640739429086,
0.709295869736167));
#18227=CARTESIAN_POINT('Ctrl Pts',(0.0263620853553792,-0.159582904138124,
0.717238037858949));
#18228=CARTESIAN_POINT('Ctrl Pts',(0.148402221984423,-0.0643307340819919,
0.725180205981728));
#18229=CARTESIAN_POINT('Ctrl Pts',(0.134490677336207,0.0898549973406614,
0.733122374104509));
#18230=CARTESIAN_POINT('Ctrl Pts',(-0.00262814450422035,0.161724320044658,
0.741064542227287));
#18231=CARTESIAN_POINT('Ctrl Pts',(-0.137339315979238,0.0854375510170853,
0.749006710350069));
#18232=CARTESIAN_POINT('Ctrl Pts',(-0.146233564613262,-0.0691187920752458,
0.756948878472847));
#18233=CARTESIAN_POINT('Ctrl Pts',(-0.0211628449166461,-0.160355220783347,
0.764891046595629));
#18234=CARTESIAN_POINT('Ctrl Pts',(0.12329521486528,-0.104689793336152,
0.772833214718408));
#18235=CARTESIAN_POINT('Ctrl Pts',(0.154802191231926,0.0468822399980663,
0.780775382841188));
#18236=CARTESIAN_POINT('Ctrl Pts',(0.0444944569967772,0.155505325098544,
0.788717550963968));
#18237=CARTESIAN_POINT('Ctrl Pts',(-0.106574770936664,0.121669556739719,
0.796659719086747));
#18238=CARTESIAN_POINT('Ctrl Pts',(-0.160010559849905,-0.0236280251811701,
0.804601887209529));
#18239=CARTESIAN_POINT('Ctrl Pts',(-0.0668602374312443,-0.147279908636853,
0.812544055332307));
#18240=CARTESIAN_POINT('Ctrl Pts',(0.0875409312876049,-0.13600826514128,
0.820486223455089));
#18241=CARTESIAN_POINT('Ctrl Pts',(0.161745613525436,-0.000139078116330951,
0.828428391577867));
#18242=CARTESIAN_POINT('Ctrl Pts',(0.0877746970157421,0.135857518751215,
0.836370559700649));
#18243=CARTESIAN_POINT('Ctrl Pts',(-0.0666068593976089,0.147394671269449,
0.844312727823428));
#18244=CARTESIAN_POINT('Ctrl Pts',(-0.159969689820096,0.0239031624749592,
0.852254895946208));
#18245=CARTESIAN_POINT('Ctrl Pts',(-0.106783850056725,-0.121486098811777,
0.860197064068988));
#18246=CARTESIAN_POINT('Ctrl Pts',(0.0442269666803361,-0.155581612845794,
0.868139232191768));
#18247=CARTESIAN_POINT('Ctrl Pts',(0.154721338329289,-0.0471483860066884,
0.876081400314548));
#18248=CARTESIAN_POINT('Ctrl Pts',(0.123475068941597,0.104477606152275,
0.884023568437328));
#18249=CARTESIAN_POINT('Ctrl Pts',(-0.0208870486723946,0.160391377683462,
0.891965736560109));
#18250=CARTESIAN_POINT('Ctrl Pts',(-0.146114483894434,0.0693701696243073,
0.899907904682887));
#18251=CARTESIAN_POINT('Ctrl Pts',(-0.137486040957907,-0.0852012404790134,
0.907850072805669));
#18252=CARTESIAN_POINT('Ctrl Pts',(-0.00290626002629624,-0.161719561247554,
0.915792240928448));
#18253=CARTESIAN_POINT('Ctrl Pts',(0.134335953660838,-0.0900861498315643,
0.923734409051229));
#18254=CARTESIAN_POINT('Ctrl Pts',(0.148512632937768,0.0640754297319473,
0.931676577174007));
#18255=CARTESIAN_POINT('Ctrl Pts',(0.0266364831612253,0.159537332941991,
0.939618745296788));
#18256=CARTESIAN_POINT('Ctrl Pts',(-0.119641421660886,0.10884664928423,
0.947560913419568));
#18257=CARTESIAN_POINT('Ctrl Pts',(-0.156315493011378,-0.0415587473590326,
0.955503081542348));
#18258=CARTESIAN_POINT('Ctrl Pts',(-0.0497885138626987,-0.153892061929087,
0.963445249665127));
#18259=CARTESIAN_POINT('Ctrl Pts',(0.102349858952582,-0.125244437839883,
0.971387417787908));
#18260=CARTESIAN_POINT('Ctrl Pts',(0.160725246166783,0.018139958160622,
0.979329585910688));
#18261=CARTESIAN_POINT('Ctrl Pts',(0.0718597959603077,0.14490628889729,
0.987271754033468));
#18262=CARTESIAN_POINT('Ctrl Pts',(-0.0828366097831417,0.138923572215364,
0.995213922156248));
#18263=CARTESIAN_POINT('Ctrl Pts',(-0.161646170836971,0.00567259122332548,
1.00315609027903));
#18264=CARTESIAN_POINT('Ctrl Pts',(-0.0923712328620446,-0.132775066096718,
1.01109825840181));
#18265=CARTESIAN_POINT('Ctrl Pts',(0.0615252440718216,-0.149587122371362,
1.01904042652459));
#18266=CARTESIAN_POINT('Ctrl Pts',(0.159058276707423,-0.0293620068848675,
1.02698259464737));
#18267=CARTESIAN_POINT('Ctrl Pts',(0.1108775872014,0.117761723381742,1.03492476277015));
#18268=CARTESIAN_POINT('Ctrl Pts',(-0.0388783630684312,0.157003616909169,
1.04286693089293));
#18269=CARTESIAN_POINT('Ctrl Pts',(-0.153017738641585,0.0524140677533946,
1.05080909901571));
#18270=CARTESIAN_POINT('Ctrl Pts',(-0.126977145509477,-0.10019215216626,
1.05875126713849));
#18271=CARTESIAN_POINT('Ctrl Pts',(0.0153875577671049,-0.161012067570745,
1.06669343526127));
#18272=CARTESIAN_POINT('Ctrl Pts',(0.143655677305146,-0.0743283876822416,
1.07463560338405));
#18273=CARTESIAN_POINT('Ctrl Pts',(0.140320438123209,0.080447731368589,
1.08257777150683));
#18274=CARTESIAN_POINT('Ctrl Pts',(0.00843726195408678,0.161525463776335,
1.09051993962961));
#18275=CARTESIAN_POINT('Ctrl Pts',(-0.131175312957834,0.094629277223576,
1.09846210775239));
#18276=CARTESIAN_POINT('Ctrl Pts',(-0.150617825048456,-0.0589570489009974,
1.10640427587517));
#18277=CARTESIAN_POINT('Ctrl Pts',(-0.0320789358376135,-0.158532661344495,
1.11434644399795));
#18278=CARTESIAN_POINT('Ctrl Pts',(0.115847554194776,-0.112876069317329,
1.12228861212073));
#18279=CARTESIAN_POINT('Ctrl Pts',(0.157645783113317,0.0361865984037055,
1.13023078024351));
#18280=CARTESIAN_POINT('Ctrl Pts',(0.0550242791334153,0.152098624396442,
1.13817294836629));
#18281=CARTESIAN_POINT('Ctrl Pts',(-0.0980051173916675,0.128672684756662,
1.14611511648907));
#18282=CARTESIAN_POINT('Ctrl Pts',(-0.161251757937727,-0.0126306531673768,
1.15405728461185));
#18283=CARTESIAN_POINT('Ctrl Pts',(-0.0767752221903169,-0.142363015193798,
1.16199945273463));
#18284=CARTESIAN_POINT('Ctrl Pts',(0.0780353045016797,-0.141676229794458,
1.16994162085741));
#18285=CARTESIAN_POINT('Ctrl Pts',(0.161357475398708,-0.0111994629512984,
1.17788378898019));
#18286=CARTESIAN_POINT('Ctrl Pts',(0.0968596219472387,0.129537162519796,
1.18582595710297));
#18287=CARTESIAN_POINT('Ctrl Pts',(-0.0563715959749383,0.151604439264423,
1.19376812522575));
#18288=CARTESIAN_POINT('Ctrl Pts',(-0.157960640709981,0.0347864747270306,
1.20171029334853));
#18289=CARTESIAN_POINT('Ctrl Pts',(-0.114841510641486,-0.113899474410655,
1.20965246147131));
#18290=CARTESIAN_POINT('Ctrl Pts',(0.03348424129126,-0.158241803650584,
1.21759462959409));
#18291=CARTESIAN_POINT('Ctrl Pts',(0.151134988234409,-0.0576183839484237,
1.22553679771687));
#18292=CARTESIAN_POINT('Ctrl Pts',(0.130330559267559,0.0957893948119858,
1.23347896583965));
#18293=CARTESIAN_POINT('Ctrl Pts',(-0.0098700513554357,0.16144424710618,
1.24142113396243));
#18294=CARTESIAN_POINT('Ctrl Pts',(-0.141028680947982,0.0791995832534545,
1.24936330208521));
#18295=CARTESIAN_POINT('Ctrl Pts',(-0.142990550365238,-0.0756000353418,
1.25730547020799));
#18296=CARTESIAN_POINT('Ctrl Pts',(-0.013958385670676,-0.161142254877177,
1.26524763833077));
#18297=CARTESIAN_POINT('Ctrl Pts',(0.127861094297897,-0.0990616141723472,
1.27318980645355));
#18298=CARTESIAN_POINT('Ctrl Pts',(0.152546676219863,0.0537696421008814,
1.28113197457633));
#18299=CARTESIAN_POINT('Ctrl Pts',(0.0374838310097642,0.157342382244044,
1.28907414269911));
#18300=CARTESIAN_POINT('Ctrl Pts',(-0.111918054267102,0.116773335855419,
1.29701631082189));
#18301=CARTESIAN_POINT('Ctrl Pts',(-0.158791504053787,-0.0307720827589687,
1.30495847894467));
#18302=CARTESIAN_POINT('Ctrl Pts',(-0.060195622861772,-0.150127112226926,
1.31290064706745));
#18303=CARTESIAN_POINT('Ctrl Pts',(0.0935456330135535,-0.131950283756556,
1.32084281519023));
#18304=CARTESIAN_POINT('Ctrl Pts',(0.161589478720268,0.00710656041347678,
1.32878498331301));
#18305=CARTESIAN_POINT('Ctrl Pts',(0.0816007612396376,0.139653065139265,
1.33672715143579));
#18306=CARTESIAN_POINT('Ctrl Pts',(-0.0731426367739486,0.144263015132499,
1.34466931955857));
#18307=CARTESIAN_POINT('Ctrl Pts',(-0.160879865135934,0.0167132224867059,
1.35261148768135));
#18308=CARTESIAN_POINT('Ctrl Pts',(-0.101234609479067,-0.126147598829082,
1.36055365580413));
#18309=CARTESIAN_POINT('Ctrl Pts',(0.051151949184981,-0.153444260252591,
1.36849582392691));
#18310=CARTESIAN_POINT('Ctrl Pts',(0.15667806641111,-0.0401702148435725,
1.37643799204969));
#18311=CARTESIAN_POINT('Ctrl Pts',(0.118670980449659,0.10990387323047,1.38438016017247));
#18312=CARTESIAN_POINT('Ctrl Pts',(-0.0280509185434417,0.159294724422008,
1.39232232829525));
#18313=CARTESIAN_POINT('Ctrl Pts',(-0.149075287902345,0.0627552395607943,
1.40026449641803));
#18314=CARTESIAN_POINT('Ctrl Pts',(-0.133531390736797,-0.0912744851582948,
1.40820666454081));
#18315=CARTESIAN_POINT('Ctrl Pts',(0.00434100186018791,-0.161687417152987,
1.41614883266359));
#18316=CARTESIAN_POINT('Ctrl Pts',(0.138236546518021,-0.0839780402106489,
1.42409100078637));
#18317=CARTESIAN_POINT('Ctrl Pts',(0.145493297031458,0.07066380330362,1.43203316890915));
#18318=CARTESIAN_POINT('Ctrl Pts',(0.0194630807988606,0.160570430100525,
1.43997533703193));
#18319=CARTESIAN_POINT('Ctrl Pts',(-0.124397014000637,0.103377882332206,
1.44791750515471));
#18320=CARTESIAN_POINT('Ctrl Pts',(-0.15429723939393,-0.0485191136187331,
1.45585967327749));
#18321=CARTESIAN_POINT('Ctrl Pts',(-0.042844249846,-0.155968210152522,1.46380184140027));
#18322=CARTESIAN_POINT('Ctrl Pts',(0.107856400646442,-0.120533276677448,
1.47174400952305));
#18323=CARTESIAN_POINT('Ctrl Pts',(0.159753444358638,0.0253203827049868,
1.47968617764583));
#18324=CARTESIAN_POINT('Ctrl Pts',(0.0652924466007548,0.147982030257331,
1.48762834576861));
#18325=CARTESIAN_POINT('Ctrl Pts',(-0.0889689487809616,0.13506922671723,
1.49557051389139));
#18326=CARTESIAN_POINT('Ctrl Pts',(-0.161752593421533,-0.00156622680492735,
1.50351268201417));
#18327=CARTESIAN_POINT('Ctrl Pts',(-0.086303059730943,-0.136794666273195,
1.51145485013695));
#18328=CARTESIAN_POINT('Ctrl Pts',(0.0681115549116652,-0.14665217563879,
1.51939701825973));
#18329=CARTESIAN_POINT('Ctrl Pts',(0.160315645894948,-0.02226314405755,
1.52733918638251));
#18330=CARTESIAN_POINT('Ctrl Pts',(0.105284883301553,0.122726172858702,
1.53528135450529));
#18331=CARTESIAN_POINT('Ctrl Pts',(0.00484533846358528,0.144116573583224,
1.54057613325381));
#18332=CARTESIAN_POINT('Ctrl Pts',(-0.0388047044047284,0.131206995015745,
1.54322352262807));
#18333=CARTESIAN_POINT('Ctrl Pts',(-0.0634007094575145,0.131904027763688,
-3.88578058618805E-16));
#18334=CARTESIAN_POINT('Ctrl Pts',(-0.107282641710421,0.110811831533068,
0.00264738937425961));
#18335=CARTESIAN_POINT('Ctrl Pts',(-0.171581760589518,0.0217576868851663,
0.0079421681227796));
#18336=CARTESIAN_POINT('Ctrl Pts',(-0.111156590520044,-0.1327225175337,
0.0158843362455596));
#18337=CARTESIAN_POINT('Ctrl Pts',(0.0512451567233008,-0.165187689797298,
0.0238265043683396));
#18338=CARTESIAN_POINT('Ctrl Pts',(0.16662620135312,-0.0465387668729445,
0.0317686724911196));
#18339=CARTESIAN_POINT('Ctrl Pts',(0.129399745666171,0.114856349193662,
0.0397108406138996));
#18340=CARTESIAN_POINT('Ctrl Pts',(-0.026390801400978,0.170972456562021,
0.0476530087366796));
#18341=CARTESIAN_POINT('Ctrl Pts',(-0.157993800025737,0.070491178324729,
0.0555951768594596));
#18342=CARTESIAN_POINT('Ctrl Pts',(-0.144863967768493,-0.0945835600760224,
0.0635373449822396));
#18343=CARTESIAN_POINT('Ctrl Pts',(0.000979154756195248,-0.17300145605975,
0.0714795131050195));
#18344=CARTESIAN_POINT('Ctrl Pts',(0.145923683802689,-0.0929367665856833,
0.0794216812277997));
#18345=CARTESIAN_POINT('Ctrl Pts',(0.157187963117837,0.0722699302633024,
0.0873638493505794));
#18346=CARTESIAN_POINT('Ctrl Pts',(0.0244514793930555,0.171268692120756,
0.0953060174733598));
#18347=CARTESIAN_POINT('Ctrl Pts',(-0.130684839550095,0.113368397534175,
0.103248185596139));
#18348=CARTESIAN_POINT('Ctrl Pts',(-0.166100541844429,-0.0483893439312075,
0.11119035371892));
#18349=CARTESIAN_POINT('Ctrl Pts',(-0.0493510193195793,-0.165817291858885,
0.119132521841699));
#18350=CARTESIAN_POINT('Ctrl Pts',(0.112609073040783,-0.131339661914923,
0.12707468996448));
#18351=CARTESIAN_POINT('Ctrl Pts',(0.17140770357293,0.0234586422209967,
0.135016858087259));
#18352=CARTESIAN_POINT('Ctrl Pts',(0.0731792588499177,0.156766393306209,
0.14295902621004));
#18353=CARTESIAN_POINT('Ctrl Pts',(-0.0920889000195865,0.146460037003638,
0.150901194332819));
#18354=CARTESIAN_POINT('Ctrl Pts',(-0.172994168426659,0.00198123296575728,
0.1588433624556));
#18355=CARTESIAN_POINT('Ctrl Pts',(-0.0954190048152776,-0.144312580095855,
0.16678553057838));
#18356=CARTESIAN_POINT('Ctrl Pts',(0.0695697692503139,-0.158401246055831,
0.17472769870116));
#18357=CARTESIAN_POINT('Ctrl Pts',(0.170825487889685,-0.0273780963649298,
0.18266986682394));
#18358=CARTESIAN_POINT('Ctrl Pts',(0.115587509852263,0.128726201683253,
0.19061203494672));
#18359=CARTESIAN_POINT('Ctrl Pts',(-0.0455405018601966,0.16690407474553,
0.198554203069499));
#18360=CARTESIAN_POINT('Ctrl Pts',(-0.164948735370872,0.0521806684752238,
0.20649637119228));
#18361=CARTESIAN_POINT('Ctrl Pts',(-0.133246981425072,-0.110345590758605,
0.214438539315059));
#18362=CARTESIAN_POINT('Ctrl Pts',(0.0205226964731592,-0.171783952668295,
0.22238070743784));
#18363=CARTESIAN_POINT('Ctrl Pts',(0.155491476033395,-0.0758505658746651,
0.230322875560619));
#18364=CARTESIAN_POINT('Ctrl Pts',(0.148014089296488,0.0895697316726553,
0.2382650436834));
#18365=CARTESIAN_POINT('Ctrl Pts',(0.00494059070111224,0.172934953166096,
0.24620721180618));
#18366=CARTESIAN_POINT('Ctrl Pts',(-0.142658996543838,0.0978739912732451,
0.25414937992896));
#18367=CARTESIAN_POINT('Ctrl Pts',(-0.159568287038446,-0.0668496016012732,
0.262091548051739));
#18368=CARTESIAN_POINT('Ctrl Pts',(-0.0302966335331915,-0.170332091689456,
0.27003371617452));
#18369=CARTESIAN_POINT('Ctrl Pts',(0.126729848780061,-0.11777288690896,
0.2779758842973));
#18370=CARTESIAN_POINT('Ctrl Pts',(0.167658770158652,0.0426783815482623,
0.28591805242008));
#18371=CARTESIAN_POINT('Ctrl Pts',(0.0549950338320791,0.164031867990689,
0.293860220542859));
#18372=CARTESIAN_POINT('Ctrl Pts',(-0.108049803339193,0.135115311719503,
0.30180238866564));
#18373=CARTESIAN_POINT('Ctrl Pts',(-0.1721099202737,-0.0175807510100837,
0.309744556788419));
#18374=CARTESIAN_POINT('Ctrl Pts',(-0.0784996687135917,-0.154171039675278,
0.3176867249112));
#18375=CARTESIAN_POINT('Ctrl Pts',(0.087024343965547,-0.14952481740522,
0.325628893033979));
#18376=CARTESIAN_POINT('Ctrl Pts',(0.172825117221703,-0.00789850112384905,
0.33357106115676));
#18377=CARTESIAN_POINT('Ctrl Pts',(0.100300328103893,0.140963653630822,
0.341513229279539));
#18378=CARTESIAN_POINT('Ctrl Pts',(-0.0641098658012952,0.160688619913292,
0.349455397402319));
#18379=CARTESIAN_POINT('Ctrl Pts',(-0.16978883637574,0.033206302186043,
0.357397565525099));
#18380=CARTESIAN_POINT('Ctrl Pts',(-0.119923789760104,-0.124696399756661,
0.36533973364788));
#18381=CARTESIAN_POINT('Ctrl Pts',(0.0398037685148125,-0.168364388974385,
0.373281901770659));
#18382=CARTESIAN_POINT('Ctrl Pts',(0.163066985633654,-0.0577933011607096,
0.38122406989344));
#18383=CARTESIAN_POINT('Ctrl Pts',(0.136944091404129,0.10572238784759,0.38916623801622));
#18384=CARTESIAN_POINT('Ctrl Pts',(-0.0146336593526265,0.172385508313924,
0.397108406138999));
#18385=CARTESIAN_POINT('Ctrl Pts',(-0.152805474769431,0.0811257933285562,
0.40505057426178));
#18386=CARTESIAN_POINT('Ctrl Pts',(-0.150991776994562,-0.0844534827151793,
0.412992742384559));
#18387=CARTESIAN_POINT('Ctrl Pts',(-0.0108540995180527,-0.172664692355881,
0.42093491050734));
#18388=CARTESIAN_POINT('Ctrl Pts',(0.139227048201004,-0.102697305280782,
0.428877078630119));
#18389=CARTESIAN_POINT('Ctrl Pts',(0.16176191642983,0.0613513639265466,
0.4368192467529));
#18390=CARTESIAN_POINT('Ctrl Pts',(0.0361062507758455,0.169195880912067,
0.444761414875679));
#18391=CARTESIAN_POINT('Ctrl Pts',(-0.12262644992489,0.12203958882886,0.45270358299846));
#18392=CARTESIAN_POINT('Ctrl Pts',(-0.169020724600573,-0.0369175042249048,
0.460645751121239));
#18393=CARTESIAN_POINT('Ctrl Pts',(-0.0605746513833496,-0.162054370729346,
0.468587919244019));
#18394=CARTESIAN_POINT('Ctrl Pts',(0.103364025571403,-0.138732785167649,
0.4765300873668));
#18395=CARTESIAN_POINT('Ctrl Pts',(0.172610636112938,0.0116822841681558,
0.484472255489579));
#18396=CARTESIAN_POINT('Ctrl Pts',(0.083728171010617,0.151395181039277,
0.49241442361236));
#18397=CARTESIAN_POINT('Ctrl Pts',(-0.081857900459256,0.152414538660527,
0.500356591735139));
#18398=CARTESIAN_POINT('Ctrl Pts',(-0.172453725526818,0.0138065207282529,
0.50829875985792));
#18399=CARTESIAN_POINT('Ctrl Pts',(-0.105064221167447,-0.137449688588867,
0.516240927980699));
#18400=CARTESIAN_POINT('Ctrl Pts',(0.0585749034388466,-0.162787862415564,
0.52418309610348));
#18401=CARTESIAN_POINT('Ctrl Pts',(0.168553398866689,-0.0389956304370821,
0.532125264226259));
#18402=CARTESIAN_POINT('Ctrl Pts',(0.124119664784058,0.120520605195094,
0.54006743234904));
#18403=CARTESIAN_POINT('Ctrl Pts',(-0.0340204335384149,0.16962758491636,
0.548009600471819));
#18404=CARTESIAN_POINT('Ctrl Pts',(-0.160994319687769,0.0633382703503284,
0.5559517685946));
#18405=CARTESIAN_POINT('Ctrl Pts',(-0.14048086942825,-0.100975406844349,
0.563893936717379));
#18406=CARTESIAN_POINT('Ctrl Pts',(0.00872748937560605,-0.172785237771916,
0.57183610484016));
#18407=CARTESIAN_POINT('Ctrl Pts',(0.149940571302356,-0.0863060399984934,
0.579778272962939));
#18408=CARTESIAN_POINT('Ctrl Pts',(0.153792685935992,0.0792383569699183,
0.58772044108572));
#18409=CARTESIAN_POINT('Ctrl Pts',(0.0167549005293281,0.17219227848818,
0.595662609208499));
#18410=CARTESIAN_POINT('Ctrl Pts',(-0.135632095058532,0.107400382926376,
0.60360477733128));
#18411=CARTESIAN_POINT('Ctrl Pts',(-0.163766157558233,-0.0557812970565469,
0.611546945454059));
#18412=CARTESIAN_POINT('Ctrl Pts',(-0.0418735953979919,-0.167861578305293,
0.61948911357684));
#18413=CARTESIAN_POINT('Ctrl Pts',(0.118379481984711,-0.126163408751231,
0.627431281699619));
#18414=CARTESIAN_POINT('Ctrl Pts',(0.17018479228316,0.0311134044783985,
0.6353734498224));
#18415=CARTESIAN_POINT('Ctrl Pts',(0.0660833491022344,0.159887142804326,
0.643315617945179));
#18416=CARTESIAN_POINT('Ctrl Pts',(-0.0985572308567358,0.142187832491218,
0.651257786067961));
#18417=CARTESIAN_POINT('Ctrl Pts',(-0.172909262181909,-0.00577013989488307,
0.659199954190738));
#18418=CARTESIAN_POINT('Ctrl Pts',(-0.0888586457050277,-0.148442071348278,
0.667142122313521));
#18419=CARTESIAN_POINT('Ctrl Pts',(0.0765956190331784,-0.155125815413241,
0.675084290436298));
#18420=CARTESIAN_POINT('Ctrl Pts',(0.171880427770071,-0.0196983758791502,
0.683026458559081));
#18421=CARTESIAN_POINT('Ctrl Pts',(0.109705106722326,0.133774799651286,
0.690968626681858));
#18422=CARTESIAN_POINT('Ctrl Pts',(-0.0529713625168984,0.164696515493808,
0.698910794804641));
#18423=CARTESIAN_POINT('Ctrl Pts',(-0.167120621735807,0.0447393032280997,
0.706852962927418));
#18424=CARTESIAN_POINT('Ctrl Pts',(-0.12817022249092,-0.116203707037801,
0.7147951310502));
#18425=CARTESIAN_POINT('Ctrl Pts',(0.0281972679828983,-0.17069218359667,
0.722737299172979));
#18426=CARTESIAN_POINT('Ctrl Pts',(0.158733164168978,-0.0688090841067,0.73067946729576));
#18427=CARTESIAN_POINT('Ctrl Pts',(0.14385317469873,0.0961102054508026,
0.738621635418538));
#18428=CARTESIAN_POINT('Ctrl Pts',(-0.00281110139369983,0.172982673038814,
0.746563803541321));
#18429=CARTESIAN_POINT('Ctrl Pts',(-0.146900119814081,0.0913852409380608,
0.754505971664098));
#18430=CARTESIAN_POINT('Ctrl Pts',(-0.156413536862055,-0.0739304602244656,
0.762448139786881));
#18431=CARTESIAN_POINT('Ctrl Pts',(-0.0226360851712103,-0.171518264656626,
0.770390307909658));
#18432=CARTESIAN_POINT('Ctrl Pts',(0.131878346029848,-0.111977717922496,
0.778332476032441));
#18433=CARTESIAN_POINT('Ctrl Pts',(0.165578663890314,0.0501459223366878,
0.786274644155218));
#18434=CARTESIAN_POINT('Ctrl Pts',(0.047591915084802,0.166330746049129,
0.794216812278001));
#18435=CARTESIAN_POINT('Ctrl Pts',(-0.113993917241593,0.130139518573781,
0.802158980400778));
#18436=CARTESIAN_POINT('Ctrl Pts',(-0.171149610334614,-0.0252728776558711,
0.81010114852356));
#18437=CARTESIAN_POINT('Ctrl Pts',(-0.0715146774936035,-0.157532721571376,
0.818043316646339));
#18438=CARTESIAN_POINT('Ctrl Pts',(0.0936350469135118,-0.14547640857611,
0.825985484769119));
#18439=CARTESIAN_POINT('Ctrl Pts',(0.173005448853992,-0.000148759965830227,
0.8339276528919));
#18440=CARTESIAN_POINT('Ctrl Pts',(0.0938850861191564,0.145315168055841,
0.841869821014678));
#18441=CARTESIAN_POINT('Ctrl Pts',(-0.0712436606821878,0.157655473343934,
0.849811989137461));
#18442=CARTESIAN_POINT('Ctrl Pts',(-0.171105895159299,0.0255671684868261,
0.857754157260238));
#18443=CARTESIAN_POINT('Ctrl Pts',(-0.114217551294,-0.129943289319231,0.86569632538302));
#18444=CARTESIAN_POINT('Ctrl Pts',(0.0473058035714782,-0.166412344527548,
0.873638493505798));
#18445=CARTESIAN_POINT('Ctrl Pts',(0.16549218245563,-0.0504305959589149,
0.88158066162858));
#18446=CARTESIAN_POINT('Ctrl Pts',(0.132070720552549,0.111750759440056,
0.889522829751358));
#18447=CARTESIAN_POINT('Ctrl Pts',(-0.022341089517305,0.171556938600217,
0.89746499787414));
#18448=CARTESIAN_POINT('Ctrl Pts',(-0.156286166401977,0.074199337288632,
0.905407165996919));
#18449=CARTESIAN_POINT('Ctrl Pts',(-0.147057058974526,-0.0911324797668838,
0.913349334119699));
#18450=CARTESIAN_POINT('Ctrl Pts',(-0.00310857778072832,-0.172977582960567,
0.92129150224248));
#18451=CARTESIAN_POINT('Ctrl Pts',(0.143687680016546,-0.0963574495000853,
0.929233670365259));
#18452=CARTESIAN_POINT('Ctrl Pts',(0.158851261322436,0.0685360068793772,
0.93717583848804));
#18453=CARTESIAN_POINT('Ctrl Pts',(0.0284907678468484,0.170643439985825,
0.945118006610819));
#18454=CARTESIAN_POINT('Ctrl Pts',(-0.127970195944242,0.116423951198588,
0.9530601747336));
#18455=CARTESIAN_POINT('Ctrl Pts',(-0.167197313372666,-0.0444518375735043,
0.961002342856378));
#18456=CARTESIAN_POINT('Ctrl Pts',(-0.0532545149190986,-0.164605176417482,
0.96894451097916));
#18457=CARTESIAN_POINT('Ctrl Pts',(0.10947489024455,-0.133963263130763,
0.976886679101939));
#18458=CARTESIAN_POINT('Ctrl Pts',(0.1719140491614,0.0194027617526574,0.984828847224719));
#18459=CARTESIAN_POINT('Ctrl Pts',(0.0768622776450996,0.154993863549195,
0.992771015347499));
#18460=CARTESIAN_POINT('Ctrl Pts',(-0.088603236555915,0.148594663210074,
1.00071318347028));
#18461=CARTESIAN_POINT('Ctrl Pts',(-0.172899083515371,0.00606748566075909,
1.00865535159306));
#18462=CARTESIAN_POINT('Ctrl Pts',(-0.0988016073770141,-0.142018132090297,
1.01659751971584));
#18463=CARTESIAN_POINT('Ctrl Pts',(0.0658082913934689,-0.160000550769587,
1.02453968783862));
#18464=CARTESIAN_POINT('Ctrl Pts',(0.170131034504888,-0.0314060274628177,
1.0324818559614));
#18465=CARTESIAN_POINT('Ctrl Pts',(0.118596271784576,0.125959643463681,
1.04042402408418));
#18466=CARTESIAN_POINT('Ctrl Pts',(-0.0415848597483297,0.167933340651612,
1.04836619220696));
#18467=CARTESIAN_POINT('Ctrl Pts',(-0.163669987576804,0.0560628453550813,
1.05630836032974));
#18468=CARTESIAN_POINT('Ctrl Pts',(-0.135816592328243,-0.107166975841641,
1.06425052845252));
#18469=CARTESIAN_POINT('Ctrl Pts',(0.0164587544616562,-0.172220837485682,
1.0721926965753));
#18470=CARTESIAN_POINT('Ctrl Pts',(0.153656191292587,-0.0795027190739688,
1.08013486469808));
#18471=CARTESIAN_POINT('Ctrl Pts',(0.150088771199207,0.0860480576341552,
1.08807703282086));
#18472=CARTESIAN_POINT('Ctrl Pts',(0.00902461748204118,0.172769973496559,
1.09601920094364));
#18473=CARTESIAN_POINT('Ctrl Pts',(-0.140307012982855,0.101216844302358,
1.10396136906642));
#18474=CARTESIAN_POINT('Ctrl Pts',(-0.161103005268346,-0.0630613126743013,
1.1119035371892));
#18475=CARTESIAN_POINT('Ctrl Pts',(-0.0343120939874615,-0.1695688287065,
1.11984570531198));
#18476=CARTESIAN_POINT('Ctrl Pts',(0.123912220401285,-0.120733877175888,
1.12778787343476));
#18477=CARTESIAN_POINT('Ctrl Pts',(0.168620210916381,0.0387057093103061,
1.13573004155754));
#18478=CARTESIAN_POINT('Ctrl Pts',(0.0588547652196237,0.162686889679659,
1.14367220968032));
#18479=CARTESIAN_POINT('Ctrl Pts',(-0.104827691798069,0.137630165643247,
1.1516143778031));
#18480=CARTESIAN_POINT('Ctrl Pts',(-0.172477213770776,-0.0135099294065116,
1.15955654592588));
#18481=CARTESIAN_POINT('Ctrl Pts',(-0.0821198886720452,-0.152273541192125,
1.16749871404866));
#18482=CARTESIAN_POINT('Ctrl Pts',(0.083467690946984,-0.15153894559049,
1.17544088217144));
#18483=CARTESIAN_POINT('Ctrl Pts',(0.172590290696882,-0.0119791076405788,
1.18338305029422));
#18484=CARTESIAN_POINT('Ctrl Pts',(0.103602453294194,0.13855482356859,1.191325218417));
#18485=CARTESIAN_POINT('Ctrl Pts',(-0.0602958748103966,0.162158302111078,
1.19926738653978));
#18486=CARTESIAN_POINT('Ctrl Pts',(-0.168956987158091,0.0372081167644847,
1.20720955466256));
#18487=CARTESIAN_POINT('Ctrl Pts',(-0.122836141658186,-0.121828526073448,
1.21515172278534));
#18488=CARTESIAN_POINT('Ctrl Pts',(0.0358152290369173,-0.169257723108079,
1.22309389090812));
#18489=CARTESIAN_POINT('Ctrl Pts',(0.161656170495932,-0.0616294572691503,
1.2310360590309));
#18490=CARTESIAN_POINT('Ctrl Pts',(0.13940345221127,0.102457722863032,1.23897822715368));
#18491=CARTESIAN_POINT('Ctrl Pts',(-0.0105571497596809,0.172683102970871,
1.24692039527646));
#18492=CARTESIAN_POINT('Ctrl Pts',(-0.150846317973597,0.0847130203482025,
1.25486256339924));
#18493=CARTESIAN_POINT('Ctrl Pts',(-0.152944761892581,-0.0808628918127005,
1.26280473152202));
#18494=CARTESIAN_POINT('Ctrl Pts',(-0.0149300913057054,-0.172360087712588,
1.2707468996448));
#18495=CARTESIAN_POINT('Ctrl Pts',(0.136762076743997,-0.105957736043287,
1.27868906776758));
#18496=CARTESIAN_POINT('Ctrl Pts',(0.163166132393764,0.0575127872937276,
1.28663123589036));
#18497=CARTESIAN_POINT('Ctrl Pts',(0.0400932480780463,0.168295688956082,
1.29457340401314));
#18498=CARTESIAN_POINT('Ctrl Pts',(-0.119709170414695,0.124902449862528,
1.30251557213592));
#18499=CARTESIAN_POINT('Ctrl Pts',(-0.169845690614082,-0.0329142650230248,
1.3104577402587));
#18500=CARTESIAN_POINT('Ctrl Pts',(-0.0643861093061943,-0.160578131733314,
1.31839990838148));
#18501=CARTESIAN_POINT('Ctrl Pts',(0.100057762773863,-0.141135932963798,
1.32634207650426));
#18502=CARTESIAN_POINT('Ctrl Pts',(0.172838444806952,0.00760127985757451,
1.33428424462704));
#18503=CARTESIAN_POINT('Ctrl Pts',(0.0872813550697656,0.149374939398002,
1.34222641274982));
#18504=CARTESIAN_POINT('Ctrl Pts',(-0.0782344227434143,0.154305808621531,
1.3501685808726));
#18505=CARTESIAN_POINT('Ctrl Pts',(-0.172079431848303,0.0178767046294837,
1.35811074899538));
#18506=CARTESIAN_POINT('Ctrl Pts',(-0.108282003268856,-0.134929297194493,
1.36605291711816));
#18507=CARTESIAN_POINT('Ctrl Pts',(0.0547128650701426,-0.164126201264144,
1.37399508524094));
#18508=CARTESIAN_POINT('Ctrl Pts',(0.167585127127835,-0.0429666431014547,
1.38193725336372));
#18509=CARTESIAN_POINT('Ctrl Pts',(0.126932197981417,0.117554773230619,
1.3898794214865));
#18510=CARTESIAN_POINT('Ctrl Pts',(-0.0300036684000219,0.170383942402052,
1.39782158960928));
#18511=CARTESIAN_POINT('Ctrl Pts',(-0.159453085214751,0.0671239123677834,
1.40576375773206));
#18512=CARTESIAN_POINT('Ctrl Pts',(-0.142827107870127,-0.0976285101620078,
1.41370592585484));
#18513=CARTESIAN_POINT('Ctrl Pts',(0.00464319840846943,-0.172943201171859,
1.42164809397762));
#18514=CARTESIAN_POINT('Ctrl Pts',(0.147859810582222,-0.0898241270588577,
1.4295902621004));
#18515=CARTESIAN_POINT('Ctrl Pts',(0.155621735944117,0.0755830265922534,
1.43753243022318));
#18516=CARTESIAN_POINT('Ctrl Pts',(0.0208179928734729,0.171748455656582,
1.44547459834596));
#18517=CARTESIAN_POINT('Ctrl Pts',(-0.133056846329205,0.11057447892796,
1.45341676646874));
#18518=CARTESIAN_POINT('Ctrl Pts',(-0.165038560097216,-0.0518967460486161,
1.46135893459152));
#18519=CARTESIAN_POINT('Ctrl Pts',(-0.0458268296361176,-0.166825854601292,
1.4693011027143));
#18520=CARTESIAN_POINT('Ctrl Pts',(0.115364766925686,-0.128924136976022,
1.47724327083708));
#18521=CARTESIAN_POINT('Ctrl Pts',(0.170874595884426,0.0270830477535184,
1.48518543895986));
#18522=CARTESIAN_POINT('Ctrl Pts',(0.0698377457337486,0.158283721017069,
1.49312760708264));
#18523=CARTESIAN_POINT('Ctrl Pts',(-0.0951624750893037,0.144471999488883,
1.50106977520542));
#18524=CARTESIAN_POINT('Ctrl Pts',(-0.173012914651864,-0.00167525885548286,
1.5090119433282));
#18525=CARTESIAN_POINT('Ctrl Pts',(-0.092311001583214,-0.14631755460685,
1.51695411145098));
#18526=CARTESIAN_POINT('Ctrl Pts',(0.072853104778531,-0.156861289272697,
1.52489627957376));
#18527=CARTESIAN_POINT('Ctrl Pts',(0.171475934783304,-0.0238129810547936,
1.53283844769654));
#18528=CARTESIAN_POINT('Ctrl Pts',(0.11261423476106,0.131269690464983,1.54078061581932));
#18529=CARTESIAN_POINT('Ctrl Pts',(0.00518264413773371,0.154149172621267,
1.54607539456784));
#18530=CARTESIAN_POINT('Ctrl Pts',(-0.0415060733757155,0.140340900570467,
1.5487227839421));
#18531=CARTESIAN_POINT('Ctrl Pts',(-0.146248097568756,-0.000123763188177425,
1.45893449541571));
#18532=CARTESIAN_POINT('Ctrl Pts',(-0.146367493381718,-0.0150081347743067,
1.45974264180765));
#18533=CARTESIAN_POINT('Ctrl Pts',(-0.144277648885518,-0.0298597803798721,
1.46055078819958));
#18534=CARTESIAN_POINT('Ctrl Pts',(-0.139839652725699,-0.043973059977961,
1.46135893459152));
#18535=CARTESIAN_POINT('Ctrl Pts',(-0.125301316610186,-0.0902064488995044,
1.46400632396578));
#18536=CARTESIAN_POINT('Ctrl Pts',(-0.08556407312315,-0.1285161517504,1.46665371334004));
#18537=CARTESIAN_POINT('Ctrl Pts',(-0.0388301852859989,-0.141354050238301,
1.4693011027143));
#18538=CARTESIAN_POINT('Ctrl Pts',(0.00790370255115092,-0.154191948726202,
1.47194849208856));
#18539=CARTESIAN_POINT('Ctrl Pts',(0.0616342347384179,-0.141558042851112,
1.47459588146282));
#18540=CARTESIAN_POINT('Ctrl Pts',(0.0977511389918415,-0.109239892458645,
1.47724327083708));
#18541=CARTESIAN_POINT('Ctrl Pts',(0.133868043245265,-0.0769217420661769,
1.47989066021134));
#18542=CARTESIAN_POINT('Ctrl Pts',(0.152371319564846,-0.024919347156331,
1.4825380495856));
#18543=CARTESIAN_POINT('Ctrl Pts',(0.144783482699524,0.0229486291758506,
1.48518543895986));
#18544=CARTESIAN_POINT('Ctrl Pts',(0.137195645834202,0.0708166055080336,
1.48783282833412));
#18545=CARTESIAN_POINT('Ctrl Pts',(0.103516695783975,0.114550163262552,
1.49048021770838));
#18546=CARTESIAN_POINT('Ctrl Pts',(0.0591771839550196,0.13411498855178,
1.49312760708264));
#18547=CARTESIAN_POINT('Ctrl Pts',(0.014837672126065,0.153679813841007,
1.4957749964569));
#18548=CARTESIAN_POINT('Ctrl Pts',(-0.0401624014816186,0.149075906664945,
1.49842238583116));
#18549=CARTESIAN_POINT('Ctrl Pts',(-0.0806375115458872,0.122416076686187,
1.50106977520542));
#18550=CARTESIAN_POINT('Ctrl Pts',(-0.0937869288003098,0.113754921033589,
1.50192985013695));
#18551=CARTESIAN_POINT('Ctrl Pts',(-0.105403311347291,0.102765876910903,
1.50278992506847));
#18552=CARTESIAN_POINT('Ctrl Pts',(-0.115078604842433,0.0902138214954038,
1.50365));
#18553=CARTESIAN_POINT('Ctrl Pts',(-0.0686146973663081,-0.0959584553529135,
1.07336015076065E-17));
#18554=CARTESIAN_POINT('Ctrl Pts',(-0.0712979561985307,-0.0944995001033786,
9.02613639135873E-18));
#18555=CARTESIAN_POINT('Ctrl Pts',(-0.0739152333025289,-0.0929325179580126,
1.64107321374712E-17));
#18556=CARTESIAN_POINT('Ctrl Pts',(-0.0764591723283171,-0.0912589988675934,
1.6154612370034E-17));
#18557=CARTESIAN_POINT('Ctrl Pts',(-0.0824897891353913,-0.0872917841461184,
1.52077426268717E-17));
#18558=CARTESIAN_POINT('Ctrl Pts',(-0.0881090519769445,-0.0827275518978924,
1.30971627060498E-17));
#18559=CARTESIAN_POINT('Ctrl Pts',(-0.0932912133381108,-0.0776621329443405,
1.43114686768087E-17));
#18560=CARTESIAN_POINT('Ctrl Pts',(-0.0960634919631888,-0.074952307504085,
1.49610807310118E-17));
#18561=CARTESIAN_POINT('Ctrl Pts',(-0.0987043519497191,-0.0721043812799658,
1.74993329480528E-17));
#18562=CARTESIAN_POINT('Ctrl Pts',(-0.101206237074718,-0.0691378820326018,
9.97465998686664E-18));
#18563=CARTESIAN_POINT('Ctrl Pts',(-0.105823426721714,-0.0636632543305198,
-3.91200561030858E-18));
#18564=CARTESIAN_POINT('Ctrl Pts',(-0.109972666997065,-0.0577811896139199,
2.24798207762934E-18));
#18565=CARTESIAN_POINT('Ctrl Pts',(-0.113625452403263,-0.0515741981665521,
9.54097911787244E-18));
#18566=CARTESIAN_POINT('Ctrl Pts',(-0.115386295340069,-0.0485820878086944,
1.30566037435822E-17));
#18567=CARTESIAN_POINT('Ctrl Pts',(-0.117027309103105,-0.0455212415157476,
-2.79521757168051E-18));
#18568=CARTESIAN_POINT('Ctrl Pts',(-0.118543833519887,-0.0424058589801268,
-3.46944695195361E-18));
#18569=CARTESIAN_POINT('Ctrl Pts',(-0.122700941917732,-0.0338659484069709,
-5.31764971597768E-18));
#18570=CARTESIAN_POINT('Ctrl Pts',(-0.125931492798984,-0.0249085743588085,
-1.15219401683824E-18));
#18571=CARTESIAN_POINT('Ctrl Pts',(-0.128167520083254,-0.0157105262534848,
9.54097911787244E-18));
#18572=CARTESIAN_POINT('Ctrl Pts',(-0.128992166906242,-0.0123182862745252,
1.3484621181291E-17));
#18573=CARTESIAN_POINT('Ctrl Pts',(-0.129681150280034,-0.00889298553317688,
1.10989611676181E-17));
#18574=CARTESIAN_POINT('Ctrl Pts',(-0.130229483957028,-0.00544263935519351,
9.54097911787244E-18));
#18575=CARTESIAN_POINT('Ctrl Pts',(-0.130761899349706,-0.00209245771889707,
8.02822573502553E-18));
#18576=CARTESIAN_POINT('Ctrl Pts',(-0.131160261982709,0.00127366115726457,
1.11791151702242E-17));
#18577=CARTESIAN_POINT('Ctrl Pts',(-0.131420990891747,0.00464012593483382,
8.67361737988404E-18));
#18578=CARTESIAN_POINT('Ctrl Pts',(-0.131728666658755,0.00861275649723166,
5.71697955546795E-18));
#18579=CARTESIAN_POINT('Ctrl Pts',(-0.131845259942619,0.0125891451047215,
-9.26473565962443E-18));
#18580=CARTESIAN_POINT('Ctrl Pts',(-0.131765781147177,0.0165567997877194,
-1.04083408558608E-17));
#18581=CARTESIAN_POINT('Ctrl Pts',(-0.131635692412819,0.0230509492424239,
-1.21888544026837E-17));
#18582=CARTESIAN_POINT('Ctrl Pts',(-0.13098103789945,0.0295216962360144,
-2.67049856555875E-17));
#18583=CARTESIAN_POINT('Ctrl Pts',(-0.129839098367345,0.0359278479980343,
-3.46944695195361E-17));
#18584=CARTESIAN_POINT('Ctrl Pts',(-0.129254890951344,0.0392051855997028,
-3.87818275556788E-17));
#18585=CARTESIAN_POINT('Ctrl Pts',(-0.128542951403208,0.0424656461998481,
-3.10678831811161E-17));
#18586=CARTESIAN_POINT('Ctrl Pts',(-0.1277070993652,0.0457037274559979,
-3.29597460435593E-17));
#18587=CARTESIAN_POINT('Ctrl Pts',(-0.126886363095037,0.0488832504000222,
-3.48173959609792E-17));
#18588=CARTESIAN_POINT('Ctrl Pts',(-0.125948031872817,0.0520333657183593,
-3.53366201082739E-17));
#18589=CARTESIAN_POINT('Ctrl Pts',(-0.124899042599898,0.0551436241923499,
-3.46944695195361E-17));
#18590=CARTESIAN_POINT('Ctrl Pts',(-0.122234979928128,0.0630425834229368,
-3.30636335736642E-17));
#18591=CARTESIAN_POINT('Ctrl Pts',(-0.118856305871375,0.070695441500891,
-2.1366080483524E-17));
#18592=CARTESIAN_POINT('Ctrl Pts',(-0.114834854776346,0.078019637496205,
-1.73472347597681E-17));
#18593=CARTESIAN_POINT('Ctrl Pts',(-0.11215901866562,0.0828930893082948,
-1.46731322388254E-17));
#18594=CARTESIAN_POINT('Ctrl Pts',(-0.109198005187061,0.0876211033078822,
8.28606628989234E-18));
#18595=CARTESIAN_POINT('Ctrl Pts',(-0.105966883726074,0.0921780034666525,
8.67361737988404E-18));
#18596=CARTESIAN_POINT('Ctrl Pts',(-0.104137243112614,0.094758373688769,
8.89307035390601E-18));
#18597=CARTESIAN_POINT('Ctrl Pts',(-0.102221042121924,0.0972831505018574,
-2.31209379389524E-17));
#18598=CARTESIAN_POINT('Ctrl Pts',(-0.100229777791505,0.0997373632832089,
-2.08166817117217E-17));
#18599=CARTESIAN_POINT('Ctrl Pts',(-0.0937202782075859,0.107760254486057,
-1.32840027382311E-17));
#18600=CARTESIAN_POINT('Ctrl Pts',(-0.0863914655699752,0.115060936709644,
5.4842312373535E-18));
#18601=CARTESIAN_POINT('Ctrl Pts',(-0.0783508402622743,0.121487309774744,
1.38777878078145E-17));
#18602=CARTESIAN_POINT('Ctrl Pts',(-0.073610711791116,0.125275800441382,
1.8825977152717E-17));
#18603=CARTESIAN_POINT('Ctrl Pts',(-0.068622257850438,0.128760167547443,
-9.09579695168528E-18));
#18604=CARTESIAN_POINT('Ctrl Pts',(-0.0634007094575209,0.131904027763685,
-6.93889390390723E-18));
#18605=CARTESIAN_POINT('Origin',(0.,0.,0.));
#18606=CARTESIAN_POINT('Origin',(-0.0721687836487033,-0.125,-0.3));
#18607=CARTESIAN_POINT('',(-0.0721687836487033,-0.125,-0.3));
#18608=CARTESIAN_POINT('',(0.0721687836487032,-0.125,-0.3));
#18609=CARTESIAN_POINT('',(-0.0360843918243517,-0.125,-0.3));
#18610=CARTESIAN_POINT('',(-0.0721687836487033,-0.125,-0.15));
#18611=CARTESIAN_POINT('',(-0.0721687836487033,-0.125,-0.3));
#18612=CARTESIAN_POINT('',(0.0721687836487032,-0.125,-0.15));
#18613=CARTESIAN_POINT('',(-0.0721687836487033,-0.125,-0.15));
#18614=CARTESIAN_POINT('',(0.0721687836487032,-0.125,-0.3));
#18615=CARTESIAN_POINT('Origin',(-0.144337567297406,1.76762539787485E-17,
-0.3));
#18616=CARTESIAN_POINT('',(-0.144337567297406,1.76762539787485E-17,-0.3));
#18617=CARTESIAN_POINT('',(-0.126295371385231,-0.03125,-0.3));
#18618=CARTESIAN_POINT('',(-0.144337567297406,2.77555756156289E-17,-0.15));
#18619=CARTESIAN_POINT('',(-0.144337567297406,1.76762539787485E-17,-0.3));
#18620=CARTESIAN_POINT('',(-0.144337567297406,1.76762539787485E-17,-0.15));
#18621=CARTESIAN_POINT('Origin',(-0.0721687836487032,0.125,-0.3));
#18622=CARTESIAN_POINT('',(-0.0721687836487032,0.125,-0.3));
#18623=CARTESIAN_POINT('',(-0.090210979560879,0.09375,-0.3));
#18624=CARTESIAN_POINT('',(-0.0721687836487032,0.125,-0.15));
#18625=CARTESIAN_POINT('',(-0.0721687836487032,0.125,-0.3));
#18626=CARTESIAN_POINT('',(-0.0721687836487032,0.125,-0.15));
#18627=CARTESIAN_POINT('Origin',(0.0721687836487032,0.125,-0.3));
#18628=CARTESIAN_POINT('',(0.0721687836487032,0.125,-0.3));
#18629=CARTESIAN_POINT('',(0.0360843918243516,0.125,-0.3));
#18630=CARTESIAN_POINT('',(0.0721687836487032,0.125,-0.15));
#18631=CARTESIAN_POINT('',(0.0721687836487032,0.125,-0.3));
#18632=CARTESIAN_POINT('',(0.0721687836487032,0.125,-0.15));
#18633=CARTESIAN_POINT('Origin',(0.144337567297406,0.,-0.3));
#18634=CARTESIAN_POINT('',(0.144337567297406,0.,-0.3));
#18635=CARTESIAN_POINT('',(0.126295371385231,0.03125,-0.3));
#18636=CARTESIAN_POINT('',(0.144337567297406,0.,-0.15));
#18637=CARTESIAN_POINT('',(0.144337567297406,0.,-0.3));
#18638=CARTESIAN_POINT('',(0.144337567297406,0.,-0.15));
#18639=CARTESIAN_POINT('Origin',(0.0721687836487032,-0.125,-0.3));
#18640=CARTESIAN_POINT('',(0.0902109795608791,-0.09375,-0.3));
#18641=CARTESIAN_POINT('',(0.0721687836487032,-0.125,-0.15));
#18642=CARTESIAN_POINT('Origin',(0.,0.,-0.15));
#18643=CARTESIAN_POINT('Origin',(0.,0.,0.));
#18644=CARTESIAN_POINT('',(-0.275,-3.36777869765522E-17,0.));
#18645=CARTESIAN_POINT('Origin',(0.,0.,0.));
#18646=CARTESIAN_POINT('Origin',(0.,0.,-0.3));
#18647=CARTESIAN_POINT('',(-0.275,-3.36777869765522E-17,-0.3));
#18648=CARTESIAN_POINT('',(-0.275,-3.36777869765522E-17,-0.3));
#18649=CARTESIAN_POINT('Origin',(0.,0.,-0.3));
#18650=CARTESIAN_POINT('Origin',(0.,0.,-0.3));
#18651=CARTESIAN_POINT('Origin',(0.,0.,1.6));
#19602=UNCERTAINTY_MEASURE_WITH_UNIT(LENGTH_MEASURE(0.001),#19619,
'DISTANCE_ACCURACY_VALUE',
'Maximum model space distance between geometric entities at asserted c
onnectivities');
#19605=UNCERTAINTY_MEASURE_WITH_UNIT(LENGTH_MEASURE(0.001),#19619,
'DISTANCE_ACCURACY_VALUE',
'Maximum model space distance between geometric entities at asserted c
onnectivities');
#19615=(
GEOMETRIC_REPRESENTATION_CONTEXT(3)
GLOBAL_UNCERTAINTY_ASSIGNED_CONTEXT((#19602))
GLOBAL_UNIT_ASSIGNED_CONTEXT((#19619,#19621,#19622))
REPRESENTATION_CONTEXT('','3D')
);
#19618=(
GEOMETRIC_REPRESENTATION_CONTEXT(3)
GLOBAL_UNCERTAINTY_ASSIGNED_CONTEXT((#19605))
GLOBAL_UNIT_ASSIGNED_CONTEXT((#19619,#19621,#19622))
REPRESENTATION_CONTEXT('','3D')
);
#19619=(
LENGTH_UNIT()
NAMED_UNIT(*)
SI_UNIT(.CENTI.,.METRE.)
);
#19621=(
NAMED_UNIT(*)
PLANE_ANGLE_UNIT()
SI_UNIT($,.RADIAN.)
);
#19622=(
NAMED_UNIT(*)
SI_UNIT($,.STERADIAN.)
SOLID_ANGLE_UNIT()
);
#19632=SHAPE_DEFINITION_REPRESENTATION(#19644,#19672);
#19644=PRODUCT_DEFINITION_SHAPE('',$,#19685);
#19672=SHAPE_REPRESENTATION('',(#7636),#19615);
#19675=PRODUCT_DEFINITION_CONTEXT('part definition',#19713,'design');
#19685=PRODUCT_DEFINITION('2026-11-10-01-34-59-967',
'Socket head cap screw M3x16',#19697,#19675);
#19697=PRODUCT_DEFINITION_FORMATION('',$,#19724);
#19713=APPLICATION_CONTEXT(
'Core Data for Automotive Mechanical Design Process');
#19714=PRODUCT_CONTEXT('part definition',#19713,'mechanical');
#19724=PRODUCT('2026-11-10-01-34-59-967','Socket head cap screw M3x16',
$,(#19714));
#19730=PRESENTATION_STYLE_ASSIGNMENT((#19738));
#19738=SURFACE_STYLE_USAGE(.BOTH.,#19746);
#19746=SURFACE_SIDE_STYLE('',(#19754));
#19754=SURFACE_STYLE_FILL_AREA(#19762);
#19762=FILL_AREA_STYLE('Dark gray',(#19770));
#19770=FILL_AREA_STYLE_COLOUR('Dark gray',#19778);
#19778=COLOUR_RGB('Dark gray',0.250980392156863,0.282352941176471,0.32156862745098);
ENDSEC;
END-ISO-10303-21;
